ISO-10303-21;
HEADER;
FILE_DESCRIPTION (('STEP AP214'),
    '1' );
FILE_NAME ('3. Bracket.step',
    '2026-10-09T14:04:53',
    ( '' ),
    ( '' ),
    'SwSTEP 2.0',
    'SolidWorks 2021',
    '' );
FILE_SCHEMA (( 'AUTOMOTIVE_DESIGN' ));
ENDSEC;

DATA;
#12=DIRECTION ( 'NONE',  ( -1.000000000000000000, -0.000000000000000000, -0.000000000000000000 ) ) ;
#42=( LENGTH_UNIT ( ) NAMED_UNIT ( * ) SI_UNIT ( .MILLI., .METRE. ) );
#54=CARTESIAN_POINT ( 'NONE',  ( 1.000000000000000000, -32.16482459199326627, -4.060956965557648957 ) ) ;
#57=CARTESIAN_POINT ( 'NONE',  ( 12.30686711561308577, -4.727852861241523819, 20.32466816526829234 ) ) ;
#62=CARTESIAN_POINT ( 'NONE',  ( -2.120783755322036335, -49.78473794080423431, 102.5525762030298722 ) ) ;
#85=ORIENTED_EDGE ( 'NONE', *, *, #25518, .T. ) ;
#124=CARTESIAN_POINT ( 'NONE',  ( 4.284822031654965890, -1.092833614412281218, 104.4267991316945086 ) ) ;
#144=CARTESIAN_POINT ( 'NONE',  ( 6.999999999999995559, -46.00000000000000000, 39.12435565298213902 ) ) ;
#170=VERTEX_POINT ( 'NONE', #86462 ) ;
#185=ADVANCED_FACE ( 'NONE', ( #78858 ), #30718, .T. ) ;
#192=CARTESIAN_POINT ( 'NONE',  ( -3.604576940039468269, -48.95215848635412215, 104.3731177596929314 ) ) ;
#214=VERTEX_POINT ( 'NONE', #23851 ) ;
#222=CARTESIAN_POINT ( 'NONE',  ( -3.833028914485100636, -68.60312449208545615, 13.52676978846691469 ) ) ;
#253=DIRECTION ( 'NONE',  ( 0.000000000000000000, 0.000000000000000000, -1.000000000000000000 ) ) ;
#259=CARTESIAN_POINT ( 'NONE',  ( 15.95426957152705860, -2.597798534188847874, 14.77606491407465406 ) ) ;
#274=CARTESIAN_POINT ( 'NONE',  ( 2.923709067210019441, -69.56508743643901482, 13.30482931429384585 ) ) ;
#291=SURFACE_STYLE_USAGE ( .BOTH. , #18137 ) ;
#305=CARTESIAN_POINT ( 'NONE',  ( 5.000000000000000000, -15.25461064037142833, 12.58690023576579620 ) ) ;
#317=( GEOMETRIC_REPRESENTATION_CONTEXT ( 3 ) GLOBAL_UNCERTAINTY_ASSIGNED_CONTEXT ( ( #48311 ) ) GLOBAL_UNIT_ASSIGNED_CONTEXT ( ( #53769, #12768, #45689 ) ) REPRESENTATION_CONTEXT ( 'NONE', 'WORKASPACE' ) );
#323=SURFACE_STYLE_FILL_AREA ( #74247 ) ;
#327=CARTESIAN_POINT ( 'NONE',  ( 4.586789253316146286, -47.77528324151398209, 102.5764008378948091 ) ) ;
#336=ORIENTED_EDGE ( 'NONE', *, *, #86962, .T. ) ;
#340=CARTESIAN_POINT ( 'NONE',  ( -5.413519594459913264, -11.02779875410785237, -10.18303460993699971 ) ) ;
#362=SURFACE_STYLE_USAGE ( .BOTH. , #70999 ) ;
#365=FILL_AREA_STYLE ('',( #52142 ) ) ;
#376=CARTESIAN_POINT ( 'NONE',  ( 0.000000000000000000, 0.000000000000000000, 27.00000000000000000 ) ) ;
#377=CARTESIAN_POINT ( 'NONE',  ( 30.00000000000000000, 0.000000000000000000, 15.00000000000000000 ) ) ;
#395=AXIS2_PLACEMENT_3D ( 'NONE', #92986, #43904, #76792 ) ;
#408=DIRECTION ( 'NONE',  ( 0.000000000000000000, 0.000000000000000000, -1.000000000000000000 ) ) ;
#423=CARTESIAN_POINT ( 'NONE',  ( -6.081241251370744116, -12.38970427209902425, 12.35256966254870115 ) ) ;
#443=CARTESIAN_POINT ( 'NONE',  ( 12.37144696128341792, -4.000000000000002665, 20.44658103856077602 ) ) ;
#453=FACE_OUTER_BOUND ( 'NONE', #37066, .T. ) ;
#481=CARTESIAN_POINT ( 'NONE',  ( 9.113097280746998763, -53.73680858635314905, 31.11721482942555639 ) ) ;
#504=CARTESIAN_POINT ( 'NONE',  ( -12.40466434899015447, -3.812810247667897112, 20.50928832961362502 ) ) ;
#508=FACE_OUTER_BOUND ( 'NONE', #74890, .T. ) ;
#510=EDGE_CURVE ( 'NONE', #30914, #85394, #78873, .T. ) ;
#541=CARTESIAN_POINT ( 'NONE',  ( -5.385673916453011856, 3.157894736842104866, 14.66382285868950675 ) ) ;
#550=VERTEX_POINT ( 'NONE', #55500 ) ;
#589=FACE_OUTER_BOUND ( 'NONE', #76016, .T. ) ;
#612=AXIS2_PLACEMENT_3D ( 'NONE', #25378, #80380, #57689 ) ;
#628=SURFACE_STYLE_FILL_AREA ( #82659 ) ;
#679=( LENGTH_UNIT ( ) NAMED_UNIT ( * ) SI_UNIT ( .MILLI., .METRE. ) );
#683=CARTESIAN_POINT ( 'NONE',  ( -5.169066395376114897, -13.70246774098932541, -6.130298896215165882 ) ) ;
#687=CARTESIAN_POINT ( 'NONE',  ( 7.000000000000000000, -15.93202192939576634, -5.930487099830196840 ) ) ;
#697=CARTESIAN_POINT ( 'NONE',  ( 8.181629489174529368, -12.25161225291834377, 8.655449601632003720 ) ) ;
#714=( LENGTH_UNIT ( ) NAMED_UNIT ( * ) SI_UNIT ( .MILLI., .METRE. ) );
#719=PRESENTATION_STYLE_ASSIGNMENT (( #26673 ) ) ;
#757=COLOUR_RGB ( '', 0.09019608, 0.27058824, 0.51372549) ;
#764=COLOUR_RGB ( '', 0.31764706, 0.68627451, 0.89019608) ;
#797=EDGE_CURVE ( 'NONE', #94943, #52640, #39408, .T. ) ;
#804=AXIS2_PLACEMENT_3D ( 'NONE', #25250, #74290, #100690 ) ;
#809=CARTESIAN_POINT ( 'NONE',  ( 4.254610347505312973, -66.83165319588984232, 13.14363822686244099 ) ) ;
#833=PRODUCT_DEFINITION_FORMATION_WITH_SPECIFIED_SOURCE ( 'ANY', '', #3601, .NOT_KNOWN. ) ;
#835=CARTESIAN_POINT ( 'NONE',  ( 5.000000000000000888, -15.62228920881127081, 13.86359191440427807 ) ) ;
#847=CARTESIAN_POINT ( 'NONE',  ( 6.063014363552462704, -12.44085613821209080, 12.46297707981380753 ) ) ;
#852=( NAMED_UNIT ( * ) PLANE_ANGLE_UNIT ( ) SI_UNIT ( $, .RADIAN. ) );
#914=CARTESIAN_POINT ( 'NONE',  ( 4.284822031654949015, -48.90716638558772900, 104.4267991316944943 ) ) ;
#943=CARTESIAN_POINT ( 'NONE',  ( 0.9999999999999956701, -46.00000000000000000, 40.07669683062201926 ) ) ;
#974=CARTESIAN_POINT ( 'NONE',  ( 15.95167959069860508, -2.669324059294185147, 14.76264669450079126 ) ) ;
#980=CARTESIAN_POINT ( 'NONE',  ( -27.99999999999999645, 0.000000000000000000, -11.00000000000000000 ) ) ;
#990=ORIENTED_EDGE ( 'NONE', *, *, #58627, .T. ) ;
#1036=DIRECTION ( 'NONE',  ( 0.000000000000000000, 0.000000000000000000, -1.000000000000000000 ) ) ;
#1045=CARTESIAN_POINT ( 'NONE',  ( -11.16486260932954444, -1.276900883929068975, 20.44370595537206370 ) ) ;
#1056=CARTESIAN_POINT ( 'NONE',  ( 4.302752950498871520, -1.102340297636630106, 104.4121132197325181 ) ) ;
#1078=CARTESIAN_POINT ( 'NONE',  ( -4.551587301587291634, -48.79941684889506348, 104.4018401814738013 ) ) ;
#1083=MECHANICAL_DESIGN_GEOMETRIC_PRESENTATION_REPRESENTATION('',(#80331),#71707);
#1120=CARTESIAN_POINT ( 'NONE',  ( 9.378402013738298848, -55.78449074848818157, 23.52762072402763849 ) ) ;
#1125=CARTESIAN_POINT ( 'NONE',  ( 1.000000000000000000, -10.14931581696268026, -12.32157755740822402 ) ) ;
#1157=SURFACE_SIDE_STYLE ('',( #35186 ) ) ;
#1181=( BOUNDED_SURFACE ( )  B_SPLINE_SURFACE ( 3, 2, ( 
 ( #5338, #103493, #29642 ),
 ( #47890, #55972, #96475 ),
 ( #105606, #38772, #47369 ),
 ( #46324, #80259, #87850 ) ),
 .UNSPECIFIED., .F., .F., .F. ) 
 B_SPLINE_SURFACE_WITH_KNOTS ( ( 4, 4 ),
 ( 3, 3 ),
 ( 1.626303258728256651E-18, 0.0009823161607561291166 ),
 ( 0.000000000000000000, 1.000000000000000000 ),
 .UNSPECIFIED. ) 
 GEOMETRIC_REPRESENTATION_ITEM ( )  RATIONAL_B_SPLINE_SURFACE ( (
 ( 1.000000000000000000, 0.9359444767143315635, 1.000000000000000000),
 ( 1.000000000000000000, 0.9457608441872460414, 1.000000000000000000),
 ( 1.000000000000000000, 0.9551386542018357462, 1.000000000000000000),
 ( 1.000000000000000000, 0.9603284238771496728, 1.000000000000000000) ) ) 
 REPRESENTATION_ITEM ( '' )  SURFACE ( )  );
#1182=CARTESIAN_POINT ( 'NONE',  ( -5.000000000000000000, -61.57181732616183467, 13.02933472593649533 ) ) ;
#1204=EDGE_CURVE ( 'NONE', #27751, #76782, #1387, .T. ) ;
#1224=CARTESIAN_POINT ( 'NONE',  ( -6.934100574218754254, -13.60622170956001398, -6.341742298311178416 ) ) ;
#1230=STYLED_ITEM ( 'NONE', ( #95479 ), #1826 ) ;
#1258=CARTESIAN_POINT ( 'NONE',  ( -3.769311339735803124, -48.92514534113568203, 104.1674216685380969 ) ) ;
#1277=ORIENTED_EDGE ( 'NONE', *, *, #16474, .F. ) ;
#1284=EDGE_CURVE ( 'NONE', #77091, #40703, #51379, .T. ) ;
#1300=FACE_OUTER_BOUND ( 'NONE', #36868, .T. ) ;
#1335=CARTESIAN_POINT ( 'NONE',  ( 3.039836064073310862, -49.44988477872288968, 44.27385412736651205 ) ) ;
#1359=CARTESIAN_POINT ( 'NONE',  ( 4.457938013472972472, -66.14659025852527918, 13.13206513276273313 ) ) ;
#1373=FILL_AREA_STYLE_COLOUR ( '', #73048 ) ;
#1385=CARTESIAN_POINT ( 'NONE',  ( 5.000000000000000000, -14.24437098773438315, 11.98245615812517784 ) ) ;
#1387=LINE ( 'NONE', #83925, #53182 ) ;
#1407=CARTESIAN_POINT ( 'NONE',  ( 6.898673495379865628, -0.02001816142087574704, 19.00543362303419670 ) ) ;
#1410=COLOUR_RGB ( '', 0.08235294, 0.09019608, 0.10196078) ;
#1421=ORIENTED_EDGE ( 'NONE', *, *, #89266, .F. ) ;
#1447=STYLED_ITEM ( 'NONE', ( #79901 ), #44605 ) ;
#1469=MECHANICAL_DESIGN_GEOMETRIC_PRESENTATION_REPRESENTATION('',(#84110),#61812);
#1470=CARTESIAN_POINT ( 'NONE',  ( 0.000000000000000000, -5.000000000000000000, -14.14213562373095101 ) ) ;
#1505=CARTESIAN_POINT ( 'NONE',  ( -3.668277386370349280, -1.103629945923298106, 104.6014336420241051 ) ) ;
#1515=COLOUR_RGB ( '', 0.08235294, 0.09019608, 0.10196078) ;
#1531=CARTESIAN_POINT ( 'NONE',  ( 9.886129545901154003, -3.298559501015256856, 15.11875162840864739 ) ) ;
#1533=( LENGTH_UNIT ( ) NAMED_UNIT ( * ) SI_UNIT ( .MILLI., .METRE. ) );
#1561=CARTESIAN_POINT ( 'NONE',  ( 3.208180356140310163, -10.20788741807700717, -11.61546768905490445 ) ) ;
#1568=ADVANCED_FACE ( 'NONE', ( #9765 ), #3048, .T. ) ;
#1574=FACE_BOUND ( 'NONE', #45713, .T. ) ;
#1589=FILL_AREA_STYLE_COLOUR ( '', #61034 ) ;
#1617=( NAMED_UNIT ( * ) SI_UNIT ( $, .STERADIAN. ) SOLID_ANGLE_UNIT ( ) );
#1634=ORIENTED_EDGE ( 'NONE', *, *, #54089, .T. ) ;
#1637=( BOUNDED_SURFACE ( )  B_SPLINE_SURFACE ( 3, 2, ( 
 ( #12824, #20989, #61951 ),
 ( #94844, #37694, #53822 ),
 ( #11763, #68435, #45744 ),
 ( #43611, #18850, #51695 ),
 ( #26940, #93232, #86754 ),
 ( #93768, #61413, #86229 ),
 ( #94305, #60878, #84612 ),
 ( #78621, #4755, #3703 ),
 ( #69495, #20468, #10697 ),
 ( #2612, #19394, #52226 ),
 ( #85137, #11229, #44154 ),
 ( #77043, #3159, #45228 ) ),
 .UNSPECIFIED., .F., .F., .T. ) 
 B_SPLINE_SURFACE_WITH_KNOTS ( ( 4, 2, 2, 2, 2, 4 ),
 ( 3, 3 ),
 ( 0.000000000000000000, 0.0007735885786023083931, 0.001547177157204616786, 0.001933971446505770983, 0.002320765735806925179, 0.003094354314409233572 ),
 ( 0.000000000000000000, 1.000000000000000000 ),
 .UNSPECIFIED. ) 
 GEOMETRIC_REPRESENTATION_ITEM ( )  RATIONAL_B_SPLINE_SURFACE ( (
 ( 1.000000000000000000, 0.9603284238771501169, 1.000000000000000000),
 ( 1.000000000000000000, 0.9628724889917420482, 1.000000000000000000),
 ( 1.000000000000000000, 0.9663306537743326929, 1.000000000000000000),
 ( 1.000000000000000000, 0.9744563874115806934, 1.000000000000000000),
 ( 1.000000000000000000, 0.9789903143386278206, 1.000000000000000000),
 ( 1.000000000000000000, 0.9855527733005997604, 1.000000000000000000),
 ( 1.000000000000000000, 0.9877025284828834240, 1.000000000000000000),
 ( 1.000000000000000000, 0.9916277982505393718, 1.000000000000000000),
 ( 1.000000000000000000, 0.9934221110297505319, 1.000000000000000000),
 ( 1.000000000000000000, 0.9980179737617284053, 1.000000000000000000),
 ( 1.000000000000000000, 1.000016370385679254, 1.000000000000000000),
 ( 1.000000000000000000, 1.000000000000000000, 1.000000000000000000) ) ) 
 REPRESENTATION_ITEM ( '' )  SURFACE ( )  );
#1640=EDGE_CURVE ( 'NONE', #57615, #33722, #26541, .T. ) ;
#1729=( LENGTH_UNIT ( ) NAMED_UNIT ( * ) SI_UNIT ( .MILLI., .METRE. ) );
#1735=CARTESIAN_POINT ( 'NONE',  ( -1.000000000000000000, -70.02685735654881682, 13.01550610203317682 ) ) ;
#1749=CARTESIAN_POINT ( 'NONE',  ( 1.224646799147353256E-15, -80.00000000000000000, 17.00000000000000000 ) ) ;
#1773=CARTESIAN_POINT ( 'NONE',  ( -15.90614609307868399, -3.157894736842107530, 14.66382285868950675 ) ) ;
#1792=FILL_AREA_STYLE ('',( #77832 ) ) ;
#1826=ADVANCED_FACE ( 'NONE', ( #21110 ), #60489, .F. ) ;
#1848=ORIENTED_EDGE ( 'NONE', *, *, #36708, .T. ) ;
#1850=CARTESIAN_POINT ( 'NONE',  ( 3.473244378093581108, -49.24695708051920207, 40.73076878102696696 ) ) ;
#1898=CARTESIAN_POINT ( 'NONE',  ( 3.387540951686171198, -69.89757699288746551, 13.41458569023665959 ) ) ;
#1901=VECTOR ( 'NONE', #97341, 1000.000000000000000 ) ;
#1915=( NAMED_UNIT ( * ) SI_UNIT ( $, .STERADIAN. ) SOLID_ANGLE_UNIT ( ) );
#1929=CARTESIAN_POINT ( 'NONE',  ( 5.990115786909115947, -12.91256367767907420, 13.08452859117424616 ) ) ;
#1945=CARTESIAN_POINT ( 'NONE',  ( -7.000000000000000000, -46.00000000000000000, 39.12435565298213902 ) ) ;
#1946=CARTESIAN_POINT ( 'NONE',  ( 5.958501008717178138, -13.50719282745116701, 13.62690037880517302 ) ) ;
#1947=DIRECTION ( 'NONE',  ( 0.000000000000000000, 0.000000000000000000, -1.000000000000000000 ) ) ;
#1950=SURFACE_SIDE_STYLE ('',( #92568 ) ) ;
#1969=EDGE_CURVE ( 'NONE', #85296, #41445, #16906, .T. ) ;
#2009=DIRECTION ( 'NONE',  ( 1.000000000000000000, 0.000000000000000000, 0.000000000000000000 ) ) ;
#2017=CARTESIAN_POINT ( 'NONE',  ( 6.737208386734103271, -48.35039989235347946, 39.27323200384739010 ) ) ;
#2068=CARTESIAN_POINT ( 'NONE',  ( 9.336331243639834909, -2.525205179013640056, 14.78776590177819372 ) ) ;
#2104=STYLED_ITEM ( 'NONE', ( #41395 ), #14634 ) ;
#2111=STYLED_ITEM ( 'NONE', ( #20193 ), #93726 ) ;
#2114=MECHANICAL_DESIGN_GEOMETRIC_PRESENTATION_REPRESENTATION('',(#64141),#72723);
#2141=( NAMED_UNIT ( * ) SI_UNIT ( $, .STERADIAN. ) SOLID_ANGLE_UNIT ( ) );
#2143=FILL_AREA_STYLE_COLOUR ( '', #97854 ) ;
#2153=VERTEX_POINT ( 'NONE', #37695 ) ;
#2158=FILL_AREA_STYLE ('',( #59910 ) ) ;
#2172=EDGE_CURVE ( 'NONE', #12254, #89611, #106433, .T. ) ;
#2198=CARTESIAN_POINT ( 'NONE',  ( -3.350247031700762879, -1.071204144247461576, 104.4269854689273558 ) ) ;
#2201=SURFACE_STYLE_USAGE ( .BOTH. , #41619 ) ;
#2205=CARTESIAN_POINT ( 'NONE',  ( 9.051760805868392268, -13.60634430745754386, 16.31685301915852548 ) ) ;
#2244=EDGE_LOOP ( 'NONE', ( #77086, #3933, #61631, #24307 ) ) ;
#2261=CARTESIAN_POINT ( 'NONE',  ( -5.000000000000000000, -62.87784732671490673, 13.68732737529383670 ) ) ;
#2273=CARTESIAN_POINT ( 'NONE',  ( -1.000000000000000888, -50.00000000000000000, 40.07669683062201926 ) ) ;
#2298=CARTESIAN_POINT ( 'NONE',  ( 3.365451957726484977, -0.9314134953375798887, 104.1992105446103096 ) ) ;
#2300=CARTESIAN_POINT ( 'NONE',  ( -7.000000000000000000, -14.05766640829038749, -5.232782735144286157 ) ) ;
#2304=CARTESIAN_POINT ( 'NONE',  ( -14.73107898043755881, -7.226827713034739809, 13.14759240030440424 ) ) ;
#2305=CARTESIAN_POINT ( 'NONE',  ( -6.920567593065749534, -12.35473601147217870, 8.513547508574108136 ) ) ;
#2312=EDGE_CURVE ( 'NONE', #5281, #3985, #17106, .T. ) ;
#2340=UNCERTAINTY_MEASURE_WITH_UNIT (LENGTH_MEASURE( 1.000000000000000082E-05 ), #36595, 'distance_accuracy_value', 'NONE');
#2344=CARTESIAN_POINT ( 'NONE',  ( 5.374793246923871948, -2.224716758540632888, 104.0614974883207537 ) ) ;
#2346=FILL_AREA_STYLE ('',( #16958 ) ) ;
#2356=DIRECTION ( 'NONE',  ( 0.000000000000000000, 1.000000000000000000, 0.000000000000000000 ) ) ;
#2357=DIRECTION ( 'NONE',  ( -0.000000000000000000, -1.000000000000000000, -0.000000000000000000 ) ) ;
#2390=CARTESIAN_POINT ( 'NONE',  ( 4.136210027783189247, -48.58433892124558184, 40.56527332860810020 ) ) ;
#2416=COLOUR_RGB ( '', 0.09019608, 0.27058824, 0.51372549) ;
#2420=ORIENTED_EDGE ( 'NONE', *, *, #5467, .F. ) ;
#2421=CARTESIAN_POINT ( 'NONE',  ( 4.457519228156027857, -48.07754600148881252, 43.17321295657507818 ) ) ;
#2427=CARTESIAN_POINT ( 'NONE',  ( -5.385673916453011856, 4.000000000000000000, 18.57417562100670949 ) ) ;
#2435=CARTESIAN_POINT ( 'NONE',  ( -3.279721309033237109, -49.29419538185737792, 103.5044183211188198 ) ) ;
#2454=CARTESIAN_POINT ( 'NONE',  ( 7.000000000000000000, -15.62228920881129390, 12.61250543006183378 ) ) ;
#2466=CARTESIAN_POINT ( 'NONE',  ( 5.963307081834043899, -13.30359940716316558, 13.46515011340868639 ) ) ;
#2481=CARTESIAN_POINT ( 'NONE',  ( 6.999999999999998224, -12.54465221550629472, 8.223849511755000563 ) ) ;
#2485=FILL_AREA_STYLE_COLOUR ( '', #14951 ) ;
#2498=EDGE_LOOP ( 'NONE', ( #37662, #11773, #16239, #82159 ) ) ;
#2512=DIRECTION ( 'NONE',  ( -0.7142857142857147457, -0.6998542122237648710, 0.000000000000000000 ) ) ;
#2525=CARTESIAN_POINT ( 'NONE',  ( -4.448407490268954767, -1.969035902430321006, 102.6871849564181076 ) ) ;
#2567=B_SPLINE_CURVE_WITH_KNOTS ( 'NONE', 3,
 ( #39205, #46226, #104989, #12775, #64534, #37642, #54824, #79114, #30061, #62943, #46747, #49921 ),
 .UNSPECIFIED., .F., .F.,
 ( 4, 2, 2, 2, 2, 4 ),
 ( 8.673617379884035472E-19, 0.001111604437821193773, 0.002223208875642386680, 0.003334813313463579586, 0.003890615532374176039, 0.004446417751284772492 ),
 .UNSPECIFIED. ) ;
#2569=ORIENTED_EDGE ( 'NONE', *, *, #48926, .T. ) ;
#2570=DIRECTION ( 'NONE',  ( 0.000000000000000000, 0.000000000000000000, -1.000000000000000000 ) ) ;
#2581=EDGE_LOOP ( 'NONE', ( #64797, #86771, #46556, #67787 ) ) ;
#2604=( GEOMETRIC_REPRESENTATION_CONTEXT ( 3 ) GLOBAL_UNCERTAINTY_ASSIGNED_CONTEXT ( ( #62341 ) ) GLOBAL_UNIT_ASSIGNED_CONTEXT ( ( #97403, #106027, #23565 ) ) REPRESENTATION_CONTEXT ( 'NONE', 'WORKASPACE' ) );
#2606=CARTESIAN_POINT ( 'NONE',  ( 0.000000000000000000, -46.00000000000000000, 118.0000000000000000 ) ) ;
#2612=CARTESIAN_POINT ( 'NONE',  ( 3.350247031700846367, -48.92879585575218471, 104.4269854689279242 ) ) ;
#2661=CYLINDRICAL_SURFACE ( 'NONE', #12880, 4.000000000000000000 ) ;
#2680=COLOUR_RGB ( '', 0.40784314, 0.44705882, 0.49803922) ;
#2684=PRESENTATION_STYLE_ASSIGNMENT (( #76042 ) ) ;
#2701=( NAMED_UNIT ( * ) PLANE_ANGLE_UNIT ( ) SI_UNIT ( $, .RADIAN. ) );
#2730=EDGE_LOOP ( 'NONE', ( #37276, #78580, #11053 ) ) ;
#2737=CARTESIAN_POINT ( 'NONE',  ( -3.349796915303539624, -1.132149698118623871, 104.5044954676219930 ) ) ;
#2744=CARTESIAN_POINT ( 'NONE',  ( 11.63797817910942278, -10.74185076926238835, 10.47199366613784299 ) ) ;
#2748=UNCERTAINTY_MEASURE_WITH_UNIT (LENGTH_MEASURE( 1.000000000000000082E-05 ), #97020, 'distance_accuracy_value', 'NONE');
#2754=EDGE_CURVE ( 'NONE', #17070, #82494, #76840, .T. ) ;
#2756=MECHANICAL_DESIGN_GEOMETRIC_PRESENTATION_REPRESENTATION('',(#81967),#99133);
#2764=MECHANICAL_DESIGN_GEOMETRIC_PRESENTATION_REPRESENTATION('',(#69981),#28682);
#2773=FILL_AREA_STYLE ('',( #28163 ) ) ;
#2790=ADVANCED_FACE ( 'NONE', ( #40699 ), #35967, .T. ) ;
#2795=CARTESIAN_POINT ( 'NONE',  ( -6.125000000000002665, -15.62228920881133654, 14.41094225130411211 ) ) ;
#2802=CARTESIAN_POINT ( 'NONE',  ( 7.878970821878172437, 3.088077109979846302, 14.68021914166114783 ) ) ;
#2819=AXIS2_PLACEMENT_3D ( 'NONE', #103380, #93700, #52687 ) ;
#2840=CARTESIAN_POINT ( 'NONE',  ( 3.459690225508319283, -1.108983740916838379, 104.5059395991341660 ) ) ;
#2842=CARTESIAN_POINT ( 'NONE',  ( -6.163128221576519294, -12.12876728480168254, -8.844179776184848407 ) ) ;
#2845=CARTESIAN_POINT ( 'NONE',  ( -6.163737169368993740, -12.13805321688065320, 11.84025182891627992 ) ) ;
#2868=( GEOMETRIC_REPRESENTATION_CONTEXT ( 3 ) GLOBAL_UNCERTAINTY_ASSIGNED_CONTEXT ( ( #35159 ) ) GLOBAL_UNIT_ASSIGNED_CONTEXT ( ( #1533, #18847, #75975 ) ) REPRESENTATION_CONTEXT ( 'NONE', 'WORKASPACE' ) );
#2899=CARTESIAN_POINT ( 'NONE',  ( 4.999999999999993783, -46.00000000000000000, 102.2532056551910387 ) ) ;
#2904=LINE ( 'NONE', #100543, #59383 ) ;
#2922=CARTESIAN_POINT ( 'NONE',  ( 1.078711167028171491, -50.02722306961814525, 40.96723994058017126 ) ) ;
#2938=AXIS2_PLACEMENT_3D ( 'NONE', #34087, #17353, #89632 ) ;
#2945=CARTESIAN_POINT ( 'NONE',  ( -2.634824035318301672, -49.75410657075519083, 40.87749690338997510 ) ) ;
#2949=EDGE_LOOP ( 'NONE', ( #54230, #90431, #43201, #105627 ) ) ;
#3004=AXIS2_PLACEMENT_3D ( 'NONE', #74335, #98083, #408 ) ;
#3019=ORIENTED_EDGE ( 'NONE', *, *, #75288, .F. ) ;
#3022=CARTESIAN_POINT ( 'NONE',  ( -13.45844672282477816, -54.52686498230426793, 23.14344092887451154 ) ) ;
#3048=TOROIDAL_SURFACE ( 'NONE', #58084, 12.00000000000000000, 2.000000000000000000 ) ;
#3074=CARTESIAN_POINT ( 'NONE',  ( 1.224646799147353454E-15, -78.00000000000000000, 17.00000000000000000 ) ) ;
#3085=CARTESIAN_POINT ( 'NONE',  ( 5.000000000000000888, -14.03284112334355704, 9.638321537241061776 ) ) ;
#3093=B_SPLINE_CURVE_WITH_KNOTS ( 'NONE', 3,
 ( #66354, #9700, #41552, #50678 ),
 .UNSPECIFIED., .F., .F.,
 ( 4, 4 ),
 ( 2.168404344971008868E-19, 0.002009015923125643047 ),
 .UNSPECIFIED. ) ;
#3095=CARTESIAN_POINT ( 'NONE',  ( 4.371444047847319325, -52.53631654761795033, 40.30117609609928309 ) ) ;
#3119=VERTEX_POINT ( 'NONE', #49729 ) ;
#3126=MECHANICAL_DESIGN_GEOMETRIC_PRESENTATION_REPRESENTATION('',(#99502),#8270);
#3133=EDGE_LOOP ( 'NONE', ( #99013, #9219, #4853, #12269 ) ) ;
#3156=FILL_AREA_STYLE ('',( #42538 ) ) ;
#3159=CARTESIAN_POINT ( 'NONE',  ( 3.352941176470587870, -48.79941684889504927, 104.5794940929807524 ) ) ;
#3160=CARTESIAN_POINT ( 'NONE',  ( -5.000000000000000000, -15.93202192939577344, -5.930487099830192399 ) ) ;
#3166=ORIENTED_EDGE ( 'NONE', *, *, #43628, .F. ) ;
#3193=EDGE_CURVE ( 'NONE', #22140, #5765, #43423, .T. ) ;
#3204=AXIS2_PLACEMENT_3D ( 'NONE', #26924, #3679, #77022 ) ;
#3205=ORIENTED_EDGE ( 'NONE', *, *, #2312, .T. ) ;
#3213=DIRECTION ( 'NONE',  ( -0.000000000000000000, -1.000000000000000000, -0.000000000000000000 ) ) ;
#3214=DIRECTION ( 'NONE',  ( 0.000000000000000000, 0.000000000000000000, 1.000000000000000000 ) ) ;
#3220=CARTESIAN_POINT ( 'NONE',  ( 1.276500347575403982, -1.740950606958863416E-15, 101.3106844269255760 ) ) ;
#3238=AXIS2_PLACEMENT_3D ( 'NONE', #63747, #45439, #88543 ) ;
#3241=AXIS2_PLACEMENT_3D ( 'NONE', #100713, #26877, #100187 ) ;
#3261=CARTESIAN_POINT ( 'NONE',  ( -4.324717655747483569, -1.111686313677800131, 104.4045892612656417 ) ) ;
#3270=DIRECTION ( 'NONE',  ( 0.000000000000000000, 0.000000000000000000, 1.000000000000000000 ) ) ;
#3286=CARTESIAN_POINT ( 'NONE',  ( -1.226488475359366337, -0.004841394705047758623, 101.2642676850169892 ) ) ;
#3291=SURFACE_STYLE_USAGE ( .BOTH. , #28664 ) ;
#3310=CARTESIAN_POINT ( 'NONE',  ( 5.000000000000000888, -57.08339339093014786, 10.85455184355725144 ) ) ;
#3328=AXIS2_PLACEMENT_3D ( 'NONE', #35715, #50768, #83679 ) ;
#3333=VERTEX_POINT ( 'NONE', #103987 ) ;
#3344=DIRECTION ( 'NONE',  ( 1.000000000000000000, 0.000000000000000000, 0.000000000000000000 ) ) ;
#3348=CARTESIAN_POINT ( 'NONE',  ( 6.638999116915723420, 3.157894740940597522, 14.66382285780688655 ) ) ;
#3357=VECTOR ( 'NONE', #38581, 1000.000000000000000 ) ;
#3361=AXIS2_PLACEMENT_3D ( 'NONE', #80700, #102877, #4713 ) ;
#3389=CARTESIAN_POINT ( 'NONE',  ( -1.000000000000000000, -5.000000000000018652, -14.14213562373094568 ) ) ;
#3406=CARTESIAN_POINT ( 'NONE',  ( 13.97222917066916992, -57.87254792530227121, 26.08167946173673002 ) ) ;
#3440=DIRECTION ( 'NONE',  ( 0.000000000000000000, 1.000000000000000000, 0.000000000000000000 ) ) ;
#3452=CARTESIAN_POINT ( 'NONE',  ( -9.301012663197237629, -55.30021075719776036, 23.32537848786287782 ) ) ;
#3466=SURFACE_SIDE_STYLE ('',( #4518 ) ) ;
#3470=CARTESIAN_POINT ( 'NONE',  ( 1.431705818242835271, -50.02825494199252887, 40.96159436747194604 ) ) ;
#3471=EDGE_CURVE ( 'NONE', #96331, #81100, #62643, .T. ) ;
#3565=FACE_OUTER_BOUND ( 'NONE', #41606, .T. ) ;
#3566=CARTESIAN_POINT ( 'NONE',  ( -13.50905259634051170, -55.29488368535347576, 23.32354201833150853 ) ) ;
#3601=PRODUCT ( '3. Bracket', '3. Bracket', '', ( #6660 ) ) ;
#3639=( LENGTH_UNIT ( ) NAMED_UNIT ( * ) SI_UNIT ( .MILLI., .METRE. ) );
#3674=ORIENTED_EDGE ( 'NONE', *, *, #75635, .F. ) ;
#3679=DIRECTION ( 'NONE',  ( -1.000000000000000000, 0.000000000000000000, 0.000000000000000000 ) ) ;
#3698=ORIENTED_EDGE ( 'NONE', *, *, #4582, .F. ) ;
#3703=CARTESIAN_POINT ( 'NONE',  ( 3.753470829068648484, -48.91069040221620412, 104.5911851069064085 ) ) ;
#3705=CARTESIAN_POINT ( 'NONE',  ( -4.948897516043240685, -15.25620596204638701, -6.941429743102868422 ) ) ;
#3709=EDGE_LOOP ( 'NONE', ( #17749, #71832, #29570, #5003 ) ) ;
#3724=CARTESIAN_POINT ( 'NONE',  ( 4.956067050182457301, -15.30475822382861928, -6.874165724332473637 ) ) ;
#3726=VECTOR ( 'NONE', #13923, 1000.000000000000000 ) ;
#3727=DIRECTION ( 'NONE',  ( -0.5166563581655519988, 0.4014477553984793223, 0.7562446080816918048 ) ) ;
#3738=DIRECTION ( 'NONE',  ( 0.000000000000000000, 0.000000000000000000, 1.000000000000000000 ) ) ;
#3743=AXIS2_PLACEMENT_3D ( 'NONE', #61742, #78419, #44479 ) ;
#3772=CARTESIAN_POINT ( 'NONE',  ( -14.25073637597874665, 0.6890215015240969132, 14.98521214194409445 ) ) ;
#3787=CARTESIAN_POINT ( 'NONE',  ( -3.433097520132042835, -0.8249796456130259470, 103.8029795887030815 ) ) ;
#3798=( NAMED_UNIT ( * ) PLANE_ANGLE_UNIT ( ) SI_UNIT ( $, .RADIAN. ) );
#3806=CIRCLE ( 'NONE', #51990, 4.000000000000003553 ) ;
#3823=CARTESIAN_POINT ( 'NONE',  ( -4.359081798055807866, -66.52598855954795454, 13.14323235564549819 ) ) ;
#3833=COLOUR_RGB ( '', 0.40784314, 0.44705882, 0.49803922) ;
#3849=CARTESIAN_POINT ( 'NONE',  ( 5.000000000000000000, -51.57174003072816504, 8.340209667212416633 ) ) ;
#3871=DIRECTION ( 'NONE',  ( 0.000000000000000000, 0.000000000000000000, 1.000000000000000000 ) ) ;
#3883=CARTESIAN_POINT ( 'NONE',  ( -4.284822031654912600, -48.90716638558775031, 104.4267991316945228 ) ) ;
#3905=VERTEX_POINT ( 'NONE', #69064 ) ;
#3921=CARTESIAN_POINT ( 'NONE',  ( 1.000000000000000222, -10.50453238069598960, -12.19598953690542231 ) ) ;
#3923=CARTESIAN_POINT ( 'NONE',  ( -3.684569285721631005, -8.676863831078836853, -12.27927943165845193 ) ) ;
#3933=ORIENTED_EDGE ( 'NONE', *, *, #43928, .F. ) ;
#3937=CARTESIAN_POINT ( 'NONE',  ( 13.42014116845449934, -55.04332197544540151, 30.98782490008220236 ) ) ;
#3957=CARTESIAN_POINT ( 'NONE',  ( 4.188755055078403622, -1.571875576994826718, 102.8981131900555113 ) ) ;
#3959=CARTESIAN_POINT ( 'NONE',  ( -3.352941176470584761, -48.79941684889506348, 104.5794940929807524 ) ) ;
#3964=DIRECTION ( 'NONE',  ( 0.000000000000000000, 0.000000000000000000, 1.000000000000000000 ) ) ;
#3972=( LENGTH_UNIT ( ) NAMED_UNIT ( * ) SI_UNIT ( .MILLI., .METRE. ) );
#3982=EDGE_CURVE ( 'NONE', #34973, #25211, #39351, .T. ) ;
#3985=VERTEX_POINT ( 'NONE', #88423 ) ;
#4003=CARTESIAN_POINT ( 'NONE',  ( 6.162708901257258454, -50.04180103047903572, 39.57312441009716508 ) ) ;
#4023=CARTESIAN_POINT ( 'NONE',  ( -1.081074338060140638, -50.02734650443385789, 40.96720160546766465 ) ) ;
#4031=COLOUR_RGB ( '', 0.66274510, 0.83137255, 0.94901961) ;
#4081=CARTESIAN_POINT ( 'NONE',  ( 1.000000000000000222, -5.000000000000000000, -14.14213562373095101 ) ) ;
#4094=ORIENTED_EDGE ( 'NONE', *, *, #7312, .F. ) ;
#4115=CARTESIAN_POINT ( 'NONE',  ( 1.347111479062088996E-15, -4.000000000000003553, 100.9999999999999858 ) ) ;
#4143=DIRECTION ( 'NONE',  ( 0.000000000000000000, 0.000000000000000000, 1.000000000000000000 ) ) ;
#4144=( NAMED_UNIT ( * ) SI_UNIT ( $, .STERADIAN. ) SOLID_ANGLE_UNIT ( ) );
#4169=FACE_OUTER_BOUND ( 'NONE', #104137, .T. ) ;
#4171=VERTEX_POINT ( 'NONE', #98091 ) ;
#4202=CIRCLE ( 'NONE', #66244, 9.999999999999998224 ) ;
#4219=CARTESIAN_POINT ( 'NONE',  ( -6.835098440474090431, -6.776903958348333035, 13.91313563306597700 ) ) ;
#4250=COLOUR_RGB ( '', 0.31764706, 0.68627451, 0.89019608) ;
#4293=CARTESIAN_POINT ( 'NONE',  ( -9.517455598866080280, -3.342537638539781586, 14.84703453944758955 ) ) ;
#4305=EDGE_LOOP ( 'NONE', ( #60907, #86496 ) ) ;
#4321=CARTESIAN_POINT ( 'NONE',  ( -2.900817060773052347, -70.21372430060392844, 13.30197803733283379 ) ) ;
#4346=CARTESIAN_POINT ( 'NONE',  ( -3.954440898799530313, -67.58589629217112815, 13.13255854702942926 ) ) ;
#4347=DIRECTION ( 'NONE',  ( 0.000000000000000000, 1.000000000000000000, 0.000000000000000000 ) ) ;
#4373=EDGE_CURVE ( 'NONE', #87124, #26304, #48275, .T. ) ;
#4389=AXIS2_PLACEMENT_3D ( 'NONE', #82025, #33513, #41055 ) ;
#4395=DIRECTION ( 'NONE',  ( 0.000000000000000000, 0.000000000000000000, -1.000000000000000000 ) ) ;
#4407=CARTESIAN_POINT ( 'NONE',  ( -5.000000000000000000, -46.95680582063142339, 6.322184883410053580 ) ) ;
#4413=DIRECTION ( 'NONE',  ( 0.000000000000000000, 0.000000000000000000, 1.000000000000000000 ) ) ;
#4431=SURFACE_STYLE_USAGE ( .BOTH. , #30321 ) ;
#4478=CARTESIAN_POINT ( 'NONE',  ( 1.000000000000000000, -67.35888985745027924, 11.51944599225194210 ) ) ;
#4486=CARTESIAN_POINT ( 'NONE',  ( 4.980618096941269002, -3.539029780453324392, 103.2912570477108716 ) ) ;
#4488=CARTESIAN_POINT ( 'NONE',  ( -3.358578016107393260, -49.02765317499757458, 104.2746939430699342 ) ) ;
#4518=SURFACE_STYLE_FILL_AREA ( #86535 ) ;
#4544=CARTESIAN_POINT ( 'NONE',  ( -1.000000000000000000, -67.04094093996420156, 11.34959271884451937 ) ) ;
#4550=CARTESIAN_POINT ( 'NONE',  ( -2.301926985296694372, -49.78450636680690877, 44.63741750628801697 ) ) ;
#4551=AXIS2_PLACEMENT_3D ( 'NONE', #34691, #59477, #27133 ) ;
#4578=COLOUR_RGB ( '', 0.66274510, 0.83137255, 0.94901961) ;
#4582=EDGE_CURVE ( 'NONE', #3985, #63587, #68939, .T. ) ;
#4618=ORIENTED_EDGE ( 'NONE', *, *, #27844, .T. ) ;
#4621=VECTOR ( 'NONE', #12129, 1000.000000000000000 ) ;
#4625=EDGE_LOOP ( 'NONE', ( #54639, #29857, #44064 ) ) ;
#4630=( GEOMETRIC_REPRESENTATION_CONTEXT ( 3 ) GLOBAL_UNCERTAINTY_ASSIGNED_CONTEXT ( ( #7071 ) ) GLOBAL_UNIT_ASSIGNED_CONTEXT ( ( #3639, #94789, #8394 ) ) REPRESENTATION_CONTEXT ( 'NONE', 'WORKASPACE' ) );
#4635=CARTESIAN_POINT ( 'NONE',  ( 12.13435171257998846, 2.003356828137956569, 14.86647337586970785 ) ) ;
#4652=( LENGTH_UNIT ( ) NAMED_UNIT ( * ) SI_UNIT ( .MILLI., .METRE. ) );
#4687=CARTESIAN_POINT ( 'NONE',  ( 13.87389654945780215, -50.52883469042527764, 25.11216171227248850 ) ) ;
#4713=DIRECTION ( 'NONE',  ( -8.881784197001251337E-16, 0.000000000000000000, 1.000000000000000000 ) ) ;
#4720=FILL_AREA_STYLE ('',( #21455 ) ) ;
#4723=MECHANICAL_DESIGN_GEOMETRIC_PRESENTATION_REPRESENTATION('',(#87431),#68482);
#4729=EDGE_CURVE ( 'NONE', #40108, #71499, #92461, .T. ) ;
#4751=CARTESIAN_POINT ( 'NONE',  ( -12.22235868236113809, -5.447693567057124042, 20.16913045786658998 ) ) ;
#4755=CARTESIAN_POINT ( 'NONE',  ( 3.558939058152283064, -48.93902971889313847, 104.4181685828942250 ) ) ;
#4756=CARTESIAN_POINT ( 'NONE',  ( -5.000000000000002665, -15.60834397543590590, -6.449723013184157416 ) ) ;
#4784=( NAMED_UNIT ( * ) SI_UNIT ( $, .STERADIAN. ) SOLID_ANGLE_UNIT ( ) );
#4801=TOROIDAL_SURFACE ( 'NONE', #70240, 5.999999999999996447, 4.000000000000000000 ) ;
#4825=CARTESIAN_POINT ( 'NONE',  ( -9.755579246370350788, -2.371311999149684269, 15.43086382375051357 ) ) ;
#4852=ORIENTED_EDGE ( 'NONE', *, *, #41546, .F. ) ;
#4853=ORIENTED_EDGE ( 'NONE', *, *, #70200, .F. ) ;
#4856=CARTESIAN_POINT ( 'NONE',  ( -5.000000000000000000, -14.03284112244674553, 9.638321536846772730 ) ) ;
#4857=FILL_AREA_STYLE ('',( #86850 ) ) ;
#4860=STYLED_ITEM ( 'NONE', ( #97011 ), #44238 ) ;
#4901=ORIENTED_EDGE ( 'NONE', *, *, #69802, .F. ) ;
#4910=AXIS2_PLACEMENT_3D ( 'NONE', #20854, #94706, #69360 ) ;
#4917=FILL_AREA_STYLE_COLOUR ( '', #24632 ) ;
#4942=ORIENTED_EDGE ( 'NONE', *, *, #1969, .F. ) ;
#4947=CARTESIAN_POINT ( 'NONE',  ( -1.000000000000000000, -32.16754151679361939, -4.059900122495614383 ) ) ;
#4948=CARTESIAN_POINT ( 'NONE',  ( -4.999999999999999112, -4.000000000000000000, 35.66025403784438197 ) ) ;
#4955=( GEOMETRIC_REPRESENTATION_CONTEXT ( 3 ) GLOBAL_UNCERTAINTY_ASSIGNED_CONTEXT ( ( #104360 ) ) GLOBAL_UNIT_ASSIGNED_CONTEXT ( ( #103933, #5256, #80183 ) ) REPRESENTATION_CONTEXT ( 'NONE', 'WORKASPACE' ) );
#4982=DIRECTION ( 'NONE',  ( 0.000000000000000000, 1.000000000000000000, 0.000000000000000000 ) ) ;
#4987=FILL_AREA_STYLE_COLOUR ( '', #37801 ) ;
#5000=CARTESIAN_POINT ( 'NONE',  ( 0.000000000000000000, -1.200583151104947843, 112.0000000000000000 ) ) ;
#5003=ORIENTED_EDGE ( 'NONE', *, *, #48024, .F. ) ;
#5013=CARTESIAN_POINT ( 'NONE',  ( 5.000000000000000888, -63.35320086162899145, 9.447768536045829890 ) ) ;
#5015=EDGE_CURVE ( 'NONE', #89992, #85394, #47496, .T. ) ;
#5056=DIRECTION ( 'NONE',  ( 0.000000000000000000, 1.000000000000000000, 0.000000000000000000 ) ) ;
#5085=PRESENTATION_STYLE_ASSIGNMENT (( #38017 ) ) ;
#5117=PLANE ( 'NONE',  #32177 ) ;
#5118=CARTESIAN_POINT ( 'NONE',  ( 5.285714285714277594, -50.19912527334259522, 103.1763305333244176 ) ) ;
#5140=LINE ( 'NONE', #96289, #3357 ) ;
#5156=UNCERTAINTY_MEASURE_WITH_UNIT (LENGTH_MEASURE( 1.000000000000000082E-05 ), #88552, 'distance_accuracy_value', 'NONE');
#5188=CARTESIAN_POINT ( 'NONE',  ( 0.000000000000000000, 0.000000000000000000, 112.0000000000000000 ) ) ;
#5216=CARTESIAN_POINT ( 'NONE',  ( 13.48739679499482058, -52.95995205322599020, 23.24594036347893677 ) ) ;
#5219=EDGE_CURVE ( 'NONE', #3905, #13645, #22528, .T. ) ;
#5245=CARTESIAN_POINT ( 'NONE',  ( -7.000000000000000000, -15.93202192939576989, -5.930487099830191511 ) ) ;
#5256=( NAMED_UNIT ( * ) PLANE_ANGLE_UNIT ( ) SI_UNIT ( $, .RADIAN. ) );
#5266=DIRECTION ( 'NONE',  ( 0.000000000000000000, 0.000000000000000000, 1.000000000000000000 ) ) ;
#5281=VERTEX_POINT ( 'NONE', #69737 ) ;
#5289=CARTESIAN_POINT ( 'NONE',  ( -4.470931500626729616, -8.781224379427507998, 13.55547115919427448 ) ) ;
#5318=SURFACE_STYLE_USAGE ( .BOTH. , #79723 ) ;
#5333=( BOUNDED_SURFACE ( )  B_SPLINE_SURFACE ( 3, 2, ( 
 ( #51430, #10437, #33684 ),
 ( #43353, #75165, #91379 ),
 ( #17497, #1258, #27206 ),
 ( #67098, #101050, #26153 ),
 ( #82197, #60095, #92960 ),
 ( #74102, #59009, #91898 ),
 ( #19120, #192, #33156 ),
 ( #20188, #60621, #4488 ),
 ( #12035, #86499, #96553 ),
 ( #20730, #12560, #35830 ),
 ( #19659, #37424, #94027 ),
 ( #3959, #47447, #55524 ) ),
 .UNSPECIFIED., .F., .F., .F. ) 
 B_SPLINE_SURFACE_WITH_KNOTS ( ( 4, 2, 2, 2, 2, 4 ),
 ( 3, 3 ),
 ( 6.615801656506548056E-16, 0.0007735885786029156547, 0.001547177157205169729, 0.001933971446506296604, 0.002320765735807423479, 0.003094354314409677661 ),
 ( 0.000000000000000000, 1.000000000000000000 ),
 .UNSPECIFIED. ) 
 GEOMETRIC_REPRESENTATION_ITEM ( )  RATIONAL_B_SPLINE_SURFACE ( (
 ( 1.000000000000000000, 0.9603284238771456760, 1.000000000000000000),
 ( 1.000000000000000000, 0.9628724889916725482, 1.000000000000000000),
 ( 1.000000000000000000, 0.9663306537744362767, 1.000000000000000000),
 ( 1.000000000000000000, 0.9744563874114811064, 1.000000000000000000),
 ( 1.000000000000000000, 0.9789903143386875506, 1.000000000000000000),
 ( 1.000000000000000000, 0.9855527733005724489, 1.000000000000000000),
 ( 1.000000000000000000, 0.9877025284828782059, 1.000000000000000000),
 ( 1.000000000000000000, 0.9916277982505483646, 1.000000000000000000),
 ( 1.000000000000000000, 0.9934221110298375734, 1.000000000000000000),
 ( 1.000000000000000000, 0.9980179737615564317, 1.000000000000000000),
 ( 1.000000000000000000, 1.000016370385808928, 1.000000000000000000),
 ( 1.000000000000000000, 1.000000000000000000, 1.000000000000000000) ) ) 
 REPRESENTATION_ITEM ( '' )  SURFACE ( )  );
#5338=CARTESIAN_POINT ( 'NONE',  ( 4.551587301587302292, -1.200583151104948731, 104.4018401814738155 ) ) ;
#5350=CARTESIAN_POINT ( 'NONE',  ( 2.323340773570302442, -0.2161414388124262287, 102.3935653434436688 ) ) ;
#5363=CARTESIAN_POINT ( 'NONE',  ( -9.586442202745699248, -3.380526504394860687, 14.88677015134535608 ) ) ;
#5380=CARTESIAN_POINT ( 'NONE',  ( 8.572527594031475162E-16, -46.00000000000000000, 105.0000000000000000 ) ) ;
#5398=EDGE_CURVE ( 'NONE', #63587, #76134, #37309, .T. ) ;
#5400=EDGE_CURVE ( 'NONE', #56691, #12868, #73872, .T. ) ;
#5420=ORIENTED_EDGE ( 'NONE', *, *, #69631, .F. ) ;
#5436=CARTESIAN_POINT ( 'NONE',  ( 4.999999999999065636, -61.61648432250720475, 12.73941221456567163 ) ) ;
#5446=CARTESIAN_POINT ( 'NONE',  ( -9.677640526858340309, -50.98637785014530976, 24.47418066717162333 ) ) ;
#5467=EDGE_CURVE ( 'NONE', #80842, #64161, #21828, .T. ) ;
#5470=CARTESIAN_POINT ( 'NONE',  ( -5.000000000000000888, -40.36500490292060306, -0.7636728796266644137 ) ) ;
#5479=COLOUR_RGB ( '', 0.31764706, 0.68627451, 0.89019608) ;
#5493=VECTOR ( 'NONE', #38270, 1000.000000000000000 ) ;
#5495=PRESENTATION_STYLE_ASSIGNMENT (( #71280 ) ) ;
#5506=( NAMED_UNIT ( * ) SI_UNIT ( $, .STERADIAN. ) SOLID_ANGLE_UNIT ( ) );
#5510=DIRECTION ( 'NONE',  ( 0.000000000000000000, 0.000000000000000000, 1.000000000000000000 ) ) ;
#5516=MECHANICAL_DESIGN_GEOMETRIC_PRESENTATION_REPRESENTATION('',(#41704),#26281);
#5533=CARTESIAN_POINT ( 'NONE',  ( 1.000000000000000000, -40.36147667352812363, -0.7651093971834536100 ) ) ;
#5576=EDGE_LOOP ( 'NONE', ( #30220, #95488, #4852, #52584, #43115, #100259 ) ) ;
#5591=EDGE_CURVE ( 'NONE', #3333, #57238, #82057, .T. ) ;
#5614=CARTESIAN_POINT ( 'NONE',  ( 0.000000000000000000, -48.79941684889505638, 112.0000000000000000 ) ) ;
#5637=EDGE_LOOP ( 'NONE', ( #49667, #28021, #32433, #57468 ) ) ;
#5666=( GEOMETRIC_REPRESENTATION_CONTEXT ( 3 ) GLOBAL_UNCERTAINTY_ASSIGNED_CONTEXT ( ( #63993 ) ) GLOBAL_UNIT_ASSIGNED_CONTEXT ( ( #22994, #73081, #6777 ) ) REPRESENTATION_CONTEXT ( 'NONE', 'WORKASPACE' ) );
#5701=VERTEX_POINT ( 'NONE', #52959 ) ;
#5716=EDGE_CURVE ( 'NONE', #26896, #44023, #30154, .T. ) ;
#5730=CARTESIAN_POINT ( 'NONE',  ( 13.87298779988979724, -50.40831034641927033, 28.89736879381397827 ) ) ;
#5736=B_SPLINE_CURVE_WITH_KNOTS ( 'NONE', 3,
 ( #53237, #21951, #70484, #5216, #29526, #13813, #62398, #54802, #95290, #38655, #79617, #4687, #21421, #103895, #87734, #103379, #13279, #19851, #38146, #93698, #37621, #5730, #46207, #79093, #20923, #29016, #46725, #71521, #104422, #30569, #52686, #85614, #86160, #11689 ),
 .UNSPECIFIED., .F., .F.,
 ( 4, 2, 2, 2, 2, 2, 2, 2, 2, 2, 2, 2, 2, 2, 2, 2, 4 ),
 ( 0.000000000000000000, 0.0007857361314144349846, 0.001571472262828869969, 0.002357208394243305062, 0.003142944525657739938, 0.003928680657072174814, 0.004714416788486610124, 0.005500152919901044567, 0.006285889051315479877, 0.007071625182729915186, 0.007857361314144349629, 0.008643097445558784939, 0.009428833576973220248, 0.01021456970838765556, 0.01100030583980208913, 0.01178604197121652444, 0.01257177810263095975 ),
 .UNSPECIFIED. ) ;
#5765=VERTEX_POINT ( 'NONE', #89042 ) ;
#5783=CARTESIAN_POINT ( 'NONE',  ( 5.000000000000000000, -13.85537367033550638, 10.16084852767000868 ) ) ;
#5794=CARTESIAN_POINT ( 'NONE',  ( 2.911360389275831295, -70.20793806422989292, 13.30423068689236210 ) ) ;
#5800=CARTESIAN_POINT ( 'NONE',  ( -10.91923657161825822, -10.68772801090689839, 18.23046311196159053 ) ) ;
#5812=ORIENTED_EDGE ( 'NONE', *, *, #18093, .F. ) ;
#5868=CARTESIAN_POINT ( 'NONE',  ( -7.882737400093250635, 3.052883471114401726, 14.68611362084002714 ) ) ;
#5951=ORIENTED_EDGE ( 'NONE', *, *, #52085, .F. ) ;
#5957=( NAMED_UNIT ( * ) PLANE_ANGLE_UNIT ( ) SI_UNIT ( $, .RADIAN. ) );
#5961=DIRECTION ( 'NONE',  ( 0.000000000000000000, 0.000000000000000000, 1.000000000000000000 ) ) ;
#5977=ORIENTED_EDGE ( 'NONE', *, *, #97486, .T. ) ;
#5989=UNCERTAINTY_MEASURE_WITH_UNIT (LENGTH_MEASURE( 1.000000000000000082E-05 ), #90708, 'distance_accuracy_value', 'NONE');
#6006=DIRECTION ( 'NONE',  ( 0.000000000000000000, -1.000000000000000000, 0.000000000000000000 ) ) ;
#6008=SURFACE_SIDE_STYLE ('',( #38418 ) ) ;
#6011=FILL_AREA_STYLE ('',( #47003 ) ) ;
#6012=DIRECTION ( 'NONE',  ( 0.000000000000000000, 0.000000000000000000, 1.000000000000000000 ) ) ;
#6033=VERTEX_POINT ( 'NONE', #23673 ) ;
#6041=CARTESIAN_POINT ( 'NONE',  ( 3.351411280263732362, -49.00492482622130552, 104.3292055665660456 ) ) ;
#6051=FILL_AREA_STYLE ('',( #14139 ) ) ;
#6119=CARTESIAN_POINT ( 'NONE',  ( -1.000000000000000000, -56.57158839598558586, 6.200363299246187232 ) ) ;
#6126=CARTESIAN_POINT ( 'NONE',  ( -5.000000000000000888, -46.00000000000000000, 42.58845726811989607 ) ) ;
#6131=ADVANCED_FACE ( 'NONE', ( #41415 ), #74831, .F. ) ;
#6161=EDGE_CURVE ( 'NONE', #99731, #3333, #29095, .T. ) ;
#6173=SURFACE_STYLE_USAGE ( .BOTH. , #87654 ) ;
#6191=ORIENTED_EDGE ( 'NONE', *, *, #68616, .F. ) ;
#6195=DIRECTION ( 'NONE',  ( 0.000000000000000000, 0.000000000000000000, -1.000000000000000000 ) ) ;
#6233=SURFACE_STYLE_FILL_AREA ( #104405 ) ;
#6246=( LENGTH_UNIT ( ) NAMED_UNIT ( * ) SI_UNIT ( .MILLI., .METRE. ) );
#6262=CARTESIAN_POINT ( 'NONE',  ( 1.000000000000004441, -69.59657292934913642, 12.76848391599222410 ) ) ;
#6289=CARTESIAN_POINT ( 'NONE',  ( 3.910186774093608264, -1.060342764005019589, 104.5757226097576336 ) ) ;
#6298=SURFACE_STYLE_FILL_AREA ( #40803 ) ;
#6313=SURFACE_SIDE_STYLE ('',( #83798 ) ) ;
#6319=CARTESIAN_POINT ( 'NONE',  ( -13.71361667675544993, -8.878897062923181593, 12.10099128770297661 ) ) ;
#6326=ORIENTED_EDGE ( 'NONE', *, *, #2754, .F. ) ;
#6355=CARTESIAN_POINT ( 'NONE',  ( -5.000000000000000888, -50.00000000000000000, 42.58845726811989607 ) ) ;
#6371=PRESENTATION_STYLE_ASSIGNMENT (( #88902 ) ) ;
#6372=ORIENTED_EDGE ( 'NONE', *, *, #54863, .T. ) ;
#6391=PRESENTATION_STYLE_ASSIGNMENT (( #97518 ) ) ;
#6405=SURFACE_STYLE_USAGE ( .BOTH. , #106699 ) ;
#6420=CARTESIAN_POINT ( 'NONE',  ( -6.158544544216538519, -12.16561743015693153, 11.88011416285757349 ) ) ;
#6423=( NAMED_UNIT ( * ) SI_UNIT ( $, .STERADIAN. ) SOLID_ANGLE_UNIT ( ) );
#6485=CARTESIAN_POINT ( 'NONE',  ( 9.574562898131892652, -51.35212381342775956, 24.10796671758935261 ) ) ;
#6489=CARTESIAN_POINT ( 'NONE',  ( -9.574118164638793615, -51.35373487335582610, 24.10642939627973291 ) ) ;
#6533=CARTESIAN_POINT ( 'NONE',  ( -2.520370815125278163, -0.4217707021250795552, 103.1554032654397588 ) ) ;
#6536=FILL_AREA_STYLE ('',( #91077 ) ) ;
#6580=CARTESIAN_POINT ( 'NONE',  ( 1.000000000000000000, -59.33342285666933691, 7.478329308248535590 ) ) ;
#6620=CARTESIAN_POINT ( 'NONE',  ( -3.433100064643267224, -49.17501837727334646, 103.8029703184011368 ) ) ;
#6630=AXIS2_PLACEMENT_3D ( 'NONE', #100257, #94725, #94176 ) ;
#6633=CARTESIAN_POINT ( 'NONE',  ( 4.175533140205451410, -1.555218955346045595, 102.9090322054120747 ) ) ;
#6660=PRODUCT_CONTEXT ( 'NONE', #61797, 'mechanical' ) ;
#6693=ORIENTED_EDGE ( 'NONE', *, *, #34723, .F. ) ;
#6737=CARTESIAN_POINT ( 'NONE',  ( 14.15420665121519939, 0.7683508055187184826, 14.98090773217467664 ) ) ;
#6757=CARTESIAN_POINT ( 'NONE',  ( -6.054168735073517382, -62.91602293657745548, 14.37668516551084075 ) ) ;
#6764=CARTESIAN_POINT ( 'NONE',  ( 0.000000000000000000, -78.00000000000000000, 39.00000000000000000 ) ) ;
#6766=FILL_AREA_STYLE ('',( #47744 ) ) ;
#6777=( NAMED_UNIT ( * ) SI_UNIT ( $, .STERADIAN. ) SOLID_ANGLE_UNIT ( ) );
#6829=CARTESIAN_POINT ( 'NONE',  ( -4.999999999999993783, -4.000000000000002665, 102.2532056551910387 ) ) ;
#6839=CARTESIAN_POINT ( 'NONE',  ( 5.000000000000000000, -13.90268927672022947, 9.980021953238734866 ) ) ;
#6861=CARTESIAN_POINT ( 'NONE',  ( 4.750186375024036955, -48.62189236691690297, 104.3180500829682131 ) ) ;
#6872=AXIS2_PLACEMENT_3D ( 'NONE', #102579, #19586, #86421 ) ;
#6898=( NAMED_UNIT ( * ) PLANE_ANGLE_UNIT ( ) SI_UNIT ( $, .RADIAN. ) );
#6910=( LENGTH_UNIT ( ) NAMED_UNIT ( * ) SI_UNIT ( .MILLI., .METRE. ) );
#6929=SURFACE_SIDE_STYLE ('',( #7446 ) ) ;
#6946=B_SPLINE_CURVE_WITH_KNOTS ( 'NONE', 3,
 ( #42118, #66946, #69080, #59393, #60470, #75004, #93348, #51804, #52336, #101953, #9210, #58859, #50723, #34073, #103034, #52877, #20581, #13462, #102499, #30758, #78728, #45854, #95461, #85805, #53927, #86858, #44806, #13992, #46384, #63100, #29190, #11879, #53419, #54438 ),
 .UNSPECIFIED., .F., .F.,
 ( 4, 2, 2, 2, 2, 2, 2, 2, 2, 2, 2, 2, 2, 2, 2, 2, 4 ),
 ( 0.01257177810263095975, 0.01335728547384937119, 0.01414279284506778263, 0.01492830021628619580, 0.01571380758750460724, 0.01649931495872301868, 0.01728482232994143011, 0.01807032970115984155, 0.01885583707237825299, 0.01964134444359666443, 0.02042685181481507933, 0.02121235918603348730, 0.02199786655725190221, 0.02278337392847031018, 0.02356888129968872508, 0.02435438867090713652, 0.02513989604212554796 ),
 .UNSPECIFIED. ) ;
#6959=CARTESIAN_POINT ( 'NONE',  ( -5.000000000000000000, -14.50704001784967012, 12.23934196172818289 ) ) ;
#7020=ORIENTED_EDGE ( 'NONE', *, *, #4729, .F. ) ;
#7026=DIRECTION ( 'NONE',  ( 0.000000000000000000, 1.000000000000000000, -1.224646799147353207E-16 ) ) ;
#7029=AXIS2_PLACEMENT_3D ( 'NONE', #87377, #38310, #36736 ) ;
#7048=CARTESIAN_POINT ( 'NONE',  ( -4.175533140205450522, -48.44478104465395774, 102.9090322054120890 ) ) ;
#7070=CARTESIAN_POINT ( 'NONE',  ( -3.352941176470589646, -48.79941684889505638, 104.5794940929807524 ) ) ;
#7071=UNCERTAINTY_MEASURE_WITH_UNIT (LENGTH_MEASURE( 1.000000000000000082E-05 ), #3639, 'distance_accuracy_value', 'NONE');
#7091=DIRECTION ( 'NONE',  ( 0.000000000000000000, 0.000000000000000000, 1.000000000000000000 ) ) ;
#7110=CARTESIAN_POINT ( 'NONE',  ( 9.728280252476675827, -57.17794266280819926, 24.67413300948206967 ) ) ;
#7115=CARTESIAN_POINT ( 'NONE',  ( 15.26274976730916499, -5.960238452850545876, 13.77689897405315200 ) ) ;
#7171=FACE_OUTER_BOUND ( 'NONE', #21911, .T. ) ;
#7185=CARTESIAN_POINT ( 'NONE',  ( -10.51914831753094148, -11.53309007499742478, 17.75417121042075053 ) ) ;
#7187=CARTESIAN_POINT ( 'NONE',  ( -4.572719631913240157, -47.86564882870907667, 40.42917486031264929 ) ) ;
#7203=COLOUR_RGB ( '', 0.40784314, 0.44705882, 0.49803922) ;
#7216=SURFACE_STYLE_FILL_AREA ( #73000 ) ;
#7266=ORIENTED_EDGE ( 'NONE', *, *, #92792, .T. ) ;
#7276=CARTESIAN_POINT ( 'NONE',  ( -4.458592195379179834, -66.17896604625831003, 13.13601379408565961 ) ) ;
#7282=AXIS2_PLACEMENT_3D ( 'NONE', #31912, #12, #6012 ) ;
#7286=SURFACE_STYLE_USAGE ( .BOTH. , #72562 ) ;
#7307=DIRECTION ( 'NONE',  ( 0.000000000000000000, 0.000000000000000000, 1.000000000000000000 ) ) ;
#7312=EDGE_CURVE ( 'NONE', #97430, #3119, #18790, .T. ) ;
#7316=CARTESIAN_POINT ( 'NONE',  ( 15.94658505612039612, -2.878035407438557236, 14.72409133791870595 ) ) ;
#7339=CARTESIAN_POINT ( 'NONE',  ( 5.000000000000000000, -32.50000000000000000, 13.00000000000000178 ) ) ;
#7340=( GEOMETRIC_REPRESENTATION_CONTEXT ( 3 ) GLOBAL_UNCERTAINTY_ASSIGNED_CONTEXT ( ( #55326 ) ) GLOBAL_UNIT_ASSIGNED_CONTEXT ( ( #12742, #82252, #72572 ) ) REPRESENTATION_CONTEXT ( 'NONE', 'WORKASPACE' ) );
#7355=CARTESIAN_POINT ( 'NONE',  ( -5.437321008177367077, -2.342832151771177429, 104.0362115404844587 ) ) ;
#7364=FILL_AREA_STYLE_COLOUR ( '', #71436 ) ;
#7376=ORIENTED_EDGE ( 'NONE', *, *, #40651, .T. ) ;
#7378=CARTESIAN_POINT ( 'NONE',  ( -4.804117642141982891, -64.31448375944374618, 13.02803471175172945 ) ) ;
#7384=CARTESIAN_POINT ( 'NONE',  ( 4.902312018371809188, -46.91782384206802448, 103.3400275729950692 ) ) ;
#7405=DIRECTION ( 'NONE',  ( 0.000000000000000000, 1.000000000000000000, 0.000000000000000000 ) ) ;
#7414=CARTESIAN_POINT ( 'NONE',  ( -4.031080902170634417, -48.62189207507201161, 103.0284855429847681 ) ) ;
#7419=CARTESIAN_POINT ( 'NONE',  ( -4.225138137263944493, -48.93880982128749224, 104.4756818702664134 ) ) ;
#7428=DIRECTION ( 'NONE',  ( 0.000000000000000000, 0.000000000000000000, 1.000000000000000000 ) ) ;
#7446=SURFACE_STYLE_FILL_AREA ( #73784 ) ;
#7477=CARTESIAN_POINT ( 'NONE',  ( -5.000000000000000000, -14.06131484383571717, 13.29904837184955824 ) ) ;
#7528=CARTESIAN_POINT ( 'NONE',  ( 2.125394136664333633, -69.49483494517815529, 12.89457257817287328 ) ) ;
#7538=CARTESIAN_POINT ( 'NONE',  ( 9.171181789971550202, -52.95185826047487154, 30.98656384792473162 ) ) ;
#7543=CARTESIAN_POINT ( 'NONE',  ( -9.820360545668073371, -50.41108204965477313, 28.90271669672396726 ) ) ;
#7576=DIRECTION ( 'NONE',  ( 0.000000000000000000, 0.000000000000000000, -1.000000000000000000 ) ) ;
#7600=COLOUR_RGB ( '', 0.66274510, 0.83137255, 0.94901961) ;
#7603=EDGE_LOOP ( 'NONE', ( #57407, #42936, #68682, #86439 ) ) ;
#7620=CARTESIAN_POINT ( 'NONE',  ( 13.48753244636324489, -55.04205951323852730, 23.24642415514733429 ) ) ;
#7624=CARTESIAN_POINT ( 'NONE',  ( 6.999999999999993783, -46.00000000000000000, 102.2532056551910387 ) ) ;
#7638=FILL_AREA_STYLE_COLOUR ( '', #83452 ) ;
#7644=CARTESIAN_POINT ( 'NONE',  ( -2.894864961504455270, -49.53440618355075031, 103.3614437639316463 ) ) ;
#7680=( GEOMETRIC_REPRESENTATION_CONTEXT ( 3 ) GLOBAL_UNCERTAINTY_ASSIGNED_CONTEXT ( ( #105251 ) ) GLOBAL_UNIT_ASSIGNED_CONTEXT ( ( #679, #17460, #34189 ) ) REPRESENTATION_CONTEXT ( 'NONE', 'WORKASPACE' ) );
#7694=( GEOMETRIC_REPRESENTATION_CONTEXT ( 3 ) GLOBAL_UNCERTAINTY_ASSIGNED_CONTEXT ( ( #29725 ) ) GLOBAL_UNIT_ASSIGNED_CONTEXT ( ( #4652, #21390, #47208 ) ) REPRESENTATION_CONTEXT ( 'NONE', 'WORKASPACE' ) );
#7712=ORIENTED_EDGE ( 'NONE', *, *, #69802, .T. ) ;
#7716=MECHANICAL_DESIGN_GEOMETRIC_PRESENTATION_REPRESENTATION('',(#66318),#68019);
#7718=CARTESIAN_POINT ( 'NONE',  ( -3.505862197715600814, -49.11848138796074892, 103.6125913840231902 ) ) ;
#7721=DIRECTION ( 'NONE',  ( 0.000000000000000000, 1.000000000000000000, 0.000000000000000000 ) ) ;
#7733=( NAMED_UNIT ( * ) SI_UNIT ( $, .STERADIAN. ) SOLID_ANGLE_UNIT ( ) );
#7797=EDGE_CURVE ( 'NONE', #77091, #45005, #96641, .T. ) ;
#7798=ORIENTED_EDGE ( 'NONE', *, *, #13852, .T. ) ;
#7805=CARTESIAN_POINT ( 'NONE',  ( -3.175070672093349700, -70.04843617429949632, 13.36307156052828127 ) ) ;
#7814=PRESENTATION_STYLE_ASSIGNMENT (( #90342 ) ) ;
#7866=CARTESIAN_POINT ( 'NONE',  ( 0.8749999999999992228, -70.58759490697438821, 13.02737050516260098 ) ) ;
#7868=ADVANCED_FACE ( 'NONE', ( #63744 ), #105015, .T. ) ;
#7873=CARTESIAN_POINT ( 'NONE',  ( 3.857142857142850101, -48.79941684889506348, 103.1763305333244176 ) ) ;
#7914=CARTESIAN_POINT ( 'NONE',  ( 6.033336773385737040, -14.92884390011191975, 14.31563199681414034 ) ) ;
#7920=CARTESIAN_POINT ( 'NONE',  ( 5.374793246923686318, -47.77528324145958294, 104.0614974883207680 ) ) ;
#7934=CARTESIAN_POINT ( 'NONE',  ( -2.680466883780622034, -7.322484912031441695, -13.10124357497377012 ) ) ;
#7950=CARTESIAN_POINT ( 'NONE',  ( -4.792515968931544634, -47.29776092521724706, 102.4138677444032055 ) ) ;
#7954=CARTESIAN_POINT ( 'NONE',  ( 2.505859880111868332, -49.58693854473261808, 103.1328899680561904 ) ) ;
#7955=DIRECTION ( 'NONE',  ( 0.000000000000000000, 0.000000000000000000, 1.000000000000000000 ) ) ;
#7994=CARTESIAN_POINT ( 'NONE',  ( -6.458864185833882665, -0.2568716777371773397, 15.39536780018543993 ) ) ;
#8018=CARTESIAN_POINT ( 'NONE',  ( -5.000000000000039968, -14.59885031841968228, 13.58543933205532817 ) ) ;
#8039=CARTESIAN_POINT ( 'NONE',  ( 13.57536397604353340, 1.208058863777641267, 14.95207728893323562 ) ) ;
#8074=CARTESIAN_POINT ( 'NONE',  ( 4.225954871949793912, -66.94789023181898813, 13.14696679065552765 ) ) ;
#8084=CARTESIAN_POINT ( 'NONE',  ( 9.215420734788356327, -54.00000000000000000, 23.11721482942554928 ) ) ;
#8095=CARTESIAN_POINT ( 'NONE',  ( 5.833333333333329485, -46.00000000000000000, 103.8776713793258608 ) ) ;
#8101=PRESENTATION_STYLE_ASSIGNMENT (( #81979 ) ) ;
#8139=COLOUR_RGB ( '', 0.08235294, 0.09019608, 0.10196078) ;
#8171=( NAMED_UNIT ( * ) PLANE_ANGLE_UNIT ( ) SI_UNIT ( $, .RADIAN. ) );
#8178=CARTESIAN_POINT ( 'NONE',  ( 9.215420734788356327, -54.00000000000000000, 23.11721482942554928 ) ) ;
#8186=( NAMED_UNIT ( * ) PLANE_ANGLE_UNIT ( ) SI_UNIT ( $, .RADIAN. ) );
#8208=CARTESIAN_POINT ( 'NONE',  ( -0.7777777777777781232, -54.00000000000000711, 40.97837836547555668 ) ) ;
#8214=CARTESIAN_POINT ( 'NONE',  ( -9.901690565149895207, -57.79096752242128332, 28.42036373910763558 ) ) ;
#8229=SURFACE_STYLE_USAGE ( .BOTH. , #74551 ) ;
#8254=CARTESIAN_POINT ( 'NONE',  ( -3.454253436624922458, -49.15858197120396511, 103.7259032015043090 ) ) ;
#8270=( GEOMETRIC_REPRESENTATION_CONTEXT ( 3 ) GLOBAL_UNCERTAINTY_ASSIGNED_CONTEXT ( ( #24646 ) ) GLOBAL_UNIT_ASSIGNED_CONTEXT ( ( #17419, #75087, #68081 ) ) REPRESENTATION_CONTEXT ( 'NONE', 'WORKASPACE' ) );
#8282=AXIS2_PLACEMENT_3D ( 'NONE', #11201, #77018, #5266 ) ;
#8286=DIRECTION ( 'NONE',  ( 6.051620703560613215E-16, 0.3488521823429523994, -0.9371777605526925292 ) ) ;
#8296=COLOUR_RGB ( '', 0.31764706, 0.68627451, 0.89019608) ;
#8331=CARTESIAN_POINT ( 'NONE',  ( -15.83718408913613374, -1.753567716153235923, 14.89780694040802267 ) ) ;
#8344=CARTESIAN_POINT ( 'NONE',  ( -2.907876107285823686, -69.03782668178834570, 13.00348232047688768 ) ) ;
#8345=CARTESIAN_POINT ( 'NONE',  ( 2.705399370281704297, -49.45330424000481173, 103.4497616813456631 ) ) ;
#8366=VERTEX_POINT ( 'NONE', #36717 ) ;
#8386=CARTESIAN_POINT ( 'NONE',  ( 2.342558418285032307, -49.77031626379333318, 44.62063500984325515 ) ) ;
#8394=( NAMED_UNIT ( * ) SI_UNIT ( $, .STERADIAN. ) SOLID_ANGLE_UNIT ( ) );
#8405=CARTESIAN_POINT ( 'NONE',  ( 4.472061920348587627, -67.30643333997242905, 13.71894798482393441 ) ) ;
#8436=CARTESIAN_POINT ( 'NONE',  ( 5.988549711970140521, -14.40160760345763435, 14.13124080977622476 ) ) ;
#8457=CARTESIAN_POINT ( 'NONE',  ( 4.051286199644062336, -48.60127012969240923, 103.8758286790404952 ) ) ;
#8466=ADVANCED_FACE ( 'NONE', ( #89476 ), #77072, .F. ) ;
#8486=CARTESIAN_POINT ( 'NONE',  ( -5.164787682159340143, -48.11244280217349001, 104.1470044518086837 ) ) ;
#8521=CARTESIAN_POINT ( 'NONE',  ( 6.999999999999993783, -50.00000000000000000, 102.2532056551910387 ) ) ;
#8553=AXIS2_PLACEMENT_3D ( 'NONE', #2606, #12295, #70553 ) ;
#8554=CARTESIAN_POINT ( 'NONE',  ( -5.000000000000000000, -13.89959410955659891, 11.33893914917399925 ) ) ;
#8558=CARTESIAN_POINT ( 'NONE',  ( -30.00000000000000000, 0.000000000000000000, -11.00000000000000000 ) ) ;
#8575=CARTESIAN_POINT ( 'NONE',  ( 12.41126668015367862, -3.690571904192825325, 20.54162461381810090 ) ) ;
#8581=DIRECTION ( 'NONE',  ( 0.000000000000000000, 0.000000000000000000, -1.000000000000000000 ) ) ;
#8613=CARTESIAN_POINT ( 'NONE',  ( 9.336538098104073313, -51.98968743527834846, 30.58506923019146839 ) ) ;
#8629=CARTESIAN_POINT ( 'NONE',  ( 5.683639242321874896, -47.06573826195068477, 103.9372442403038548 ) ) ;
#8637=CARTESIAN_POINT ( 'NONE',  ( -10.18570692333505256, -0.7115926177181285395, 20.11367956310897753 ) ) ;
#8708=CARTESIAN_POINT ( 'NONE',  ( 9.820360545668073371, -57.58891795034524108, 28.90271669672396726 ) ) ;
#8753=CIRCLE ( 'NONE', #41472, 2.000000000000001776 ) ;
#8755=SURFACE_STYLE_USAGE ( .BOTH. , #16868 ) ;
#8794=MECHANICAL_DESIGN_GEOMETRIC_PRESENTATION_REPRESENTATION('',(#41525),#13943);
#8813=CIRCLE ( 'NONE', #72571, 2.000000000000000888 ) ;
#8843=SURFACE_STYLE_FILL_AREA ( #2346 ) ;
#8849=ORIENTED_EDGE ( 'NONE', *, *, #36673, .F. ) ;
#8860=CARTESIAN_POINT ( 'NONE',  ( -15.90614609307868399, -3.157894736842107530, 14.66382285868950675 ) ) ;
#8877=CARTESIAN_POINT ( 'NONE',  ( -2.914466931036500341, -69.57166512993157426, 13.30289308728773001 ) ) ;
#8880=ORIENTED_EDGE ( 'NONE', *, *, #94659, .F. ) ;
#8911=CARTESIAN_POINT ( 'NONE',  ( -5.000000000000000000, -60.71953810597282342, 12.61250543006821978 ) ) ;
#8934=CARTESIAN_POINT ( 'NONE',  ( 5.624554194580569266, -65.83898597127696917, 14.17938030110289560 ) ) ;
#8955=ORIENTED_EDGE ( 'NONE', *, *, #94181, .T. ) ;
#8959=CARTESIAN_POINT ( 'NONE',  ( 5.000000000000000888, -14.19087030043145603, 13.37859801196370313 ) ) ;
#8977=CARTESIAN_POINT ( 'NONE',  ( 5.979482036612520979, -14.26481676427871470, 14.07238976267240815 ) ) ;
#8981=EDGE_LOOP ( 'NONE', ( #16881, #51707, #69251, #45826 ) ) ;
#8984=ORIENTED_EDGE ( 'NONE', *, *, #91225, .T. ) ;
#9001=CARTESIAN_POINT ( 'NONE',  ( 0.000000000000000000, -80.00000000000000000, 27.00000000000000000 ) ) ;
#9010=MECHANICAL_DESIGN_GEOMETRIC_PRESENTATION_REPRESENTATION('',(#98550),#81362);
#9068=PRESENTATION_STYLE_ASSIGNMENT (( #92119 ) ) ;
#9090=MECHANICAL_DESIGN_GEOMETRIC_PRESENTATION_REPRESENTATION('',(#57200),#50429);
#9099=CARTESIAN_POINT ( 'NONE',  ( 9.587897109658308992, -3.381009470459365840, 14.88767535522079122 ) ) ;
#9110=FILL_AREA_STYLE ('',( #66297 ) ) ;
#9128=CARTESIAN_POINT ( 'NONE',  ( 4.586505539341392712, -65.62869095158480093, 13.11449450926818905 ) ) ;
#9156=DIRECTION ( 'NONE',  ( 0.000000000000000000, 0.000000000000000000, 1.000000000000000000 ) ) ;
#9179=SURFACE_STYLE_FILL_AREA ( #82558 ) ;
#9210=CARTESIAN_POINT ( 'NONE',  ( -13.76576316043658643, -50.82162839084075756, 29.55959131405483475 ) ) ;
#9219=ORIENTED_EDGE ( 'NONE', *, *, #77028, .F. ) ;
#9225=FILL_AREA_STYLE ('',( #66959 ) ) ;
#9231=CARTESIAN_POINT ( 'NONE',  ( -3.423905177083978568, -0.8279751000748389878, 103.8439100969757902 ) ) ;
#9238=( BOUNDED_SURFACE ( )  B_SPLINE_SURFACE ( 3, 2, ( 
 ( #79061, #62892, #20358 ),
 ( #95784, #12192, #45123 ),
 ( #28975, #20888, #78519 ),
 ( #53721, #86651, #45643 ),
 ( #37585, #70448, #72552 ),
 ( #39677, #89812, #55810 ),
 ( #90333, #64482, #97351 ),
 ( #31597, #8877, #7805 ),
 ( #8344, #105457, #82231 ),
 ( #98934, #81166, #49867 ),
 ( #16441, #96846, #22974 ),
 ( #23505, #222, #73601 ),
 ( #56885, #82773, #25094 ),
 ( #15912, #47735, #48790 ),
 ( #80634, #98420, #41248 ),
 ( #7276, #49324, #41781 ),
 ( #74137, #81683, #33186 ),
 ( #56349, #15378, #73062 ),
 ( #89284, #97889, #57951 ),
 ( #90875, #40713, #16989 ),
 ( #48265, #40184, #6757 ),
 ( #106505, #105970, #66057 ),
 ( #74663, #32661, #88746 ),
 ( #24572, #32114, #24044 ) ),
 .UNSPECIFIED., .F., .F., .F. ) 
 B_SPLINE_SURFACE_WITH_KNOTS ( ( 4, 2, 2, 2, 2, 2, 2, 2, 2, 2, 2, 4 ),
 ( 3, 3 ),
 ( -4.813857645835639687E-17, 0.0008230535544303435634, 0.001646107108860735265, 0.002469160663291127076, 0.003292214217721518670, 0.004115267772151910697, 0.004938321326582301857, 0.006584428435443085911, 0.008230535544303869966, 0.009876642653164652286, 0.01152274976202543634, 0.01316885687088622039 ),
 ( 0.000000000000000000, 1.000000000000000000 ),
 .UNSPECIFIED. ) 
 GEOMETRIC_REPRESENTATION_ITEM ( )  RATIONAL_B_SPLINE_SURFACE ( (
 ( 1.000000000000000000, 0.9661530732048738690, 1.000000000000000000),
 ( 1.000000000000000000, 0.9666063512417644166, 1.000000000000000000),
 ( 1.000000000000000000, 0.9668885125913321277, 1.000000000000000000),
 ( 1.000000000000000000, 0.9671064463919448739, 1.000000000000000000),
 ( 1.000000000000000000, 0.9670400754974565194, 1.000000000000000000),
 ( 1.000000000000000000, 0.9665156221367009470, 1.000000000000000000),
 ( 1.000000000000000000, 0.9660635237047728863, 1.000000000000000000),
 ( 1.000000000000000000, 0.9647383115599591497, 1.000000000000000000),
 ( 1.000000000000000000, 0.9638533720310250574, 1.000000000000000000),
 ( 1.000000000000000000, 0.9616640248515039291, 1.000000000000000000),
 ( 1.000000000000000000, 0.9603588023342733981, 1.000000000000000000),
 ( 1.000000000000000000, 0.9572958383012356576, 1.000000000000000000),
 ( 1.000000000000000000, 0.9555348605131571693, 1.000000000000000000),
 ( 1.000000000000000000, 0.9497070466053008087, 1.000000000000000000),
 ( 1.000000000000000000, 0.9450513559736188895, 1.000000000000000000),
 ( 1.000000000000000000, 0.9341981514132724485, 1.000000000000000000),
 ( 1.000000000000000000, 0.9281422303525033168, 1.000000000000000000),
 ( 1.000000000000000000, 0.9149199938659065001, 1.000000000000000000),
 ( 1.000000000000000000, 0.9077435111970268977, 1.000000000000000000),
 ( 1.000000000000000000, 0.8923013556734193941, 1.000000000000000000),
 ( 1.000000000000000000, 0.8840358383164468314, 1.000000000000000000),
 ( 1.000000000000000000, 0.8666181798904939448, 1.000000000000000000),
 ( 1.000000000000000000, 0.8574420302237928393, 1.000000000000000000),
 ( 1.000000000000000000, 0.8477912478909354066, 1.000000000000000000) ) ) 
 REPRESENTATION_ITEM ( '' )  SURFACE ( )  );
#9239=CARTESIAN_POINT ( 'NONE',  ( 6.838568993993028755, -6.773438558311645430, 13.91365169226505927 ) ) ;
#9243=CARTESIAN_POINT ( 'NONE',  ( -3.215218824033913680, -48.98362140152097766, 104.3206516315225940 ) ) ;
#9293=CARTESIAN_POINT ( 'NONE',  ( -5.000000000000000888, -67.36501624949291056, 11.52273887431363697 ) ) ;
#9309=DIRECTION ( 'NONE',  ( 0.000000000000000000, 0.000000000000000000, 1.000000000000000000 ) ) ;
#9321=VECTOR ( 'NONE', #84543, 1000.000000000000000 ) ;
#9331=CARTESIAN_POINT ( 'NONE',  ( -13.85357083679006251, -8.697779628897517767, 12.23407158846710985 ) ) ;
#9344=CARTESIAN_POINT ( 'NONE',  ( 15.61654987365426983, -4.700132877332916514, 14.24804686413672528 ) ) ;
#9372=CARTESIAN_POINT ( 'NONE',  ( 0.000000000000000000, -4.000000000000003553, 27.00000000000000000 ) ) ;
#9373=AXIS2_PLACEMENT_3D ( 'NONE', #76479, #83510, #19374 ) ;
#9382=EDGE_LOOP ( 'NONE', ( #101256, #63652, #3205, #91433 ) ) ;
#9390=DIRECTION ( 'NONE',  ( 0.6505632072693934287, 0.6639782930160490482, 0.3686466326319202125 ) ) ;
#9427=DIRECTION ( 'NONE',  ( 1.000000000000000000, 0.000000000000000000, 0.000000000000000000 ) ) ;
#9431=CARTESIAN_POINT ( 'NONE',  ( 4.855129149332425342, -47.10165964154809615, 42.75273515042984229 ) ) ;
#9457=CARTESIAN_POINT ( 'NONE',  ( 6.125000001138555028, -61.81780766021304885, 14.41094225185805477 ) ) ;
#9477=UNCERTAINTY_MEASURE_WITH_UNIT (LENGTH_MEASURE( 1.000000000000000082E-05 ), #50185, 'distance_accuracy_value', 'NONE');
#9486=CARTESIAN_POINT ( 'NONE',  ( 5.000000000000040856, -13.35938963217494724, 12.71467713436114799 ) ) ;
#9549=UNCERTAINTY_MEASURE_WITH_UNIT (LENGTH_MEASURE( 1.000000000000000082E-05 ), #65546, 'distance_accuracy_value', 'NONE');
#9624=EDGE_LOOP ( 'NONE', ( #84174, #83832, #27247, #77449 ) ) ;
#9627=CARTESIAN_POINT ( 'NONE',  ( 12.16009604706015779, -2.477469372512389967, 20.68467756193690121 ) ) ;
#9638=( LENGTH_UNIT ( ) NAMED_UNIT ( * ) SI_UNIT ( .MILLI., .METRE. ) );
#9654=CARTESIAN_POINT ( 'NONE',  ( 3.783418949173140255, -11.62946060510860313, -10.57964823094882512 ) ) ;
#9690=CARTESIAN_POINT ( 'NONE',  ( -11.46837915170103983, -1.524771657339345721, 20.53918122967341375 ) ) ;
#9700=CARTESIAN_POINT ( 'NONE',  ( 0.3351242481862675704, -69.52513411664634191, 12.72773023341044940 ) ) ;
#9706=CARTESIAN_POINT ( 'NONE',  ( -15.92336767484350801, -2.186116430727330417, 14.84188263806296426 ) ) ;
#9765=FACE_OUTER_BOUND ( 'NONE', #93105, .T. ) ;
#9769=CARTESIAN_POINT ( 'NONE',  ( 6.101956569544443987, -7.474254432360360134, 13.82088739650973963 ) ) ;
#9773=CARTESIAN_POINT ( 'NONE',  ( -2.520370815125025477, -49.57822929787493393, 103.1554032654396735 ) ) ;
#9787=CARTESIAN_POINT ( 'NONE',  ( 5.000000000000000000, -31.04498766150742384, -0.1867737091359144008 ) ) ;
#9797=ORIENTED_EDGE ( 'NONE', *, *, #79066, .F. ) ;
#9825=CARTESIAN_POINT ( 'NONE',  ( -1.000000000000000000, -59.33879011272768622, 7.480853745783086595 ) ) ;
#9849=CIRCLE ( 'NONE', #75302, 15.00000000000000000 ) ;
#9866=( LENGTH_UNIT ( ) NAMED_UNIT ( * ) SI_UNIT ( .MILLI., .METRE. ) );
#9883=ORIENTED_EDGE ( 'NONE', *, *, #25905, .T. ) ;
#9889=CARTESIAN_POINT ( 'NONE',  ( -6.999999999999999112, 0.000000000000000000, 0.000000000000000000 ) ) ;
#9898=CARTESIAN_POINT ( 'NONE',  ( 3.505888691173186356, -49.11846080224859179, 103.6125332151819833 ) ) ;
#9947=FILL_AREA_STYLE_COLOUR ( '', #36993 ) ;
#9977=ORIENTED_EDGE ( 'NONE', *, *, #97217, .F. ) ;
#10005=CARTESIAN_POINT ( 'NONE',  ( 4.190163371923140367, -67.97891175596915048, 13.63061500497633816 ) ) ;
#10021=CARTESIAN_POINT ( 'NONE',  ( -0.8750000000009734435, -70.58759490697451611, 13.02737050516266315 ) ) ;
#10083=MECHANICAL_DESIGN_GEOMETRIC_PRESENTATION_REPRESENTATION('',(#101322),#94482);
#10089=CARTESIAN_POINT ( 'NONE',  ( -4.551587301587297851, -48.79941684889506348, 104.4018401814738013 ) ) ;
#10104=VERTEX_POINT ( 'NONE', #94188 ) ;
#10146=ORIENTED_EDGE ( 'NONE', *, *, #797, .F. ) ;
#10156=DIRECTION ( 'NONE',  ( 1.000000000000000000, -0.000000000000000000, -0.000000000000000000 ) ) ;
#10169=CARTESIAN_POINT ( 'NONE',  ( 15.75700568575396865, -1.458561159084935221, 14.93088058109044169 ) ) ;
#10188=ORIENTED_EDGE ( 'NONE', *, *, #41546, .T. ) ;
#10198=CARTESIAN_POINT ( 'NONE',  ( 2.789712857210963737, -9.223132490777652848, -12.21941282805324391 ) ) ;
#10209=CARTESIAN_POINT ( 'NONE',  ( 4.551587301587293410, -48.79941684889506348, 104.4018401814738013 ) ) ;
#10225=( LENGTH_UNIT ( ) NAMED_UNIT ( * ) SI_UNIT ( .MILLI., .METRE. ) );
#10245=CARTESIAN_POINT ( 'NONE',  ( 0.000000000000000000, -4.000000000000003553, 27.00000000000000000 ) ) ;
#10296=VERTEX_POINT ( 'NONE', #74132 ) ;
#10299=CARTESIAN_POINT ( 'NONE',  ( -3.454253436624930451, -0.8414180287960395521, 103.7259032015043232 ) ) ;
#10305=CARTESIAN_POINT ( 'NONE',  ( 5.061945117287558915, -8.365139857377744903, 13.66775534171251394 ) ) ;
#10316=ADVANCED_FACE ( 'NONE', ( #33179 ), #21134, .T. ) ;
#10355=SURFACE_SIDE_STYLE ('',( #99902 ) ) ;
#10362=CARTESIAN_POINT ( 'NONE',  ( -1.000000000000000000, -64.69605072851580019, 10.12418081636205436 ) ) ;
#10364=ADVANCED_FACE ( 'NONE', ( #10987 ), #18054, .F. ) ;
#10394=ORIENTED_EDGE ( 'NONE', *, *, #13164, .F. ) ;
#10397=CARTESIAN_POINT ( 'NONE',  ( 3.350247031700767320, -1.071204144247449586, 104.4269854689273558 ) ) ;
#10401=CARTESIAN_POINT ( 'NONE',  ( -3.964214964211822068, -12.08915882607856318, -10.21564873357087500 ) ) ;
#10404=CARTESIAN_POINT ( 'NONE',  ( -11.38238776550285003, -10.91738000822960686, 10.29643454240246214 ) ) ;
#10405=CARTESIAN_POINT ( 'NONE',  ( -6.362732954939748886, -11.89495883945591004, 10.82964177580678644 ) ) ;
#10436=CARTESIAN_POINT ( 'NONE',  ( 4.399054598113323777, -1.887557197752986804, 102.7269706464928021 ) ) ;
#10437=CARTESIAN_POINT ( 'NONE',  ( -3.801077171203096405, -48.88909605940818182, 104.1059035333590401 ) ) ;
#10444=ORIENTED_EDGE ( 'NONE', *, *, #2754, .T. ) ;
#10449=( LENGTH_UNIT ( ) NAMED_UNIT ( * ) SI_UNIT ( .MILLI., .METRE. ) );
#10480=CARTESIAN_POINT ( 'NONE',  ( 5.312125216579068443, -51.48437205207593337, 39.95393515823275266 ) ) ;
#10559=CARTESIAN_POINT ( 'NONE',  ( 4.999999999999960032, -13.81090860391464048, 13.12305563960480548 ) ) ;
#10578=EDGE_CURVE ( 'NONE', #46770, #93333, #22130, .T. ) ;
#10656=EDGE_CURVE ( 'NONE', #25416, #81100, #18317, .T. ) ;
#10661=SURFACE_SIDE_STYLE ('',( #34986 ) ) ;
#10697=CARTESIAN_POINT ( 'NONE',  ( 3.707709148205156957, -48.90047616793709295, 104.5934084724877948 ) ) ;
#10720=CARTESIAN_POINT ( 'NONE',  ( 3.684569285724539789, -8.676863831076616407, -12.27927943165980551 ) ) ;
#10728=AXIS2_PLACEMENT_3D ( 'NONE', #14983, #57033, #47878 ) ;
#10736=COLOUR_RGB ( '', 0.72549020, 0.75294118, 0.79215686) ;
#10746=PRESENTATION_STYLE_ASSIGNMENT (( #86803 ) ) ;
#10772=CARTESIAN_POINT ( 'NONE',  ( 1.000000000000000444, -69.90918681875037066, 12.94764124286841067 ) ) ;
#10820=PRESENTATION_STYLE_ASSIGNMENT (( #2201 ) ) ;
#10823=CARTESIAN_POINT ( 'NONE',  ( 0.000000000000000000, -46.00000000000000000, 112.0000000000000000 ) ) ;
#10825=CARTESIAN_POINT ( 'NONE',  ( 5.722593143194981913, -7.814937950054605231, 13.77127656069876771 ) ) ;
#10875=FILL_AREA_STYLE ('',( #50805 ) ) ;
#10877=( LENGTH_UNIT ( ) NAMED_UNIT ( * ) SI_UNIT ( .MILLI., .METRE. ) );
#10893=DIRECTION ( 'NONE',  ( -1.096832036894112098E-16, 0.000000000000000000, -1.000000000000000000 ) ) ;
#10918=CARTESIAN_POINT ( 'NONE',  ( 3.405129523702669303, -1.148734789118030619, 104.5473292671427856 ) ) ;
#10920=CARTESIAN_POINT ( 'NONE',  ( -5.109687690909018087, -13.89725820713649895, -5.663713107265619939 ) ) ;
#10933=EDGE_LOOP ( 'NONE', ( #81504, #42124, #47860, #26954 ) ) ;
#10934=CARTESIAN_POINT ( 'NONE',  ( 9.322265351940091094, -11.89100710989636411, 9.148759095228598426 ) ) ;
#10957=CARTESIAN_POINT ( 'NONE',  ( 5.688569873206805738, -2.951204850235011445, 103.9352763293503585 ) ) ;
#10974=SURFACE_STYLE_USAGE ( .BOTH. , #53056 ) ;
#10979=EDGE_CURVE ( 'NONE', #93333, #46770, #69685, .T. ) ;
#10987=FACE_OUTER_BOUND ( 'NONE', #35433, .T. ) ;
#11006=CARTESIAN_POINT ( 'NONE',  ( 1.339715621834636883, -50.03010211448981437, 40.96304831423880444 ) ) ;
#11053=ORIENTED_EDGE ( 'NONE', *, *, #11537, .F. ) ;
#11094=CARTESIAN_POINT ( 'NONE',  ( -13.64640293162734785, -56.64148551553003585, 30.13230102324352799 ) ) ;
#11097=CARTESIAN_POINT ( 'NONE',  ( 12.35731595739100186, -3.034588722688706941, 20.66425384906944274 ) ) ;
#11109=VERTEX_POINT ( 'NONE', #10209 ) ;
#11137=SURFACE_STYLE_FILL_AREA ( #365 ) ;
#11151=VECTOR ( 'NONE', #93345, 1000.000000000000000 ) ;
#11155=CARTESIAN_POINT ( 'NONE',  ( 4.999999999999999112, -14.11572642558175694, 9.475261081874535307 ) ) ;
#11163=EDGE_CURVE ( 'NONE', #89992, #26896, #106089, .T. ) ;
#11198=ORIENTED_EDGE ( 'NONE', *, *, #103751, .T. ) ;
#11201=CARTESIAN_POINT ( 'NONE',  ( 0.000000000000000000, -1.550510257216834331, 120.5000000000000000 ) ) ;
#11229=CARTESIAN_POINT ( 'NONE',  ( 3.405129524021479615, -48.85126521005803824, 104.5473292663389202 ) ) ;
#11230=CARTESIAN_POINT ( 'NONE',  ( -4.784091155926208039, -14.50372271115726086, -7.881159729540446079 ) ) ;
#11249=CARTESIAN_POINT ( 'NONE',  ( 5.109687690906336677, -13.89725820713331572, -5.663713107265837543 ) ) ;
#11291=( GEOMETRIC_REPRESENTATION_CONTEXT ( 3 ) GLOBAL_UNCERTAINTY_ASSIGNED_CONTEXT ( ( #5156 ) ) GLOBAL_UNIT_ASSIGNED_CONTEXT ( ( #88552, #21719, #5506 ) ) REPRESENTATION_CONTEXT ( 'NONE', 'WORKASPACE' ) );
#11295=SURFACE_STYLE_FILL_AREA ( #101397 ) ;
#11314=( NAMED_UNIT ( * ) PLANE_ANGLE_UNIT ( ) SI_UNIT ( $, .RADIAN. ) );
#11326=ORIENTED_EDGE ( 'NONE', *, *, #85921, .T. ) ;
#11327=SURFACE_STYLE_FILL_AREA ( #12398 ) ;
#11338=VERTEX_POINT ( 'NONE', #87306 ) ;
#11341=CARTESIAN_POINT ( 'NONE',  ( -30.00000000000000000, 0.000000000000000000, 0.000000000000000000 ) ) ;
#11348=CARTESIAN_POINT ( 'NONE',  ( -3.369683342533076331, -0.9132179776671506266, 104.1613013819149387 ) ) ;
#11385=SURFACE_SIDE_STYLE ('',( #27100 ) ) ;
#11389=CARTESIAN_POINT ( 'NONE',  ( -9.125156274357966169, -53.47050611676294096, 31.09081505442903648 ) ) ;
#11402=CARTESIAN_POINT ( 'NONE',  ( -4.440267933150495061, -1.157000248813045085, 104.3849335853022779 ) ) ;
#11455=CARTESIAN_POINT ( 'NONE',  ( 3.534854069000094690, -1.070477528868737371, 104.4405781011824956 ) ) ;
#11470=CARTESIAN_POINT ( 'NONE',  ( 13.99719405338373512, -57.99973887820377172, 27.38482409491458114 ) ) ;
#11497=CARTESIAN_POINT ( 'NONE',  ( 0.000000000000000000, -4.000000000000003553, 112.0000000000000000 ) ) ;
#11504=DIRECTION ( 'NONE',  ( 0.5166563581655553294, 0.4014477553984801550, -0.7562446080816890293 ) ) ;
#11508=AXIS2_PLACEMENT_3D ( 'NONE', #29886, #79463, #62771 ) ;
#11537=EDGE_CURVE ( 'NONE', #88345, #97345, #51629, .T. ) ;
#11539=CARTESIAN_POINT ( 'NONE',  ( 3.816044156919698782, -48.93725730783727812, 40.64983015004354172 ) ) ;
#11560=CARTESIAN_POINT ( 'NONE',  ( -0.7777777777777786783, -54.00000000000000000, 40.97837836547555668 ) ) ;
#11606=DIRECTION ( 'NONE',  ( 0.000000000000000000, 1.000000000000000000, 5.787437586309764365E-15 ) ) ;
#11633=CARTESIAN_POINT ( 'NONE',  ( -13.80732344291479663, -57.17861966895164016, 24.67475631203899411 ) ) ;
#11650=ORIENTED_EDGE ( 'NONE', *, *, #13081, .F. ) ;
#11659=AXIS2_PLACEMENT_3D ( 'NONE', #980, #100779, #8581 ) ;
#11669=CARTESIAN_POINT ( 'NONE',  ( 5.000000000000000000, -14.21727251090713828, 9.320362779989000757 ) ) ;
#11678=( GEOMETRIC_REPRESENTATION_CONTEXT ( 3 ) GLOBAL_UNCERTAINTY_ASSIGNED_CONTEXT ( ( #95573 ) ) GLOBAL_UNIT_ASSIGNED_CONTEXT ( ( #60464, #45329, #85244 ) ) REPRESENTATION_CONTEXT ( 'NONE', 'WORKASPACE' ) );
#11689=CARTESIAN_POINT ( 'NONE',  ( 13.38090213880806978, -54.00000000000000711, 31.11721482942554928 ) ) ;
#11702=CARTESIAN_POINT ( 'NONE',  ( 4.999999999999995559, -46.00000000000000000, 40.07669683062201926 ) ) ;
#11716=ORIENTED_EDGE ( 'NONE', *, *, #81985, .F. ) ;
#11749=ADVANCED_FACE ( 'NONE', ( #49972 ), #39782, .F. ) ;
#11763=CARTESIAN_POINT ( 'NONE',  ( 3.423905177084550555, -49.17202489992536130, 103.8439100969738291 ) ) ;
#11771=MECHANICAL_DESIGN_GEOMETRIC_PRESENTATION_REPRESENTATION('',(#104790),#37625);
#11773=ORIENTED_EDGE ( 'NONE', *, *, #39246, .T. ) ;
#11787=CARTESIAN_POINT ( 'NONE',  ( 7.000000000000000000, -14.05766640829038572, -5.232782735144292374 ) ) ;
#11788=STYLED_ITEM ( 'NONE', ( #16175 ), #31215 ) ;
#11825=CIRCLE ( 'NONE', #80731, 3.999999999999989786 ) ;
#11831=DIRECTION ( 'NONE',  ( 1.000000000000000000, 0.000000000000000000, 0.000000000000000000 ) ) ;
#11838=CARTESIAN_POINT ( 'NONE',  ( -12.83107512063730837, 1.658796432365972739, 14.90858414098761209 ) ) ;
#11844=( GEOMETRIC_REPRESENTATION_CONTEXT ( 3 ) GLOBAL_UNCERTAINTY_ASSIGNED_CONTEXT ( ( #106654 ) ) GLOBAL_UNIT_ASSIGNED_CONTEXT ( ( #61638, #79377, #104179 ) ) REPRESENTATION_CONTEXT ( 'NONE', 'WORKASPACE' ) );
#11869=SURFACE_SIDE_STYLE ('',( #87901 ) ) ;
#11872=B_SPLINE_CURVE_WITH_KNOTS ( 'NONE', 3,
 ( #69816, #28877, #71934, #38529, #63334, #30980, #79493, #103247, #39053, #7185, #21826, #62794, #54665, #47642, #46594, #81074, #71389, #97264, #14743, #80542 ),
 .UNSPECIFIED., .F., .F.,
 ( 4, 2, 2, 2, 2, 2, 2, 2, 2, 4 ),
 ( 0.000000000000000000, 0.001913256305722581480, 0.003826512611445162960, 0.005739768917167741187, 0.007653025222890320715, 0.009566281528612899376, 0.01052290968147418480, 0.01147953783433547197, 0.01339279414005804282, 0.01530605044578061021 ),
 .UNSPECIFIED. ) ;
#11879=CARTESIAN_POINT ( 'NONE',  ( -13.45844644947841751, -53.47274863452597771, 23.14343646736056570 ) ) ;
#11898=CARTESIAN_POINT ( 'NONE',  ( -4.582299834663618121, -65.64808143178194655, 13.11537099594930922 ) ) ;
#11902=FACE_OUTER_BOUND ( 'NONE', #36520, .T. ) ;
#11953=VECTOR ( 'NONE', #98958, 1000.000000000000000 ) ;
#11993=CARTESIAN_POINT ( 'NONE',  ( 3.564365538402894273, -1.135065884989783669, 104.5953911288830085 ) ) ;
#12011=CARTESIAN_POINT ( 'NONE',  ( 13.83893552277105776, -57.46712370362125455, 29.12875707416400317 ) ) ;
#12015=ORIENTED_EDGE ( 'NONE', *, *, #44309, .T. ) ;
#12034=FILL_AREA_STYLE ('',( #68155 ) ) ;
#12035=CARTESIAN_POINT ( 'NONE',  ( -3.707709148200944327, -48.90047616793697927, 104.5934084724859332 ) ) ;
#12058=ORIENTED_EDGE ( 'NONE', *, *, #74691, .F. ) ;
#12059=CARTESIAN_POINT ( 'NONE',  ( -9.521849859704259345, -56.44524181890594150, 23.94093251888962470 ) ) ;
#12073=DIRECTION ( 'NONE',  ( 0.000000000000000000, 0.000000000000000000, 1.000000000000000000 ) ) ;
#12077=CARTESIAN_POINT ( 'NONE',  ( 4.650424936886119021, -47.72263153603915242, 40.40425276227099971 ) ) ;
#12087=CARTESIAN_POINT ( 'NONE',  ( -6.891666673413887896E-15, -70.53271932724189242, 13.00000000000000000 ) ) ;
#12097=CARTESIAN_POINT ( 'NONE',  ( -6.167494924855482452, -50.03135609564296260, 39.57077639986113837 ) ) ;
#12116=LINE ( 'NONE', #63353, #89903 ) ;
#12129=DIRECTION ( 'NONE',  ( 2.742080092235280244E-17, 0.000000000000000000, -1.000000000000000000 ) ) ;
#12168=CARTESIAN_POINT ( 'NONE',  ( -5.833333333333327708, -46.27176886455112026, 103.8776713793258324 ) ) ;
#12169=CARTESIAN_POINT ( 'NONE',  ( -13.38090213880806978, -54.26192864245579273, 31.11721482942555639 ) ) ;
#12192=CARTESIAN_POINT ( 'NONE',  ( -1.141441439215143294, -70.08722353079659229, 13.04506332611827801 ) ) ;
#12241=CARTESIAN_POINT ( 'NONE',  ( -0.3425297379985101087, -69.52592981242614201, 12.72818415379369483 ) ) ;
#12254=VERTEX_POINT ( 'NONE', #106483 ) ;
#12269=ORIENTED_EDGE ( 'NONE', *, *, #105637, .F. ) ;
#12295=DIRECTION ( 'NONE',  ( -1.000000000000000000, 0.000000000000000000, 0.000000000000000000 ) ) ;
#12297=CARTESIAN_POINT ( 'NONE',  ( -9.389245980427300964, -2.447416405268211914, 14.81682632889905626 ) ) ;
#12301=FACE_OUTER_BOUND ( 'NONE', #79769, .T. ) ;
#12305=ADVANCED_FACE ( 'NONE', ( #88729 ), #55266, .T. ) ;
#12325=EDGE_CURVE ( 'NONE', #18508, #101939, #17224, .T. ) ;
#12328=CARTESIAN_POINT ( 'NONE',  ( -3.857142857142845660, -48.79941684889506348, 103.1763305333244176 ) ) ;
#12349=CARTESIAN_POINT ( 'NONE',  ( 0.000000000000000000, -54.00000000000000711, 27.00000000000000000 ) ) ;
#12356=CARTESIAN_POINT ( 'NONE',  ( 2.893255198029386133, -0.4647462895689700169, 103.3592142771323665 ) ) ;
#12369=CARTESIAN_POINT ( 'NONE',  ( -15.66846091137126606, -1.219547918084784133, 14.95212397148377548 ) ) ;
#12394=CARTESIAN_POINT ( 'NONE',  ( -5.000000000000000000, -13.90268927672064336, 9.980021953238050969 ) ) ;
#12398=FILL_AREA_STYLE ('',( #78210 ) ) ;
#12405=( GEOMETRIC_REPRESENTATION_CONTEXT ( 3 ) GLOBAL_UNCERTAINTY_ASSIGNED_CONTEXT ( ( #75317 ) ) GLOBAL_UNIT_ASSIGNED_CONTEXT ( ( #36232, #44829, #42681 ) ) REPRESENTATION_CONTEXT ( 'NONE', 'WORKASPACE' ) );
#12416=ORIENTED_EDGE ( 'NONE', *, *, #3193, .T. ) ;
#12446=CARTESIAN_POINT ( 'NONE',  ( 5.000000000000000000, -23.50449067138091053, -3.099878936449560474 ) ) ;
#12448=COLOUR_RGB ( '', 0.72549020, 0.75294118, 0.79215686) ;
#12458=DIRECTION ( 'NONE',  ( 1.000000000000000000, -0.000000000000000000, 1.224646799147353207E-16 ) ) ;
#12484=ADVANCED_FACE ( 'NONE', ( #66568, #99451 ), #58487, .F. ) ;
#12499=EDGE_LOOP ( 'NONE', ( #7798, #94264, #85795, #56602 ) ) ;
#12550=( NAMED_UNIT ( * ) SI_UNIT ( $, .STERADIAN. ) SOLID_ANGLE_UNIT ( ) );
#12557=CARTESIAN_POINT ( 'NONE',  ( 4.792515968931314596, -2.702239074782193384, 102.4138677444059766 ) ) ;
#12560=CARTESIAN_POINT ( 'NONE',  ( -3.459690225512181083, -48.89101625908396187, 104.5059395991341376 ) ) ;
#12600=CARTESIAN_POINT ( 'NONE',  ( 4.781207304706819983, -47.39297744640040122, 40.35843253569867528 ) ) ;
#12613=CARTESIAN_POINT ( 'NONE',  ( -1.000000000000000000, -68.32597503900204572, 12.04364623808024781 ) ) ;
#12620=CARTESIAN_POINT ( 'NONE',  ( -1.921192241758119978, -49.89471155215800735, 44.77608010490040158 ) ) ;
#12631=STYLED_ITEM ( 'NONE', ( #17257 ), #21310 ) ;
#12643=AXIS2_PLACEMENT_3D ( 'NONE', #102297, #78546, #4143 ) ;
#12654=SURFACE_SIDE_STYLE ('',( #30470 ) ) ;
#12665=ORIENTED_EDGE ( 'NONE', *, *, #50931, .T. ) ;
#12696=CARTESIAN_POINT ( 'NONE',  ( -13.38905016575103168, -54.52753545736232610, 31.09099597011418226 ) ) ;
#12721=SURFACE_STYLE_FILL_AREA ( #21917 ) ;
#12742=( LENGTH_UNIT ( ) NAMED_UNIT ( * ) SI_UNIT ( .MILLI., .METRE. ) );
#12768=( NAMED_UNIT ( * ) PLANE_ANGLE_UNIT ( ) SI_UNIT ( $, .RADIAN. ) );
#12775=CARTESIAN_POINT ( 'NONE',  ( -2.691542343445430419, -49.46338946410779869, 103.4273627254628423 ) ) ;
#12788=DIRECTION ( 'NONE',  ( 0.000000000000000000, 1.000000000000000000, 0.000000000000000000 ) ) ;
#12799=AXIS2_PLACEMENT_3D ( 'NONE', #46454, #29771, #69671 ) ;
#12824=CARTESIAN_POINT ( 'NONE',  ( 3.454253436624922902, -49.15858197120396511, 103.7259032015043090 ) ) ;
#12832=ORIENTED_EDGE ( 'NONE', *, *, #10656, .T. ) ;
#12840=VERTEX_POINT ( 'NONE', #71217 ) ;
#12847=STYLED_ITEM ( 'NONE', ( #98260 ), #27947 ) ;
#12868=VERTEX_POINT ( 'NONE', #80358 ) ;
#12873=SURFACE_SIDE_STYLE ('',( #88384 ) ) ;
#12880=AXIS2_PLACEMENT_3D ( 'NONE', #48816, #56912, #99500 ) ;
#12883=FILL_AREA_STYLE_COLOUR ( '', #1410 ) ;
#12893=CARTESIAN_POINT ( 'NONE',  ( -15.00905689107410090, -0.1007854530124032977, 15.00123387746082315 ) ) ;
#12921=ORIENTED_EDGE ( 'NONE', *, *, #24339, .F. ) ;
#12925=CARTESIAN_POINT ( 'NONE',  ( -4.933275777332625012, -67.91368662472184781, 13.89515823646121184 ) ) ;
#12928=PRESENTATION_STYLE_ASSIGNMENT (( #96528 ) ) ;
#13014=CARTESIAN_POINT ( 'NONE',  ( 27.99999999999999645, 1.347111479062088405E-15, 11.00000000000000000 ) ) ;
#13017=ORIENTED_EDGE ( 'NONE', *, *, #103803, .F. ) ;
#13068=CARTESIAN_POINT ( 'NONE',  ( -7.000000000000000000, -4.000000000000003553, 39.12435565298213902 ) ) ;
#13072=AXIS2_PLACEMENT_3D ( 'NONE', #15331, #57368, #90287 ) ;
#13078=CARTESIAN_POINT ( 'NONE',  ( 5.000000000000000000, -46.95251766935337656, 6.320350040254264279 ) ) ;
#13081=EDGE_CURVE ( 'NONE', #21120, #3985, #62856, .T. ) ;
#13091=ADVANCED_FACE ( 'NONE', ( #13247 ), #9238, .F. ) ;
#13123=( NAMED_UNIT ( * ) SI_UNIT ( $, .STERADIAN. ) SOLID_ANGLE_UNIT ( ) );
#13150=CARTESIAN_POINT ( 'NONE',  ( -4.578626833785902406, -52.33922769183001833, 40.23114928973193827 ) ) ;
#13164=EDGE_CURVE ( 'NONE', #34686, #82136, #2904, .T. ) ;
#13165=DIRECTION ( 'NONE',  ( -0.000000000000000000, -1.000000000000000000, -0.000000000000000000 ) ) ;
#13177=EDGE_CURVE ( 'NONE', #41710, #99036, #81741, .T. ) ;
#13231=CARTESIAN_POINT ( 'NONE',  ( -27.99999999999999645, 0.000000000000000000, 0.000000000000000000 ) ) ;
#13242=EDGE_LOOP ( 'NONE', ( #45662, #88612, #1277, #40669 ) ) ;
#13247=FACE_OUTER_BOUND ( 'NONE', #94606, .T. ) ;
#13279=CARTESIAN_POINT ( 'NONE',  ( 14.00172459590632457, -49.99988873354983809, 26.85642925593120722 ) ) ;
#13287=EDGE_CURVE ( 'NONE', #93762, #65995, #76601, .T. ) ;
#13308=CARTESIAN_POINT ( 'NONE',  ( 5.088838845617632778, -61.74461508817817901, 13.90681500082671462 ) ) ;
#13339=COLOUR_RGB ( '', 0.66274510, 0.83137255, 0.94901961) ;
#13348=CARTESIAN_POINT ( 'NONE',  ( -15.26380556289074697, -5.957643091172989180, 13.77816202113101163 ) ) ;
#13349=COLOUR_RGB ( '', 0.72549020, 0.75294118, 0.79215686) ;
#13402=ADVANCED_FACE ( 'NONE', ( #101764 ), #36548, .T. ) ;
#13410=CARTESIAN_POINT ( 'NONE',  ( 3.214365674771622938, -1.015224780326832832, 104.3190434908430859 ) ) ;
#13413=CYLINDRICAL_SURFACE ( 'NONE', #49988, 4.000000000000000000 ) ;
#13421=AXIS2_PLACEMENT_3D ( 'NONE', #18910, #50671, #18360 ) ;
#13423=CARTESIAN_POINT ( 'NONE',  ( -10.15372854770908617, -0.7067373757843724569, 20.10246628052868090 ) ) ;
#13434=ORIENTED_EDGE ( 'NONE', *, *, #83418, .F. ) ;
#13456=VECTOR ( 'NONE', #18798, 1000.000000000000000 ) ;
#13462=CARTESIAN_POINT ( 'NONE',  ( -14.00175760317098117, -49.99974274319190926, 26.85746939222903151 ) ) ;
#13479=CARTESIAN_POINT ( 'NONE',  ( -3.855727343237526750, -67.78910435866291095, 13.12451945574045453 ) ) ;
#13518=CARTESIAN_POINT ( 'NONE',  ( 0.000000000000000000, 0.000000000000000000, 112.0000000000000000 ) ) ;
#13526=ADVANCED_FACE ( 'NONE', ( #75626 ), #38820, .T. ) ;
#13544=CARTESIAN_POINT ( 'NONE',  ( -1.000000000000000000, -40.36500490292975485, -0.7636728796494194338 ) ) ;
#13568=( LENGTH_UNIT ( ) NAMED_UNIT ( * ) SI_UNIT ( .MILLI., .METRE. ) );
#13583=CARTESIAN_POINT ( 'NONE',  ( -1.459252261598892542, -6.102732174931079889, -13.75226092436777137 ) ) ;
#13587=AXIS2_PLACEMENT_3D ( 'NONE', #98573, #106663, #7428 ) ;
#13597=CARTESIAN_POINT ( 'NONE',  ( 13.53380759260212329, -56.00905799123083284, 30.58586009444553611 ) ) ;
#13610=CARTESIAN_POINT ( 'NONE',  ( 5.000000000000000000, -57.62779005937431265, 11.09695692297539971 ) ) ;
#13612=CARTESIAN_POINT ( 'NONE',  ( -30.00000000000000000, -54.00000000000000711, 27.11721482942554928 ) ) ;
#13645=VERTEX_POINT ( 'NONE', #20649 ) ;
#13686=CARTESIAN_POINT ( 'NONE',  ( -2.210743487168307375, -53.78942310434221241, 40.82584008148600674 ) ) ;
#13704=SURFACE_SIDE_STYLE ('',( #87621 ) ) ;
#13717=LINE ( 'NONE', #95197, #4621 ) ;
#13762=( NAMED_UNIT ( * ) SI_UNIT ( $, .STERADIAN. ) SOLID_ANGLE_UNIT ( ) );
#13774=DIRECTION ( 'NONE',  ( 1.224646799147352468E-16, 0.000000000000000000, -1.000000000000000000 ) ) ;
#13813=CARTESIAN_POINT ( 'NONE',  ( 13.56225034990342948, -52.22121833032962002, 23.52491571494838851 ) ) ;
#13829=DIRECTION ( 'NONE',  ( 1.000000000000000000, 0.000000000000000000, 0.000000000000000000 ) ) ;
#13830=FILL_AREA_STYLE ('',( #47262 ) ) ;
#13852=EDGE_CURVE ( 'NONE', #50280, #74417, #90228, .T. ) ;
#13864=CARTESIAN_POINT ( 'NONE',  ( 4.999999999999959144, -12.50629439489329364, 11.30430831584017604 ) ) ;
#13870=FACE_OUTER_BOUND ( 'NONE', #97221, .T. ) ;
#13880=ORIENTED_EDGE ( 'NONE', *, *, #98804, .T. ) ;
#13881=CARTESIAN_POINT ( 'NONE',  ( -15.71446116343726906, -4.300810710832455364, 14.38220008862084143 ) ) ;
#13919=ORIENTED_EDGE ( 'NONE', *, *, #14896, .T. ) ;
#13922=COLOUR_RGB ( '', 0.09019608, 0.27058824, 0.51372549) ;
#13923=DIRECTION ( 'NONE',  ( 0.000000000000000000, -1.000000000000000000, 0.000000000000000000 ) ) ;
#13931=FILL_AREA_STYLE ('',( #35070 ) ) ;
#13938=( BOUNDED_SURFACE ( )  B_SPLINE_SURFACE ( 3, 2, ( 
 ( #77642, #71130, #103502 ),
 ( #45803, #28589, #3220 ),
 ( #86285, #37208, #36691 ),
 ( #37749, #60936, #19979 ),
 ( #87334, #101905, #5350 ),
 ( #78680, #62009, #70077 ),
 ( #85751, #12356, #78161 ),
 ( #69554, #102978, #52824 ),
 ( #13410, #94902, #21043 ),
 ( #29654, #104022, #38271 ) ),
 .UNSPECIFIED., .F., .F., .F. ) 
 B_SPLINE_SURFACE_WITH_KNOTS ( ( 4, 2, 2, 2, 4 ),
 ( 3, 3 ),
 ( -1.185673698477823590E-05, 0.001059589481406208620, 0.002131035699797195326, 0.003202481918188181814, 0.004273928136579168736 ),
 ( 0.000000000000000000, 1.000000000000000000 ),
 .UNSPECIFIED. ) 
 GEOMETRIC_REPRESENTATION_ITEM ( )  RATIONAL_B_SPLINE_SURFACE ( (
 ( 1.000000000000000000, 1.000000000000000000, 1.000000000000000000),
 ( 1.000000000000000000, 0.9999922502423259640, 1.000000000000000000),
 ( 1.000000000000000000, 0.9961090584666545400, 1.000000000000000000),
 ( 1.000000000000000000, 0.9800114100223529245, 1.000000000000000000),
 ( 1.000000000000000000, 0.9677016975217730410, 1.000000000000000000),
 ( 1.000000000000000000, 0.9345728642048093393, 1.000000000000000000),
 ( 1.000000000000000000, 0.9137480076086517133, 1.000000000000000000),
 ( 1.000000000000000000, 0.8628371017894029826, 1.000000000000000000),
 ( 1.000000000000000000, 0.8327438998405827242, 1.000000000000000000),
 ( 1.000000000000000000, 0.7973879088788905500, 1.000000000000000000) ) ) 
 REPRESENTATION_ITEM ( '' )  SURFACE ( )  );
#13943=( GEOMETRIC_REPRESENTATION_CONTEXT ( 3 ) GLOBAL_UNCERTAINTY_ASSIGNED_CONTEXT ( ( #85020 ) ) GLOBAL_UNIT_ASSIGNED_CONTEXT ( ( #62566, #37256, #29694 ) ) REPRESENTATION_CONTEXT ( 'NONE', 'WORKASPACE' ) );
#13956=CARTESIAN_POINT ( 'NONE',  ( -7.852494914944515791, -0.7890738855012446873, 15.46605827214583329 ) ) ;
#13971=CARTESIAN_POINT ( 'NONE',  ( -3.568931636294713439, -49.06947573042521071, 103.4741166605240323 ) ) ;
#13983=SURFACE_STYLE_USAGE ( .BOTH. , #11869 ) ;
#13992=CARTESIAN_POINT ( 'NONE',  ( -13.59366797464709720, -51.99143461894139762, 23.64820470065338753 ) ) ;
#14010=UNCERTAINTY_MEASURE_WITH_UNIT (LENGTH_MEASURE( 1.000000000000000082E-05 ), #80653, 'distance_accuracy_value', 'NONE');
#14014=CARTESIAN_POINT ( 'NONE',  ( 4.506266729858585229, -48.81716041225653413, 104.3949571352749643 ) ) ;
#14047=CARTESIAN_POINT ( 'NONE',  ( -9.204611235795193025, -52.70218221418006976, 30.90985867601607850 ) ) ;
#14069=CARTESIAN_POINT ( 'NONE',  ( -1.000000000000000000, -51.24344465336813670, 3.816021516725665030 ) ) ;
#14105=SURFACE_STYLE_USAGE ( .BOTH. , #87498 ) ;
#14109=AXIS2_PLACEMENT_3D ( 'NONE', #65140, #40862, #7955 ) ;
#14139=FILL_AREA_STYLE_COLOUR ( '', #8139 ) ;
#14149=ORIENTED_EDGE ( 'NONE', *, *, #59589, .T. ) ;
#14160=CARTESIAN_POINT ( 'NONE',  ( -4.717378471607711177, -47.48249719118609846, 42.90183931269586992 ) ) ;
#14198=TOROIDAL_SURFACE ( 'NONE', #102053, 11.00000000000000533, 4.000000000000000000 ) ;
#14214=CARTESIAN_POINT ( 'NONE',  ( -4.973615039726302811, -46.53039117003746838, 42.61927381063142661 ) ) ;
#14235=VERTEX_POINT ( 'NONE', #99907 ) ;
#14260=EDGE_LOOP ( 'NONE', ( #66622, #88050, #79197, #97584 ) ) ;
#14279=CARTESIAN_POINT ( 'NONE',  ( 0.9999999999999940048, -50.00000000000000000, 101.0455488498966758 ) ) ;
#14282=ORIENTED_EDGE ( 'NONE', *, *, #5400, .T. ) ;
#14358=CARTESIAN_POINT ( 'NONE',  ( 6.125000000000000000, -60.71953810597977252, 14.41094225130410855 ) ) ;
#14364=CARTESIAN_POINT ( 'NONE',  ( 0.000000000000000000, -80.00000000000000000, 37.00000000000000000 ) ) ;
#14366=EDGE_CURVE ( 'NONE', #89992, #15547, #20549, .T. ) ;
#14376=CARTESIAN_POINT ( 'NONE',  ( -4.464768147782833374, -1.996984918325826586, 102.6740199126133888 ) ) ;
#14397=CARTESIAN_POINT ( 'NONE',  ( 5.823303048885946964, -64.88595876702598275, 14.26806532518525472 ) ) ;
#14405=CARTESIAN_POINT ( 'NONE',  ( -8.654235699476732435, -14.00093397087661629, 15.99236324148348487 ) ) ;
#14415=CARTESIAN_POINT ( 'NONE',  ( -27.99999999999999645, 0.000000000000000000, 0.000000000000000000 ) ) ;
#14482=EDGE_CURVE ( 'NONE', #81100, #26896, #83511, .T. ) ;
#14502=EDGE_CURVE ( 'NONE', #214, #82136, #21754, .T. ) ;
#14505=CARTESIAN_POINT ( 'NONE',  ( -5.000000000000000000, -14.24437098773013055, 11.98245615812826870 ) ) ;
#14541=UNCERTAINTY_MEASURE_WITH_UNIT (LENGTH_MEASURE( 1.000000000000000082E-05 ), #65980, 'distance_accuracy_value', 'NONE');
#14560=( GEOMETRIC_REPRESENTATION_CONTEXT ( 3 ) GLOBAL_UNCERTAINTY_ASSIGNED_CONTEXT ( ( #42968 ) ) GLOBAL_UNIT_ASSIGNED_CONTEXT ( ( #6246, #65027, #106003 ) ) REPRESENTATION_CONTEXT ( 'NONE', 'WORKASPACE' ) );
#14573=CARTESIAN_POINT ( 'NONE',  ( -9.668268460383899310, -50.82497190099731199, 29.56382476086920974 ) ) ;
#14574=DIRECTION ( 'NONE',  ( -0.000000000000000000, -1.000000000000000000, -0.000000000000000000 ) ) ;
#14595=CARTESIAN_POINT ( 'NONE',  ( -4.970849588242775674, -46.55209929711412542, 102.2755693391596594 ) ) ;
#14610=DIRECTION ( 'NONE',  ( 0.000000000000000000, 0.000000000000000000, 1.000000000000000000 ) ) ;
#14619=CARTESIAN_POINT ( 'NONE',  ( -2.807206530941650957, -0.4217707022279503781, 102.9378052260346834 ) ) ;
#14621=UNCERTAINTY_MEASURE_WITH_UNIT (LENGTH_MEASURE( 1.000000000000000082E-05 ), #9866, 'distance_accuracy_value', 'NONE');
#14624=CARTESIAN_POINT ( 'NONE',  ( -13.64050477809429829, 1.160452971590898885, 14.95551770859069585 ) ) ;
#14634=ADVANCED_FACE ( 'NONE', ( #13870 ), #106651, .F. ) ;
#14648=ORIENTED_EDGE ( 'NONE', *, *, #5591, .T. ) ;
#14659=CARTESIAN_POINT ( 'NONE',  ( 9.125156274357966169, -54.52949388323710878, 31.09081505442903648 ) ) ;
#14661=CARTESIAN_POINT ( 'NONE',  ( 6.125000000000095923, -15.62228920881129390, 14.41094225130415651 ) ) ;
#14663=CARTESIAN_POINT ( 'NONE',  ( 5.000000000000000000, -66.75027687118438280, 15.74257363030519663 ) ) ;
#14665=CARTESIAN_POINT ( 'NONE',  ( 7.554474191401430616, -6.015471045889135837, 14.04826599594835557 ) ) ;
#14703=CARTESIAN_POINT ( 'NONE',  ( -9.819569948016248162, -57.58692256219968897, 28.90708029074982477 ) ) ;
#14713=CARTESIAN_POINT ( 'NONE',  ( 4.382959417677087188, -1.862050784382271562, 102.7400018439556391 ) ) ;
#14733=EDGE_LOOP ( 'NONE', ( #106732, #79210, #63158, #7266, #10188, #46390 ) ) ;
#14737=CARTESIAN_POINT ( 'NONE',  ( -1.000000000000000222, -5.000000000000000000, -14.14213562373095101 ) ) ;
#14743=CARTESIAN_POINT ( 'NONE',  ( -6.662856812433364695, -15.38938976169041695, 14.67262768018345298 ) ) ;
#14810=CARTESIAN_POINT ( 'NONE',  ( -6.891666673413887896E-15, -70.53271932724189242, 13.00000000000000000 ) ) ;
#14820=CARTESIAN_POINT ( 'NONE',  ( 14.31968076504620946, 0.6252655212105243665, 14.98772011519035630 ) ) ;
#14846=CARTESIAN_POINT ( 'NONE',  ( -6.125000000000000000, -60.71953810597580059, 14.41094225130411033 ) ) ;
#14857=AXIS2_PLACEMENT_3D ( 'NONE', #15682, #7721, #14610 ) ;
#14881=CARTESIAN_POINT ( 'NONE',  ( 15.66820627147619582, -1.212563469572859987, 14.95337489854003898 ) ) ;
#14896=EDGE_CURVE ( 'NONE', #550, #67342, #45823, .T. ) ;
#14913=CARTESIAN_POINT ( 'NONE',  ( 5.371950044183567030, -2.205168805904308194, 104.0625755208173331 ) ) ;
#14915=CARTESIAN_POINT ( 'NONE',  ( -4.980618096941614503, -3.539029780453323948, 103.2912570477108716 ) ) ;
#14946=CARTESIAN_POINT ( 'NONE',  ( 4.348929473936380852, -48.21591736632261416, 103.6864098602935655 ) ) ;
#14951=COLOUR_RGB ( '', 0.31764706, 0.68627451, 0.89019608) ;
#14960=CARTESIAN_POINT ( 'NONE',  ( -5.140510257140494588, -10.64770037776033185, -10.57912409963173772 ) ) ;
#14973=CARTESIAN_POINT ( 'NONE',  ( 27.99999999999999645, 1.836970198721029589E-15, -15.00000000000000000 ) ) ;
#14983=CARTESIAN_POINT ( 'NONE',  ( 0.000000000000000000, 0.000000000000000000, 0.000000000000000000 ) ) ;
#14986=UNCERTAINTY_MEASURE_WITH_UNIT (LENGTH_MEASURE( 1.000000000000000082E-05 ), #40075, 'distance_accuracy_value', 'NONE');
#14994=COLOUR_RGB ( '', 0.66274510, 0.83137255, 0.94901961) ;
#14999=SURFACE_SIDE_STYLE ('',( #96994 ) ) ;
#15005=MECHANICAL_DESIGN_GEOMETRIC_PRESENTATION_REPRESENTATION('',(#30525),#71820);
#15034=CARTESIAN_POINT ( 'NONE',  ( 30.00000000000000000, 1.102182119232617714E-15, -9.000000000000000000 ) ) ;
#15049=CARTESIAN_POINT ( 'NONE',  ( -6.038222094116281191, -12.57840291894124363, 12.65816746961276706 ) ) ;
#15053=FILL_AREA_STYLE ('',( #38826 ) ) ;
#15057=CARTESIAN_POINT ( 'NONE',  ( 1.450851314122095559, -49.97609955501174284, 101.4859915538870609 ) ) ;
#15177=ORIENTED_EDGE ( 'NONE', *, *, #1284, .F. ) ;
#15194=CARTESIAN_POINT ( 'NONE',  ( 13.69909788704105935, -56.64682055396593796, 24.10694589033532154 ) ) ;
#15206=CARTESIAN_POINT ( 'NONE',  ( -3.685905252136130184, -1.041089327947677834, 104.2837900504744510 ) ) ;
#15213=CARTESIAN_POINT ( 'NONE',  ( 14.85285428659677720, -6.992436857781551218, 13.28281651405465702 ) ) ;
#15217=ORIENTED_EDGE ( 'NONE', *, *, #61643, .T. ) ;
#15247=CARTESIAN_POINT ( 'NONE',  ( -9.171181789971550202, -55.04814173952514977, 30.98656384792473162 ) ) ;
#15259=ADVANCED_FACE ( 'NONE', ( #16363 ), #57339, .T. ) ;
#15290=CARTESIAN_POINT ( 'NONE',  ( -4.587653515170670104, -47.78786149309958375, 43.03795885842958313 ) ) ;
#15314=CARTESIAN_POINT ( 'NONE',  ( -5.833333333333327708, -3.728231135448884181, 103.8776713793258750 ) ) ;
#15331=CARTESIAN_POINT ( 'NONE',  ( 0.000000000000000000, -48.79941684889506348, 112.0000000000000000 ) ) ;
#15352=MECHANICAL_DESIGN_GEOMETRIC_PRESENTATION_REPRESENTATION('',(#53244),#80644);
#15354=ORIENTED_EDGE ( 'NONE', *, *, #98244, .F. ) ;
#15367=CARTESIAN_POINT ( 'NONE',  ( 30.00000000000000000, 1.714505518806294441E-15, 13.00000000000000000 ) ) ;
#15378=CARTESIAN_POINT ( 'NONE',  ( -5.005299804888146298, -64.88413123474070687, 13.89682420523173079 ) ) ;
#15379=COLOUR_RGB ( '', 0.08235294, 0.09019608, 0.10196078) ;
#15384=ORIENTED_EDGE ( 'NONE', *, *, #19855, .F. ) ;
#15398=ORIENTED_EDGE ( 'NONE', *, *, #71955, .F. ) ;
#15399=VECTOR ( 'NONE', #15987, 1000.000000000000000 ) ;
#15432=CARTESIAN_POINT ( 'NONE',  ( 11.70799159436998593, -8.253155071789681330, 19.32017322931982051 ) ) ;
#15451=CARTESIAN_POINT ( 'NONE',  ( 4.147930821993710993, -1.050632865739543620, 104.5115743862824615 ) ) ;
#15462=FACE_OUTER_BOUND ( 'NONE', #80128, .T. ) ;
#15484=CARTESIAN_POINT ( 'NONE',  ( -4.999999999997973177, -61.61794147117323206, 12.73961838306073879 ) ) ;
#15490=CARTESIAN_POINT ( 'NONE',  ( 4.680975426248633831, -47.58422982932144407, 103.4780497728483368 ) ) ;
#15493=LINE ( 'NONE', #63535, #102485 ) ;
#15526=AXIS2_PLACEMENT_3D ( 'NONE', #29268, #93439, #4413 ) ;
#15527=ADVANCED_FACE ( 'NONE', ( #60049 ), #85636, .T. ) ;
#15547=VERTEX_POINT ( 'NONE', #29811 ) ;
#15558=CARTESIAN_POINT ( 'NONE',  ( -5.385673916453012744, -3.469446951953614189E-15, 18.57417562100670949 ) ) ;
#15585=CARTESIAN_POINT ( 'NONE',  ( -4.999999999999997335, -12.50629439490131389, 11.30430831583516316 ) ) ;
#15593=DIRECTION ( 'NONE',  ( 0.1108331996454379326, -0.9715652913456128692, -0.2092292678113387983 ) ) ;
#15626=CARTESIAN_POINT ( 'NONE',  ( 1.347111479062088207E-15, -1.734723475976807094E-15, 100.9999999999999858 ) ) ;
#15633=CARTESIAN_POINT ( 'NONE',  ( 4.971339166421698152, -62.51181963379390538, 12.85213906502154835 ) ) ;
#15642=CARTESIAN_POINT ( 'NONE',  ( 9.996020202094923590, -50.00033894567218340, 27.38654800878193996 ) ) ;
#15649=DIRECTION ( 'NONE',  ( 0.000000000000000000, 0.000000000000000000, 1.000000000000000000 ) ) ;
#15663=FACE_OUTER_BOUND ( 'NONE', #81796, .T. ) ;
#15682=CARTESIAN_POINT ( 'NONE',  ( 0.000000000000000000, -4.000000000000003553, 112.0000000000000000 ) ) ;
#15691=( BOUNDED_SURFACE ( )  B_SPLINE_SURFACE ( 3, 2, ( 
 ( #47839, #8457, #48900 ),
 ( #6861, #97457, #41357 ),
 ( #74251, #14946, #58066 ),
 ( #98001, #25212, #89396 ),
 ( #89913, #82349, #81795 ),
 ( #7920, #15490, #327 ),
 ( #24154, #90989, #23614 ),
 ( #33291, #40824, #66162 ),
 ( #81272, #7384, #57525 ),
 ( #99044, #33831, #17100 ),
 ( #73716, #49976, #82884 ),
 ( #106076, #106619, #41886 ) ),
 .UNSPECIFIED., .F., .F., .F. ) 
 B_SPLINE_SURFACE_WITH_KNOTS ( ( 4, 2, 2, 2, 2, 4 ),
 ( 3, 3 ),
 ( 1.734723475976807094E-18, 0.001187588843296134801, 0.001781383264944201225, 0.002375177686592267867, 0.003562766529888400716, 0.004750355373184533998 ),
 ( 0.000000000000000000, 1.000000000000000000 ),
 .UNSPECIFIED. ) 
 GEOMETRIC_REPRESENTATION_ITEM ( )  RATIONAL_B_SPLINE_SURFACE ( (
 ( 1.000000000000000000, 0.9359444767143318966, 1.000000000000000000),
 ( 1.000000000000000000, 0.9295581727144621720, 1.000000000000000000),
 ( 1.000000000000000000, 0.9234593375674586824, 1.000000000000000000),
 ( 1.000000000000000000, 0.9150808072273581839, 1.000000000000000000),
 ( 1.000000000000000000, 0.9124161408737813117, 1.000000000000000000),
 ( 1.000000000000000000, 0.9074047588826391619, 1.000000000000000000),
 ( 1.000000000000000000, 0.9050663310860130872, 1.000000000000000000),
 ( 1.000000000000000000, 0.8987692007139450601, 1.000000000000000000),
 ( 1.000000000000000000, 0.8954627112850828130, 1.000000000000000000),
 ( 1.000000000000000000, 0.8909338199771041911, 1.000000000000000000),
 ( 1.000000000000000000, 0.8897377579433939365, 1.000000000000000000),
 ( 1.000000000000000000, 0.8897565210026093796, 1.000000000000000000) ) ) 
 REPRESENTATION_ITEM ( '' )  SURFACE ( )  );
#15707=STYLED_ITEM ( 'NONE', ( #5495 ), #7868 ) ;
#15740=( LENGTH_UNIT ( ) NAMED_UNIT ( * ) SI_UNIT ( .MILLI., .METRE. ) );
#15747=CARTESIAN_POINT ( 'NONE',  ( 12.22086015683302129, -5.459618031741397814, 20.16641550308944630 ) ) ;
#15752=( LENGTH_UNIT ( ) NAMED_UNIT ( * ) SI_UNIT ( .MILLI., .METRE. ) );
#15754=MECHANICAL_DESIGN_GEOMETRIC_PRESENTATION_REPRESENTATION('',(#74333),#38199);
#15787=EDGE_CURVE ( 'NONE', #85444, #17070, #47396, .T. ) ;
#15808=AXIS2_PLACEMENT_3D ( 'NONE', #62787, #88643, #95676 ) ;
#15853=ADVANCED_FACE ( 'NONE', ( #93325 ), #27259, .F. ) ;
#15876=MECHANICAL_DESIGN_GEOMETRIC_PRESENTATION_REPRESENTATION('',(#57193),#22841);
#15891=DIRECTION ( 'NONE',  ( 0.000000000000000000, 0.000000000000000000, 1.000000000000000000 ) ) ;
#15896=ORIENTED_EDGE ( 'NONE', *, *, #25905, .F. ) ;
#15899=DIRECTION ( 'NONE',  ( 0.000000000000000000, 0.000000000000000000, 1.000000000000000000 ) ) ;
#15910=CIRCLE ( 'NONE', #76179, 9.999999999999998224 ) ;
#15912=CARTESIAN_POINT ( 'NONE',  ( -4.006803414943380659, -67.50235953894106444, 13.13861293866451696 ) ) ;
#15917=EDGE_CURVE ( 'NONE', #62818, #87124, #103944, .T. ) ;
#15922=CYLINDRICAL_SURFACE ( 'NONE', #42096, 15.00000000000000000 ) ;
#15928=CARTESIAN_POINT ( 'NONE',  ( 6.957858546966888547, -47.06965355536787854, 39.14895102431469098 ) ) ;
#15959=PRODUCT_DEFINITION ( 'UNKNOWN', '', #833, #67234 ) ;
#15968=CARTESIAN_POINT ( 'NONE',  ( 10.52478704574295776, -11.52214087695234568, 17.76063389341357279 ) ) ;
#15971=STYLED_ITEM ( 'NONE', ( #54925 ), #96092 ) ;
#15973=CARTESIAN_POINT ( 'NONE',  ( 1.354611299910297717, -70.11838715117606569, 13.05944322661130919 ) ) ;
#15980=CARTESIAN_POINT ( 'NONE',  ( 4.382959417677089853, -48.13794921561771645, 102.7400018439556391 ) ) ;
#15987=DIRECTION ( 'NONE',  ( 0.000000000000000000, 1.000000000000000000, 0.000000000000000000 ) ) ;
#16015=CARTESIAN_POINT ( 'NONE',  ( 6.163737169369001734, -12.13805321688063898, 11.84025182891623729 ) ) ;
#16033=CARTESIAN_POINT ( 'NONE',  ( -2.349680750045843425, -6.873796553395948195, -13.34206326735361081 ) ) ;
#16034=( GEOMETRIC_REPRESENTATION_CONTEXT ( 3 ) GLOBAL_UNCERTAINTY_ASSIGNED_CONTEXT ( ( #16964 ) ) GLOBAL_UNIT_ASSIGNED_CONTEXT ( ( #17784, #64730, #56618 ) ) REPRESENTATION_CONTEXT ( 'NONE', 'WORKASPACE' ) );
#16047=CARTESIAN_POINT ( 'NONE',  ( -4.980618096941786810, -46.46097021954794570, 103.2912570477109000 ) ) ;
#16085=FILL_AREA_STYLE_COLOUR ( '', #14994 ) ;
#16092=DIRECTION ( 'NONE',  ( 0.000000000000000000, 1.000000000000000000, 0.000000000000000000 ) ) ;
#16102=FILL_AREA_STYLE ('',( #31778 ) ) ;
#16115=CARTESIAN_POINT ( 'NONE',  ( -5.959015317364962705, -13.75072846948174998, 13.79531249880972510 ) ) ;
#16132=B_SPLINE_CURVE_WITH_KNOTS ( 'NONE', 3,
 ( #48731, #75131, #73007, #64425, #97294, #56285, #74606, #49266 ),
 .UNSPECIFIED., .F., .F.,
 ( 4, 2, 2, 4 ),
 ( -1.267662083608645886E-05, 0.002237097954985276579, 0.003361985242895957748, 0.004486872530806639350 ),
 .UNSPECIFIED. ) ;
#16175=PRESENTATION_STYLE_ASSIGNMENT (( #48531 ) ) ;
#16180=CARTESIAN_POINT ( 'NONE',  ( -9.442659817596066318, -51.55747247252177345, 30.29540378708609794 ) ) ;
#16189=CARTESIAN_POINT ( 'NONE',  ( 4.784092644813104478, -14.50372857256071235, -7.881152805799183092 ) ) ;
#16196=PLANE ( 'NONE',  #103724 ) ;
#16231=CARTESIAN_POINT ( 'NONE',  ( -14.32829664253850765, 0.6308854439496920374, 14.98913826414629824 ) ) ;
#16239=ORIENTED_EDGE ( 'NONE', *, *, #18891, .T. ) ;
#16259=CARTESIAN_POINT ( 'NONE',  ( 13.80753398876933247, -57.17957583240082897, 24.67600335260435074 ) ) ;
#16261=SURFACE_SIDE_STYLE ('',( #73423 ) ) ;
#16268=CARTESIAN_POINT ( 'NONE',  ( 9.521335790331885818, -56.44303812043972357, 23.93938989165062026 ) ) ;
#16275=CARTESIAN_POINT ( 'NONE',  ( 14.61159326615946163, -7.489307139270665381, 13.00852779383240510 ) ) ;
#16281=CARTESIAN_POINT ( 'NONE',  ( -2.067305840858939536, -49.86416495495519285, 102.1177254334556181 ) ) ;
#16304=CARTESIAN_POINT ( 'NONE',  ( -9.336538098104073313, -56.01031256472166575, 30.58506923019146839 ) ) ;
#16322=SURFACE_SIDE_STYLE ('',( #628 ) ) ;
#16342=CARTESIAN_POINT ( 'NONE',  ( -1.000000000000000222, -32.36379547066005813, -3.982563152095341952 ) ) ;
#16362=( NAMED_UNIT ( * ) SI_UNIT ( $, .STERADIAN. ) SOLID_ANGLE_UNIT ( ) );
#16363=FACE_OUTER_BOUND ( 'NONE', #44200, .T. ) ;
#16394=COLOUR_RGB ( '', 0.09019608, 0.27058824, 0.51372549) ;
#16407=CARTESIAN_POINT ( 'NONE',  ( -6.999999999999999112, -14.05766640829038394, -5.232782735144285269 ) ) ;
#16417=SURFACE_STYLE_FILL_AREA ( #90309 ) ;
#16428=CARTESIAN_POINT ( 'NONE',  ( -15.10151546872593187, -0.2204499704438013796, 15.00000000000002665 ) ) ;
#16441=CARTESIAN_POINT ( 'NONE',  ( -3.329593175259680127, -68.60467830133228517, 13.06284992371192999 ) ) ;
#16448=( NAMED_UNIT ( * ) PLANE_ANGLE_UNIT ( ) SI_UNIT ( $, .RADIAN. ) );
#16453=CARTESIAN_POINT ( 'NONE',  ( 4.954231026949447170, -46.71441375836365495, 40.29635317557408314 ) ) ;
#16461=MECHANICAL_DESIGN_GEOMETRIC_PRESENTATION_REPRESENTATION('',(#42327),#40631);
#16474=EDGE_CURVE ( 'NONE', #63843, #13645, #47147, .T. ) ;
#16479=ORIENTED_EDGE ( 'NONE', *, *, #81982, .T. ) ;
#16497=CARTESIAN_POINT ( 'NONE',  ( 12.37144696128342147, -4.000000000000003553, 20.44658103856077602 ) ) ;
#16502=CARTESIAN_POINT ( 'NONE',  ( 2.560557749087981616, -69.78870608840574619, 13.23340540258364584 ) ) ;
#16504=SURFACE_SIDE_STYLE ('',( #83362 ) ) ;
#16509=EDGE_CURVE ( 'NONE', #93762, #38295, #59260, .T. ) ;
#16531=CARTESIAN_POINT ( 'NONE',  ( 5.000000000000040856, -14.59885031841967518, 13.58543933205510079 ) ) ;
#16555=CARTESIAN_POINT ( 'NONE',  ( 9.475800981716794524, -0.4480317257901532124, 19.86715792471738951 ) ) ;
#16557=( LENGTH_UNIT ( ) NAMED_UNIT ( * ) SI_UNIT ( .MILLI., .METRE. ) );
#16572=CARTESIAN_POINT ( 'NONE',  ( -6.531358237270333156, -12.73775376330297782, -7.942398969220734628 ) ) ;
#16583=AXIS2_PLACEMENT_3D ( 'NONE', #42387, #74215, #106588 ) ;
#16585=CARTESIAN_POINT ( 'NONE',  ( -5.803898591548167119, -46.53140123172381948, 103.8893302396403868 ) ) ;
#16592=EDGE_CURVE ( 'NONE', #5765, #17391, #23090, .T. ) ;
#16635=DIRECTION ( 'NONE',  ( 0.000000000000000000, 1.000000000000000000, 0.000000000000000000 ) ) ;
#16653=ADVANCED_FACE ( 'NONE', ( #92187, #1574 ), #59858, .F. ) ;
#16654=CARTESIAN_POINT ( 'NONE',  ( -5.000000000000000000, -13.79684580107980985, 10.70524563036346599 ) ) ;
#16674=CARTESIAN_POINT ( 'NONE',  ( 12.32678244424858072, -2.923755400730654319, 20.67306671305708576 ) ) ;
#16677=MECHANICAL_DESIGN_GEOMETRIC_PRESENTATION_REPRESENTATION('',(#95920),#102843);
#16706=CARTESIAN_POINT ( 'NONE',  ( 1.460859247228877278, -69.63554188353550956, 12.81388706339240358 ) ) ;
#16715=CARTESIAN_POINT ( 'NONE',  ( 9.771805689013445928, -50.53686792747097911, 29.13556849961307194 ) ) ;
#16721=DIRECTION ( 'NONE',  ( 0.000000000000000000, 1.224646799147352468E-16, 1.000000000000000000 ) ) ;
#16734=SURFACE_STYLE_USAGE ( .BOTH. , #32946 ) ;
#16764=DIRECTION ( 'NONE',  ( 0.000000000000000000, 0.000000000000000000, 1.000000000000000000 ) ) ;
#16771=DIRECTION ( 'NONE',  ( 1.000000000000000000, -0.000000000000000000, -0.000000000000000000 ) ) ;
#16813=CARTESIAN_POINT ( 'NONE',  ( 9.337186727013605747, -56.01312624425312237, 30.58335800272115534 ) ) ;
#16829=ORIENTED_EDGE ( 'NONE', *, *, #70200, .T. ) ;
#16832=EDGE_CURVE ( 'NONE', #71609, #14235, #4202, .T. ) ;
#16868=SURFACE_SIDE_STYLE ('',( #60527 ) ) ;
#16874=( NAMED_UNIT ( * ) SI_UNIT ( $, .STERADIAN. ) SOLID_ANGLE_UNIT ( ) );
#16881=ORIENTED_EDGE ( 'NONE', *, *, #55075, .T. ) ;
#16906=CIRCLE ( 'NONE', #11659, 2.000000000000000000 ) ;
#16958=FILL_AREA_STYLE_COLOUR ( '', #21733 ) ;
#16964=UNCERTAINTY_MEASURE_WITH_UNIT (LENGTH_MEASURE( 1.000000000000000082E-05 ), #17784, 'distance_accuracy_value', 'NONE');
#16970=DIRECTION ( 'NONE',  ( 0.000000000000000000, 0.000000000000000000, 1.000000000000000000 ) ) ;
#16984=( LENGTH_UNIT ( ) NAMED_UNIT ( * ) SI_UNIT ( .MILLI., .METRE. ) );
#16989=CARTESIAN_POINT ( 'NONE',  ( -6.008858299639965317, -63.46485955003367252, 14.35488293964984585 ) ) ;
#17024=FILL_AREA_STYLE_COLOUR ( '', #52235 ) ;
#17048=CARTESIAN_POINT ( 'NONE',  ( 4.749156675558425356, -64.72194359721190438, 13.06006237490043453 ) ) ;
#17050=PRESENTATION_STYLE_ASSIGNMENT (( #66118 ) ) ;
#17070=VERTEX_POINT ( 'NONE', #80250 ) ;
#17078=CARTESIAN_POINT ( 'NONE',  ( 5.959015317364894315, -13.75072846948223493, 13.79531249880999155 ) ) ;
#17100=CARTESIAN_POINT ( 'NONE',  ( 4.973317752991470719, -46.53140123174533471, 102.2736751349651456 ) ) ;
#17106=LINE ( 'NONE', #83414, #20362 ) ;
#17116=CARTESIAN_POINT ( 'NONE',  ( -1.338977211094423136, -5.480044445862255031, -13.97241428226087301 ) ) ;
#17152=SURFACE_STYLE_FILL_AREA ( #25256 ) ;
#17155=ORIENTED_EDGE ( 'NONE', *, *, #74493, .F. ) ;
#17165=CARTESIAN_POINT ( 'NONE',  ( 3.508895115991522928, -48.85046701618207265, 104.5950737443334759 ) ) ;
#17184=( LENGTH_UNIT ( ) NAMED_UNIT ( * ) SI_UNIT ( .MILLI., .METRE. ) );
#17224=CIRCLE ( 'NONE', #93046, 4.000000000000000000 ) ;
#17227=CARTESIAN_POINT ( 'NONE',  ( 9.275666170511263076, -2.831271561983539797, 14.74122513583426120 ) ) ;
#17231=DIRECTION ( 'NONE',  ( 0.000000000000000000, 1.000000000000000000, 0.000000000000000000 ) ) ;
#17242=VERTEX_POINT ( 'NONE', #26860 ) ;
#17257=PRESENTATION_STYLE_ASSIGNMENT (( #98668 ) ) ;
#17263=CARTESIAN_POINT ( 'NONE',  ( 9.269255467170962604, -52.95527593926346555, 23.24713075214419433 ) ) ;
#17279=EDGE_LOOP ( 'NONE', ( #33067, #18100 ) ) ;
#17286=CARTESIAN_POINT ( 'NONE',  ( -11.84876416945811961, -1.967757499684315237, 20.63514712866197343 ) ) ;
#17300=ADVANCED_FACE ( 'NONE', ( #50017 ), #97032, .T. ) ;
#17326=CARTESIAN_POINT ( 'NONE',  ( 0.000000000000000000, -54.00000000000000711, 41.00000000000000000 ) ) ;
#17353=DIRECTION ( 'NONE',  ( 0.000000000000000000, 1.000000000000000000, 0.000000000000000000 ) ) ;
#17358=CARTESIAN_POINT ( 'NONE',  ( -3.801077171203097294, -1.110903940591820627, 104.1059035333590401 ) ) ;
#17364=CARTESIAN_POINT ( 'NONE',  ( 5.000000000000000000, -25.24897476799365492, -2.444053521653484662 ) ) ;
#17391=VERTEX_POINT ( 'NONE', #37069 ) ;
#17404=FACE_OUTER_BOUND ( 'NONE', #94315, .T. ) ;
#17419=( LENGTH_UNIT ( ) NAMED_UNIT ( * ) SI_UNIT ( .MILLI., .METRE. ) );
#17441=LINE ( 'NONE', #1749, #94638 ) ;
#17460=( NAMED_UNIT ( * ) PLANE_ANGLE_UNIT ( ) SI_UNIT ( $, .RADIAN. ) );
#17463=CARTESIAN_POINT ( 'NONE',  ( -4.956067050182347167, -15.30475822382919837, -6.874165724332737426 ) ) ;
#17466=CARTESIAN_POINT ( 'NONE',  ( -15.81527375476383668, -3.786780092678120102, 14.52839066106889554 ) ) ;
#17472=AXIS2_PLACEMENT_3D ( 'NONE', #5188, #87703, #34262 ) ;
#17479=CARTESIAN_POINT ( 'NONE',  ( 15.19779194289341895, -6.149863736328142316, 13.69448736525634303 ) ) ;
#17497=CARTESIAN_POINT ( 'NONE',  ( -4.195612334301150881, -48.94124001270379409, 104.4881327927213448 ) ) ;
#17522=DIRECTION ( 'NONE',  ( 0.05555555555555524022, 0.000000000000000000, 0.9984555975339683975 ) ) ;
#17540=SURFACE_STYLE_USAGE ( .BOTH. , #40729 ) ;
#17588=CARTESIAN_POINT ( 'NONE',  ( 3.908772774635062230, -67.68245115326362793, 13.12901559851279387 ) ) ;
#17749=ORIENTED_EDGE ( 'NONE', *, *, #34723, .T. ) ;
#17784=( LENGTH_UNIT ( ) NAMED_UNIT ( * ) SI_UNIT ( .MILLI., .METRE. ) );
#17791=FILL_AREA_STYLE ('',( #58780 ) ) ;
#17836=CARTESIAN_POINT ( 'NONE',  ( -9.335947753887891665, -2.525768943555868340, 14.78755529138710223 ) ) ;
#17842=DIRECTION ( 'NONE',  ( 0.000000000000000000, 0.000000000000000000, 1.000000000000000000 ) ) ;
#17890=CARTESIAN_POINT ( 'NONE',  ( -1.112654532564758547, -3.176373552203621264E-18, 101.1535731093139816 ) ) ;
#17910=DIRECTION ( 'NONE',  ( -0.000000000000000000, -1.000000000000000000, -0.000000000000000000 ) ) ;
#17938=PRESENTATION_STYLE_ASSIGNMENT (( #8229 ) ) ;
#17950=CARTESIAN_POINT ( 'NONE',  ( -5.000000000000000888, -64.69605072860053951, 10.12418081620033661 ) ) ;
#17989=AXIS2_PLACEMENT_3D ( 'NONE', #73342, #76010, #67411 ) ;
#17991=CARTESIAN_POINT ( 'NONE',  ( -2.789712857209384556, -9.223132490779253345, -12.21941282805327234 ) ) ;
#18023=FACE_OUTER_BOUND ( 'NONE', #97531, .T. ) ;
#18028=STYLED_ITEM ( 'NONE', ( #71495 ), #87112 ) ;
#18035=AXIS2_PLACEMENT_3D ( 'NONE', #22283, #20725, #29849 ) ;
#18036=MECHANICAL_DESIGN_GEOMETRIC_PRESENTATION_REPRESENTATION('',(#23197),#40412);
#18046=( LENGTH_UNIT ( ) NAMED_UNIT ( * ) SI_UNIT ( .MILLI., .METRE. ) );
#18054=CYLINDRICAL_SURFACE ( 'NONE', #395, 9.000000000000000000 ) ;
#18074=( BOUNDED_SURFACE ( )  B_SPLINE_SURFACE ( 3, 2, ( 
 ( #26068, #43263, #84783 ),
 ( #52399, #68066, #76680 ),
 ( #11402, #77759, #93414 ),
 ( #19032, #76145, #27117 ) ),
 .UNSPECIFIED., .F., .F., .F. ) 
 B_SPLINE_SURFACE_WITH_KNOTS ( ( 4, 4 ),
 ( 3, 3 ),
 ( -2.262729933977247754E-16, 0.0009806926547533787071 ),
 ( 0.000000000000000000, 1.000000000000000000 ),
 .UNSPECIFIED. ) 
 GEOMETRIC_REPRESENTATION_ITEM ( )  RATIONAL_B_SPLINE_SURFACE ( (
 ( 1.000000000000000000, 0.9603284238771497838, 1.000000000000000000),
 ( 1.000000000000000000, 0.9551945799212837596, 1.000000000000000000),
 ( 1.000000000000000000, 0.9458776633876946338, 1.000000000000000000),
 ( 1.000000000000000000, 0.9359444767143315635, 1.000000000000000000) ) ) 
 REPRESENTATION_ITEM ( '' )  SURFACE ( )  );
#18093=EDGE_CURVE ( 'NONE', #17070, #45005, #61468, .T. ) ;
#18100=ORIENTED_EDGE ( 'NONE', *, *, #43040, .T. ) ;
#18101=CARTESIAN_POINT ( 'NONE',  ( 4.168229866080995549, -48.49071734043477733, 43.45413307567940819 ) ) ;
#18123=CARTESIAN_POINT ( 'NONE',  ( 4.569677289105409379, -65.67692000944629171, 13.11436000269381985 ) ) ;
#18137=SURFACE_SIDE_STYLE ('',( #75820 ) ) ;
#18167=DIRECTION ( 'NONE',  ( 0.000000000000000000, -1.000000000000000000, 0.000000000000000000 ) ) ;
#18202=MECHANICAL_DESIGN_GEOMETRIC_PRESENTATION_REPRESENTATION('',(#90537),#11291);
#18204=AXIS2_PLACEMENT_3D ( 'NONE', #76398, #101749, #2512 ) ;
#18209=DIRECTION ( 'NONE',  ( 0.000000000000000000, 0.000000000000000000, 1.000000000000000000 ) ) ;
#18247=CARTESIAN_POINT ( 'NONE',  ( 0.000000000000000000, -50.00000000000000000, 112.0000000000000000 ) ) ;
#18259=EDGE_CURVE ( 'NONE', #21120, #97430, #25820, .T. ) ;
#18285=AXIS2_PLACEMENT_3D ( 'NONE', #94880, #102422, #78138 ) ;
#18295=CARTESIAN_POINT ( 'NONE',  ( 10.63911829571853929, -0.9478434794733983093, 20.26887800423669717 ) ) ;
#18317=B_SPLINE_CURVE_WITH_KNOTS ( 'NONE', 3,
 ( #97745, #24448, #81545, #82095, #96710, #81031, #6620, #22847 ),
 .UNSPECIFIED., .F., .F.,
 ( 4, 2, 2, 4 ),
 ( -1.044876449520883118E-05, 0.0004743401164197471763, 0.0007167345568772206729, 0.0009591289973346941696 ),
 .UNSPECIFIED. ) ;
#18324=CARTESIAN_POINT ( 'NONE',  ( 5.169066395376115786, -13.70246774098871079, -6.130298896213989046 ) ) ;
#18360=DIRECTION ( 'NONE',  ( 0.000000000000000000, 0.000000000000000000, -1.000000000000000000 ) ) ;
#18380=SURFACE_SIDE_STYLE ('',( #9179 ) ) ;
#18387=( NAMED_UNIT ( * ) SI_UNIT ( $, .STERADIAN. ) SOLID_ANGLE_UNIT ( ) );
#18402=ORIENTED_EDGE ( 'NONE', *, *, #74691, .T. ) ;
#18410=CARTESIAN_POINT ( 'NONE',  ( -5.000000000000000000, -14.11579947677662261, 9.475149649641746663 ) ) ;
#18417=TOROIDAL_SURFACE ( 'NONE', #76984, 13.00000000000000000, 2.000000000000000000 ) ;
#18431=AXIS2_PLACEMENT_3D ( 'NONE', #105386, #41181, #98857 ) ;
#18462=ORIENTED_EDGE ( 'NONE', *, *, #58627, .F. ) ;
#18463=SURFACE_STYLE_USAGE ( .BOTH. , #11385 ) ;
#18503=COLOUR_RGB ( '', 0.72549020, 0.75294118, 0.79215686) ;
#18508=VERTEX_POINT ( 'NONE', #61339 ) ;
#18511=EDGE_CURVE ( 'NONE', #12868, #56691, #5736, .T. ) ;
#18527=CARTESIAN_POINT ( 'NONE',  ( 3.753470829068755954, -1.089309597783790551, 104.5911851069063943 ) ) ;
#18529=CARTESIAN_POINT ( 'NONE',  ( -5.180156406282273807, -13.23729396337573050, -7.081638082358150399 ) ) ;
#18534=CARTESIAN_POINT ( 'NONE',  ( 3.386172030103295594, -0.8620675201542831179, 104.0372870256219642 ) ) ;
#18564=ADVANCED_FACE ( 'NONE', ( #102311 ), #74842, .T. ) ;
#18566=CARTESIAN_POINT ( 'NONE',  ( 4.581218816254565063, -2.199133564524530460, 103.5404609598622301 ) ) ;
#18571=EDGE_LOOP ( 'NONE', ( #7376, #98151, #74378, #65875 ) ) ;
#18582=CARTESIAN_POINT ( 'NONE',  ( 0.000000000000000000, -48.79941684889505638, 112.0000000000000000 ) ) ;
#18595=EDGE_LOOP ( 'NONE', ( #53307, #94049, #75936, #86484 ) ) ;
#18608=CARTESIAN_POINT ( 'NONE',  ( 30.00000000000000000, 0.000000000000000000, 0.000000000000000000 ) ) ;
#18614=CARTESIAN_POINT ( 'NONE',  ( 6.670804059825538701, -48.62050409103763116, 39.30984229886809800 ) ) ;
#18644=CARTESIAN_POINT ( 'NONE',  ( 4.999999999999995559, -46.00000000000000000, 42.58845726811989607 ) ) ;
#18645=MECHANICAL_DESIGN_GEOMETRIC_PRESENTATION_REPRESENTATION('',(#66894),#84058);
#18649=DIRECTION ( 'NONE',  ( -9.714451465434776236E-14, -1.000000000000000000, -2.768324312120152571E-13 ) ) ;
#18694=CARTESIAN_POINT ( 'NONE',  ( 5.000000000000000000, -15.43644767549559482, 12.61250542912354078 ) ) ;
#18749=VECTOR ( 'NONE', #52947, 1000.000000000000000 ) ;
#18757=ORIENTED_EDGE ( 'NONE', *, *, #102694, .T. ) ;
#18781=( GEOMETRIC_REPRESENTATION_CONTEXT ( 3 ) GLOBAL_UNCERTAINTY_ASSIGNED_CONTEXT ( ( #92027 ) ) GLOBAL_UNIT_ASSIGNED_CONTEXT ( ( #82656, #74023, #32001 ) ) REPRESENTATION_CONTEXT ( 'NONE', 'WORKASPACE' ) );
#18787=CARTESIAN_POINT ( 'NONE',  ( 6.999999999999995559, -46.00000000000000000, 39.12435565298213902 ) ) ;
#18790=LINE ( 'NONE', #11702, #28823 ) ;
#18797=ORIENTED_EDGE ( 'NONE', *, *, #13177, .T. ) ;
#18798=DIRECTION ( 'NONE',  ( -0.000000000000000000, 1.000000000000000000, -0.000000000000000000 ) ) ;
#18830=FACE_OUTER_BOUND ( 'NONE', #83502, .T. ) ;
#18841=EDGE_LOOP ( 'NONE', ( #39873, #87752, #94070 ) ) ;
#18847=( NAMED_UNIT ( * ) PLANE_ANGLE_UNIT ( ) SI_UNIT ( $, .RADIAN. ) );
#18850=CARTESIAN_POINT ( 'NONE',  ( 3.718188220750195505, -48.95098499554293880, 104.2423402216923591 ) ) ;
#18881=ADVANCED_FACE ( 'NONE', ( #25130 ), #85168, .F. ) ;
#18888=CARTESIAN_POINT ( 'NONE',  ( 0.000000000000000000, -80.00000000000000000, 27.00000000000000000 ) ) ;
#18890=( GEOMETRIC_REPRESENTATION_CONTEXT ( 3 ) GLOBAL_UNCERTAINTY_ASSIGNED_CONTEXT ( ( #48500 ) ) GLOBAL_UNIT_ASSIGNED_CONTEXT ( ( #82929, #80796, #37872 ) ) REPRESENTATION_CONTEXT ( 'NONE', 'WORKASPACE' ) );
#18891=EDGE_CURVE ( 'NONE', #8366, #101089, #19582, .T. ) ;
#18901=DIRECTION ( 'NONE',  ( -1.000000000000000000, 0.000000000000000000, 1.096832036894112098E-16 ) ) ;
#18910=CARTESIAN_POINT ( 'NONE',  ( -30.00000000000000000, -54.00000000000000711, 27.11721482942554928 ) ) ;
#18923=FACE_OUTER_BOUND ( 'NONE', #17279, .T. ) ;
#18933=ORIENTED_EDGE ( 'NONE', *, *, #37057, .F. ) ;
#18984=CARTESIAN_POINT ( 'NONE',  ( 0.000000000000000000, -50.00000000000000000, 27.00000000000000000 ) ) ;
#18985=UNCERTAINTY_MEASURE_WITH_UNIT (LENGTH_MEASURE( 1.000000000000000082E-05 ), #16984, 'distance_accuracy_value', 'NONE');
#18990=UNCERTAINTY_MEASURE_WITH_UNIT (LENGTH_MEASURE( 1.000000000000000082E-05 ), #69023, 'distance_accuracy_value', 'NONE');
#19014=CARTESIAN_POINT ( 'NONE',  ( 1.257641187044677311, -49.99999999632648695, 101.3278948775254094 ) ) ;
#19032=CARTESIAN_POINT ( 'NONE',  ( -4.551587301587303180, -1.200583151104949176, 104.4018401814738155 ) ) ;
#19041=CARTESIAN_POINT ( 'NONE',  ( 10.59869873574526267, 2.545575842793166732, 14.78270473238058891 ) ) ;
#19073=SURFACE_SIDE_STYLE ('',( #69192 ) ) ;
#19084=( NAMED_UNIT ( * ) SI_UNIT ( $, .STERADIAN. ) SOLID_ANGLE_UNIT ( ) );
#19098=CARTESIAN_POINT ( 'NONE',  ( 13.51445589115056833, -9.121446783585646756, 11.91887821639477707 ) ) ;
#19119=CARTESIAN_POINT ( 'NONE',  ( 5.000000000092883035, -3.772466818847466818, 103.2791840072271015 ) ) ;
#19120=CARTESIAN_POINT ( 'NONE',  ( -3.841398122528037806, -48.92777529680780901, 104.5835869663331295 ) ) ;
#19125=ADVANCED_FACE ( 'NONE', ( #70119 ), #74234, .T. ) ;
#19170=CARTESIAN_POINT ( 'NONE',  ( 3.438608821155801021, -49.17330182167980013, 44.01479443626973875 ) ) ;
#19188=VERTEX_POINT ( 'NONE', #63093 ) ;
#19243=EDGE_LOOP ( 'NONE', ( #73220, #23908, #4901, #21364 ) ) ;
#19255=CARTESIAN_POINT ( 'NONE',  ( 4.277266239492808708, -9.465691673376495530, -11.68615649787714972 ) ) ;
#19256=VECTOR ( 'NONE', #61840, 1000.000000000000000 ) ;
#19257=B_SPLINE_CURVE_WITH_KNOTS ( 'NONE', 3,
 ( #66111, #24622, #40769, #58009, #97947, #56939, #74719, #82290, #99530, #58569, #40241, #89861, #15968, #32168, #73660, #73117, #15432, #90934, #82829, #91466, #48846, #16497 ),
 .UNSPECIFIED., .F., .F.,
 ( 4, 2, 2, 2, 2, 2, 2, 2, 2, 2, 4 ),
 ( 0.001294468792936987779, 0.002255807329995941028, 0.003217145867054894276, 0.005139822941172805110, 0.006101161478231762261, 0.007062500015290718546, 0.008985177089408637185, 0.01090785416352655843, 0.01283053123764447967, 0.01475320831176240091, 0.01667588538588031868 ),
 .UNSPECIFIED. ) ;
#19361=FACE_OUTER_BOUND ( 'NONE', #98927, .T. ) ;
#19374=DIRECTION ( 'NONE',  ( 0.000000000000000000, 0.000000000000000000, 1.000000000000000000 ) ) ;
#19394=CARTESIAN_POINT ( 'NONE',  ( 3.459690225506051320, -48.89101625908396898, 104.5059395991323470 ) ) ;
#19403=ORIENTED_EDGE ( 'NONE', *, *, #22339, .F. ) ;
#19417=CARTESIAN_POINT ( 'NONE',  ( 5.180156406282274695, -13.23729396337629538, -7.081638082359322794 ) ) ;
#19478=FACE_OUTER_BOUND ( 'NONE', #67777, .T. ) ;
#19487=CARTESIAN_POINT ( 'NONE',  ( -4.460266806907394077, -1.165284401735731112, 104.3906379647731910 ) ) ;
#19496=LINE ( 'NONE', #69603, #11151 ) ;
#19517=CARTESIAN_POINT ( 'NONE',  ( -3.558939058151737722, -1.060970281106035751, 104.4181685828941966 ) ) ;
#19523=CARTESIAN_POINT ( 'NONE',  ( 11.13412560657217654, -11.04925094343736269, 10.14712091588952347 ) ) ;
#19550=CARTESIAN_POINT ( 'NONE',  ( 3.052800042147939319, -49.15628846935693730, 104.0321489743691501 ) ) ;
#19554=CARTESIAN_POINT ( 'NONE',  ( -9.113097280746996987, -54.00000000000000711, 31.11721482942554928 ) ) ;
#19564=ORIENTED_EDGE ( 'NONE', *, *, #55334, .T. ) ;
#19582=CIRCLE ( 'NONE', #64350, 9.999999999999994671 ) ;
#19586=DIRECTION ( 'NONE',  ( -1.000000000000000000, -0.000000000000000000, -0.000000000000000000 ) ) ;
#19620=CARTESIAN_POINT ( 'NONE',  ( 0.9999999999999997780, -51.24679913438006196, 3.817907945688783666 ) ) ;
#19625=CARTESIAN_POINT ( 'NONE',  ( -6.437509419382472231, -11.87447412552791448, 10.48822171390120950 ) ) ;
#19636=CARTESIAN_POINT ( 'NONE',  ( 14.32310282642602850, -7.975991125463504083, 12.70685702462689193 ) ) ;
#19646=LINE ( 'NONE', #36879, #31263 ) ;
#19657=CARTESIAN_POINT ( 'NONE',  ( 4.750186375024371799, -1.378107633083520911, 104.3180500829679289 ) ) ;
#19659=CARTESIAN_POINT ( 'NONE',  ( -3.460324465703970453, -48.83451908470669878, 104.5902739980974161 ) ) ;
#19663=DIRECTION ( 'NONE',  ( 0.000000000000000000, 1.000000000000000000, 0.000000000000000000 ) ) ;
#19701=CARTESIAN_POINT ( 'NONE',  ( 3.638102518737710955, -49.00949705677293622, 43.87169722584302889 ) ) ;
#19719=CARTESIAN_POINT ( 'NONE',  ( -3.737791945709141306, -48.91906356597342409, 43.79597853662111362 ) ) ;
#19794=CARTESIAN_POINT ( 'NONE',  ( 11.16512584324286728, -1.276815909463798526, 20.44381853242944302 ) ) ;
#19851=CARTESIAN_POINT ( 'NONE',  ( 13.99726531479253566, -50.00011198987433403, 27.38140257663831889 ) ) ;
#19852=CARTESIAN_POINT ( 'NONE',  ( 5.000000000000000000, -14.08057492516784670, 11.76246841892764827 ) ) ;
#19855=EDGE_CURVE ( 'NONE', #22140, #97138, #3806, .T. ) ;
#19912=ORIENTED_EDGE ( 'NONE', *, *, #106389, .F. ) ;
#19948=CARTESIAN_POINT ( 'NONE',  ( 4.805888432416990597, -14.59013712844782340, -7.778733730875278418 ) ) ;
#19951=CARTESIAN_POINT ( 'NONE',  ( 4.681380154937406779, 0.7378729568059335664, 103.7259032015043232 ) ) ;
#19979=CARTESIAN_POINT ( 'NONE',  ( 2.068673967786806678, -0.1361670080194822274, 102.1191603897975284 ) ) ;
#19993=PLANE ( 'NONE',  #80258 ) ;
#19996=CARTESIAN_POINT ( 'NONE',  ( -12.08879135166870888, -2.338888145639765881, 20.67789593137304749 ) ) ;
#20023=ORIENTED_EDGE ( 'NONE', *, *, #43928, .T. ) ;
#20039=ORIENTED_EDGE ( 'NONE', *, *, #68616, .T. ) ;
#20048=CARTESIAN_POINT ( 'NONE',  ( -3.626288723285919779, -1.044241108143933339, 104.3502830461760880 ) ) ;
#20084=CARTESIAN_POINT ( 'NONE',  ( 2.806188179629718782, -49.57861714546726972, 102.9366787940491861 ) ) ;
#20110=CARTESIAN_POINT ( 'NONE',  ( -4.302752950498814677, -48.89765970236341985, 104.4121132197325466 ) ) ;
#20120=ORIENTED_EDGE ( 'NONE', *, *, #104818, .F. ) ;
#20150=CARTESIAN_POINT ( 'NONE',  ( 3.384215095276188023, -0.8669809812617773614, 104.0501775326196281 ) ) ;
#20167=CARTESIAN_POINT ( 'NONE',  ( 13.87407757772530736, -57.47192967781523976, 25.11348823608586400 ) ) ;
#20187=CARTESIAN_POINT ( 'NONE',  ( 4.928386788250423756, -1.571875576847029388, 104.2441249819466833 ) ) ;
#20188=CARTESIAN_POINT ( 'NONE',  ( -3.753470829068717762, -48.91069040221621123, 104.5911851069064085 ) ) ;
#20193=PRESENTATION_STYLE_ASSIGNMENT (( #28816 ) ) ;
#20210=ADVANCED_FACE ( 'NONE', ( #11902 ), #86527, .T. ) ;
#20214=CARTESIAN_POINT ( 'NONE',  ( -9.226722513859208163, -54.52964393432027634, 23.14374324513729064 ) ) ;
#20230=MECHANICAL_DESIGN_GEOMETRIC_PRESENTATION_REPRESENTATION('',(#33902),#87314);
#20238=CARTESIAN_POINT ( 'NONE',  ( 5.029581416257693505, -51.84653879358399564, 40.06623209565592703 ) ) ;
#20257=CARTESIAN_POINT ( 'NONE',  ( -1.197355913555570028, -53.99999999817047325, 40.95503241349764778 ) ) ;
#20287=FILL_AREA_STYLE_COLOUR ( '', #45955 ) ;
#20306=MECHANICAL_DESIGN_GEOMETRIC_PRESENTATION_REPRESENTATION('',(#85713),#82210);
#20334=CARTESIAN_POINT ( 'NONE',  ( 0.000000000000000000, -50.00000000000000000, 112.0000000000000000 ) ) ;
#20338=CARTESIAN_POINT ( 'NONE',  ( 12.40471543347789485, -3.812522371550363331, 20.50938476615066719 ) ) ;
#20339=CIRCLE ( 'NONE', #90884, 2.000000000000001776 ) ;
#20356=CARTESIAN_POINT ( 'NONE',  ( -4.999999999999993783, -46.00000000000000000, 103.3397459621556180 ) ) ;
#20358=CARTESIAN_POINT ( 'NONE',  ( -0.8750000000010113022, -70.58759490697451611, 13.02737050516266493 ) ) ;
#20359=CARTESIAN_POINT ( 'NONE',  ( 12.37144696128342147, -4.000000000000003553, 20.44658103856077602 ) ) ;
#20362=VECTOR ( 'NONE', #32773, 1000.000000000000000 ) ;
#20405=CARTESIAN_POINT ( 'NONE',  ( 5.000000000000000000, -15.62228920881129390, 12.61250543006183378 ) ) ;
#20407=CARTESIAN_POINT ( 'NONE',  ( 3.778422651548691391, -1.120239677707988823, 103.2432416460067657 ) ) ;
#20458=CARTESIAN_POINT ( 'NONE',  ( 4.117685099651370528, -69.22520594386868709, 13.61356083086173285 ) ) ;
#20464=CARTESIAN_POINT ( 'NONE',  ( -15.90614609307868577, -3.157894736842101757, 14.66382285868950852 ) ) ;
#20468=CARTESIAN_POINT ( 'NONE',  ( 3.534854069001187593, -48.92952247113088760, 104.4405781011833483 ) ) ;
#20474=EDGE_CURVE ( 'NONE', #76724, #88866, #77559, .T. ) ;
#20494=CARTESIAN_POINT ( 'NONE',  ( 1.916513513605337504, -7.172711491783059223, -13.28747680017345623 ) ) ;
#20496=CARTESIAN_POINT ( 'NONE',  ( 0.9999999999999940048, 0.000000000000000000, 101.0455488498966758 ) ) ;
#20522=CARTESIAN_POINT ( 'NONE',  ( 5.385673916453011856, 3.999999999999999112, 18.57417562100670949 ) ) ;
#20527=PRESENTATION_STYLE_ASSIGNMENT (( #54388 ) ) ;
#20533=DIRECTION ( 'NONE',  ( 0.000000000000000000, 0.000000000000000000, 1.000000000000000000 ) ) ;
#20542=CARTESIAN_POINT ( 'NONE',  ( -9.877897116810617106, -2.622329759909478586, 15.38437439719164779 ) ) ;
#20549=B_SPLINE_CURVE_WITH_KNOTS ( 'NONE', 3,
 ( #95541, #37345, #78814, #103109, #79348, #77770, #20110, #3883 ),
 .UNSPECIFIED., .F., .F.,
 ( 4, 2, 2, 4 ),
 ( 8.673617379884035472E-19, 0.0001460451837441968887, 0.0002190677756162943436, 0.0002920903674883918257 ),
 .UNSPECIFIED. ) ;
#20551=DIRECTION ( 'NONE',  ( 0.000000000000000000, 0.000000000000000000, 1.000000000000000000 ) ) ;
#20572=CARTESIAN_POINT ( 'NONE',  ( -5.000000000000080824, -12.34932486159458342, 8.854147762507302843 ) ) ;
#20581=CARTESIAN_POINT ( 'NONE',  ( -13.99719405338373512, -50.00026112179624960, 27.38482409491458114 ) ) ;
#20583=CLOSED_SHELL ( 'NONE', ( #78647, #68065, #66973, #20774, #96092, #94732, #10316, #77159, #15527, #66649, #44605, #18564, #185, #93726, #20210, #6131, #24056, #49998, #65823, #36037, #87198, #35733, #65440, #12484, #101096, #10364, #104825, #16653, #99977, #76156, #55728, #11749, #59647, #26717, #82998, #85105, #22388, #27947, #44238, #51679, #60434, #45217, #90435, #100986, #105147, #13402, #17300, #84820, #38990, #44186, #44780, #30042, #15259, #60953, #12305, #98816, #18881, #98511, #59131, #67844, #38054, #21310, #8466, #41599, #14634, #35149, #104485, #13091, #1826, #56475, #57123, #59831, #1568, #19125, #49080, #13526, #42772, #58421, #89040, #29400, #85645, #68261, #2790, #7868, #92949, #76671, #31215, #39165, #97546, #15853, #88446, #55970, #95952, #85431, #58033, #100988, #87112, #86403, #60785, #27809 ) ) ;
#20598=CARTESIAN_POINT ( 'NONE',  ( -5.000000000000000000, -60.71953810597282342, 12.61250543006821978 ) ) ;
#20649=CARTESIAN_POINT ( 'NONE',  ( 6.999999999999998224, -12.54465221550629472, 8.223849511755000563 ) ) ;
#20677=CARTESIAN_POINT ( 'NONE',  ( -2.706785074969889848, -0.5477000579813379177, 103.4519997648587406 ) ) ;
#20682=FILL_AREA_STYLE_COLOUR ( '', #103520 ) ;
#20694=CARTESIAN_POINT ( 'NONE',  ( -2.374770270502819969, -6.910312371743992266, -13.35351085777655733 ) ) ;
#20713=EDGE_LOOP ( 'NONE', ( #17155, #85108, #30282, #28837 ) ) ;
#20718=CARTESIAN_POINT ( 'NONE',  ( 9.113097280746998763, -54.26300649141423804, 31.11721482942554928 ) ) ;
#20722=CARTESIAN_POINT ( 'NONE',  ( 3.702395615612342095, -48.95046109946132162, 103.3251893371222394 ) ) ;
#20725=DIRECTION ( 'NONE',  ( -1.000000000000000000, 0.000000000000000000, 0.000000000000000000 ) ) ;
#20729=CARTESIAN_POINT ( 'NONE',  ( 4.680975426248725313, -2.415770170678304130, 103.4780497728483226 ) ) ;
#20730=CARTESIAN_POINT ( 'NONE',  ( -3.564365538407123779, -48.86493411501031403, 104.5953911288849412 ) ) ;
#20771=CARTESIAN_POINT ( 'NONE',  ( 0.9263455752254985409, -50.01477469915685248, 40.97011183254556954 ) ) ;
#20774=ADVANCED_FACE ( 'NONE', ( #44433 ), #38391, .T. ) ;
#20854=CARTESIAN_POINT ( 'NONE',  ( -30.00000000000000000, 0.000000000000000000, 0.000000000000000000 ) ) ;
#20866=CARTESIAN_POINT ( 'NONE',  ( -5.371950044183563477, -47.79483119409569269, 104.0625755208173331 ) ) ;
#20867=CARTESIAN_POINT ( 'NONE',  ( -13.45079846400083312, -54.00000000000000711, 23.11721482942554928 ) ) ;
#20879=EDGE_CURVE ( 'NONE', #17391, #97138, #78677, .T. ) ;
#20888=CARTESIAN_POINT ( 'NONE',  ( -1.348501488157294759, -70.09340828808477397, 13.06360208188350214 ) ) ;
#20911=DIRECTION ( 'NONE',  ( 2.742080092235280244E-17, 0.000000000000000000, -1.000000000000000000 ) ) ;
#20923=CARTESIAN_POINT ( 'NONE',  ( 13.72588371288480857, -50.98893574582776722, 29.76328409196439750 ) ) ;
#20986=CARTESIAN_POINT ( 'NONE',  ( -5.060123309432819738, -8.366457779114602644, 13.66741525926336465 ) ) ;
#20989=CARTESIAN_POINT ( 'NONE',  ( 3.801077171203071536, -48.88909605940820313, 104.1059035333590685 ) ) ;
#20990=CARTESIAN_POINT ( 'NONE',  ( -2.745291993961042731, -9.118645366782532236, -12.27859709492980578 ) ) ;
#21031=EDGE_LOOP ( 'NONE', ( #24375, #60875, #39733, #61845 ) ) ;
#21043=CARTESIAN_POINT ( 'NONE',  ( 3.677391134430071151, -1.015220045778296276, 104.0097548473155626 ) ) ;
#21050=CARTESIAN_POINT ( 'NONE',  ( -27.99999999999999645, 0.000000000000000000, 0.000000000000000000 ) ) ;
#21053=ORIENTED_EDGE ( 'NONE', *, *, #57481, .F. ) ;
#21054=CARTESIAN_POINT ( 'NONE',  ( -9.285538112422313972, -2.937467806972811957, 14.74006110461671071 ) ) ;
#21076=ORIENTED_EDGE ( 'NONE', *, *, #3982, .T. ) ;
#21109=CARTESIAN_POINT ( 'NONE',  ( -2.224272751641298562, -69.45625592918534608, 12.90769492712830413 ) ) ;
#21110=FACE_OUTER_BOUND ( 'NONE', #3709, .T. ) ;
#21120=VERTEX_POINT ( 'NONE', #27095 ) ;
#21134=TOROIDAL_SURFACE ( 'NONE', #81337, 13.00000000000000000, 2.000000000000000000 ) ;
#21159=CIRCLE ( 'NONE', #69320, 4.000000000000000000 ) ;
#21177=DIRECTION ( 'NONE',  ( 1.224646799147353454E-16, 0.000000000000000000, -1.000000000000000000 ) ) ;
#21221=EDGE_CURVE ( 'NONE', #66555, #10104, #23529, .T. ) ;
#21247=CARTESIAN_POINT ( 'NONE',  ( -5.000000000000000000, 0.000000000000000000, 0.000000000000000000 ) ) ;
#21251=DIRECTION ( 'NONE',  ( 0.000000000000000000, 0.000000000000000000, 1.000000000000000000 ) ) ;
#21299=CARTESIAN_POINT ( 'NONE',  ( -3.015909229672554037, -49.46458095252987874, 44.28828481597984990 ) ) ;
#21307=CARTESIAN_POINT ( 'NONE',  ( 0.9999999999999954481, -50.00000000000000000, 44.97220075561143204 ) ) ;
#21310=ADVANCED_FACE ( 'NONE', ( #74395 ), #81673, .F. ) ;
#21319=STYLED_ITEM ( 'NONE', ( #83447 ), #17300 ) ;
#21357=CARTESIAN_POINT ( 'NONE',  ( 6.999999999999998224, -13.84208359229911345, -5.811937548932195163 ) ) ;
#21364=ORIENTED_EDGE ( 'NONE', *, *, #22767, .F. ) ;
#21390=( NAMED_UNIT ( * ) PLANE_ANGLE_UNIT ( ) SI_UNIT ( $, .RADIAN. ) );
#21421=CARTESIAN_POINT ( 'NONE',  ( 13.90371668366488400, -50.40548167538292290, 25.34313603510888413 ) ) ;
#21453=EDGE_LOOP ( 'NONE', ( #42985, #67379, #86534, #102278, #40101 ) ) ;
#21455=FILL_AREA_STYLE_COLOUR ( '', #72974 ) ;
#21467=CARTESIAN_POINT ( 'NONE',  ( 13.38090213880806978, -54.00000000000000711, 31.11721482942554928 ) ) ;
#21491=CARTESIAN_POINT ( 'NONE',  ( -15.43550796417891746, -5.411715871157647406, 14.00207068577347869 ) ) ;
#21562=CARTESIAN_POINT ( 'NONE',  ( -10.79486422923573485, -1.039336085533928422, 20.32133261175441774 ) ) ;
#21572=DIRECTION ( 'NONE',  ( 0.000000000000000000, 1.000000000000000000, 0.000000000000000000 ) ) ;
#21583=AXIS2_PLACEMENT_3D ( 'NONE', #72656, #73709, #106613 ) ;
#21599=CARTESIAN_POINT ( 'NONE',  ( -1.401502055033657879, -70.62283062862942984, 13.06788351849044538 ) ) ;
#21623=CARTESIAN_POINT ( 'NONE',  ( -4.855126259300333480, -63.86661610792060628, 12.98872547890887574 ) ) ;
#21628=CARTESIAN_POINT ( 'NONE',  ( 4.460266806907394965, -48.83471559826429598, 104.3906379647731910 ) ) ;
#21707=FILL_AREA_STYLE_COLOUR ( '', #27790 ) ;
#21719=( NAMED_UNIT ( * ) PLANE_ANGLE_UNIT ( ) SI_UNIT ( $, .RADIAN. ) );
#21725=SURFACE_STYLE_USAGE ( .BOTH. , #37918 ) ;
#21733=COLOUR_RGB ( '', 0.72549020, 0.75294118, 0.79215686) ;
#21745=CARTESIAN_POINT ( 'NONE',  ( 3.454253436624921569, -49.15858197120396511, 103.7259032015043090 ) ) ;
#21754=CIRCLE ( 'NONE', #14857, 7.000000000000006217 ) ;
#21767=EDGE_LOOP ( 'NONE', ( #90185, #8955, #91485, #87159 ) ) ;
#21809=AXIS2_PLACEMENT_3D ( 'NONE', #104423, #88259, #65028 ) ;
#21826=CARTESIAN_POINT ( 'NONE',  ( -10.25013302800875437, -12.02071073709907445, 17.45400528659170192 ) ) ;
#21828=CIRCLE ( 'NONE', #4551, 8.142857142857131691 ) ;
#21837=CARTESIAN_POINT ( 'NONE',  ( 1.558897133830167814, -49.97004945637518603, 44.88304531907225225 ) ) ;
#21868=EDGE_LOOP ( 'NONE', ( #93724, #55952, #52632, #98002 ) ) ;
#21873=UNCERTAINTY_MEASURE_WITH_UNIT (LENGTH_MEASURE( 1.000000000000000082E-05 ), #52105, 'distance_accuracy_value', 'NONE');
#21878=CARTESIAN_POINT ( 'NONE',  ( 0.000000000000000000, -54.00000000000000711, 27.00000000000000000 ) ) ;
#21907=( GEOMETRIC_REPRESENTATION_CONTEXT ( 3 ) GLOBAL_UNCERTAINTY_ASSIGNED_CONTEXT ( ( #83660 ) ) GLOBAL_UNIT_ASSIGNED_CONTEXT ( ( #67984, #11314, #58289 ) ) REPRESENTATION_CONTEXT ( 'NONE', 'WORKASPACE' ) );
#21911=EDGE_LOOP ( 'NONE', ( #75512, #52087, #48912, #1634, #85450, #94840, #65198, #21076, #53714, #13880, #86234 ) ) ;
#21917=FILL_AREA_STYLE ('',( #29492 ) ) ;
#21945=EDGE_CURVE ( 'NONE', #42316, #85095, #55941, .T. ) ;
#21951=CARTESIAN_POINT ( 'NONE',  ( 13.45079846400082957, -53.73420772973362602, 23.11721482942554573 ) ) ;
#21962=CARTESIAN_POINT ( 'NONE',  ( 3.857142857142850545, -1.200583151104938517, 103.1763305333244318 ) ) ;
#21998=ORIENTED_EDGE ( 'NONE', *, *, #95773, .F. ) ;
#22016=CARTESIAN_POINT ( 'NONE',  ( -9.149732096576093099, -3.297952640180834560, 14.67458069835285706 ) ) ;
#22024=EDGE_LOOP ( 'NONE', ( #62151, #22035, #55111, #74225, #101277 ) ) ;
#22032=ORIENTED_EDGE ( 'NONE', *, *, #12325, .T. ) ;
#22035=ORIENTED_EDGE ( 'NONE', *, *, #79066, .T. ) ;
#22045=CARTESIAN_POINT ( 'NONE',  ( 1.226845885076769616, -0.004855998333466520281, 101.2646151595213411 ) ) ;
#22067=FILL_AREA_STYLE ('',( #94890 ) ) ;
#22090=CARTESIAN_POINT ( 'NONE',  ( -8.621479322451524041, -1.224621629255531419, 15.49382773535086066 ) ) ;
#22118=CARTESIAN_POINT ( 'NONE',  ( -6.125000000000000000, -60.71953810597580059, 14.41094225130411033 ) ) ;
#22130=B_SPLINE_CURVE_WITH_KNOTS ( 'NONE', 3,
 ( #94052, #44446, #20214, #77341, #3452, #85988, #36398, #12059, #44989, #69784, #77874, #102137, #102676, #56753, #73468, #63820, #40586, #55680, #57281, #39547, #8214, #14703, #22317, #105327, #48661, #106363, #23912, #16304, #31988, #74007, #15247, #41123, #90204, #31470 ),
 .UNSPECIFIED., .F., .F.,
 ( 4, 2, 2, 2, 2, 2, 2, 2, 2, 2, 2, 2, 2, 2, 2, 2, 4 ),
 ( 6.938893903907228378E-18, 0.0007899780065504824781, 0.001579956013100958017, 0.002369934019651433448, 0.003159912026201909096, 0.003949890032752384310, 0.004739868039302859958, 0.005529846045853335605, 0.006319824052403811253, 0.007109802058954286900, 0.007899780065504761681, 0.008689758072055237328, 0.009479736078605712976, 0.01026971408515618862, 0.01105969209170666427, 0.01184967009825713992, 0.01263964810480761557 ),
 .UNSPECIFIED. ) ;
#22140=VERTEX_POINT ( 'NONE', #1945 ) ;
#22171=CARTESIAN_POINT ( 'NONE',  ( 5.000000000000000000, -19.72300213744072650, -4.527428753827365426 ) ) ;
#22210=CARTESIAN_POINT ( 'NONE',  ( -1.000000000000000000, -43.09265016209167953, 0.3552338647577958919 ) ) ;
#22219=DIRECTION ( 'NONE',  ( 0.000000000000000000, 1.224646799147353454E-16, 1.000000000000000000 ) ) ;
#22250=CARTESIAN_POINT ( 'NONE',  ( 1.000000000000000000, -68.32597503901369862, 12.04364623808666224 ) ) ;
#22281=SURFACE_STYLE_FILL_AREA ( #6051 ) ;
#22283=CARTESIAN_POINT ( 'NONE',  ( 0.000000000000000000, -4.000000000000003553, 123.0000000000000142 ) ) ;
#22317=CARTESIAN_POINT ( 'NONE',  ( -9.771805689013445928, -57.46313207252903510, 29.13556849961307194 ) ) ;
#22339=EDGE_CURVE ( 'NONE', #6033, #89992, #49187, .T. ) ;
#22343=CYLINDRICAL_SURFACE ( 'NONE', #33879, 14.00000000000000178 ) ;
#22388=ADVANCED_FACE ( 'NONE', ( #3565 ), #94166, .F. ) ;
#22407=AXIS2_PLACEMENT_3D ( 'NONE', #5118, #79523, #87109 ) ;
#22426=ORIENTED_EDGE ( 'NONE', *, *, #56017, .T. ) ;
#22460=DIRECTION ( 'NONE',  ( 0.000000000000000000, 0.000000000000000000, 1.000000000000000000 ) ) ;
#22516=LINE ( 'NONE', #102875, #102779 ) ;
#22528=B_SPLINE_CURVE_WITH_KNOTS ( 'NONE', 3,
 ( #60074, #91364, #100494, #26137, #9344, #93487, #17479, #83773, #59529, #68689, #19636, #27726, #19098, #51410, #42796, #50870, #84851, #26651, #10934, #52469, #697, #92397, #33664, #42256 ),
 .UNSPECIFIED., .F., .F.,
 ( 4, 2, 2, 2, 2, 2, 2, 2, 2, 2, 2, 4 ),
 ( 0.000000000000000000, 0.0009738897914509524363, 0.001947779582901903572, 0.003895559165803803674, 0.004869448957254753074, 0.005843338748705703342, 0.007791118331607603011, 0.009738897914509502679, 0.01168667749741140321, 0.01363445708031330375, 0.01460834687176425575, 0.01558223666321520776 ),
 .UNSPECIFIED. ) ;
#22564=CARTESIAN_POINT ( 'NONE',  ( -11.36340450468866337, -9.490057094874892130, 18.81418650344063792 ) ) ;
#22610=ORIENTED_EDGE ( 'NONE', *, *, #4729, .T. ) ;
#22613=SURFACE_STYLE_USAGE ( .BOTH. , #14999 ) ;
#22634=EDGE_LOOP ( 'NONE', ( #42892, #1421, #59889, #46876 ) ) ;
#22640=CARTESIAN_POINT ( 'NONE',  ( -30.00000000000000000, 0.000000000000000000, -13.00000000000000000 ) ) ;
#22657=CARTESIAN_POINT ( 'NONE',  ( -5.000000000000039968, -13.16121988547070742, 12.48675270919698299 ) ) ;
#22690=CARTESIAN_POINT ( 'NONE',  ( 4.369287899246201867, -48.87003977535613330, 104.3947014718172142 ) ) ;
#22767=EDGE_CURVE ( 'NONE', #95128, #12254, #99137, .T. ) ;
#22778=FACE_OUTER_BOUND ( 'NONE', #42887, .T. ) ;
#22801=CARTESIAN_POINT ( 'NONE',  ( 3.348045142843516064, -48.90720247195245207, 104.4613934866187179 ) ) ;
#22811=CARTESIAN_POINT ( 'NONE',  ( 5.000000000000000888, -70.02076148470872852, 13.01198664878534750 ) ) ;
#22814=CARTESIAN_POINT ( 'NONE',  ( 11.55222000106535063, -8.857086686608768744, 19.08603404707153217 ) ) ;
#22841=( GEOMETRIC_REPRESENTATION_CONTEXT ( 3 ) GLOBAL_UNCERTAINTY_ASSIGNED_CONTEXT ( ( #41927 ) ) GLOBAL_UNIT_ASSIGNED_CONTEXT ( ( #10877, #77231, #28719 ) ) REPRESENTATION_CONTEXT ( 'NONE', 'WORKASPACE' ) );
#22847=CARTESIAN_POINT ( 'NONE',  ( -3.454253436624922458, -49.15858197120396511, 103.7259032015043090 ) ) ;
#22870=SURFACE_SIDE_STYLE ('',( #81060 ) ) ;
#22880=CARTESIAN_POINT ( 'NONE',  ( -1.000000000000000000, -40.48763664056765776, -0.7135409870776373564 ) ) ;
#22885=CARTESIAN_POINT ( 'NONE',  ( -4.738695502753807354, -47.42796447909066160, 42.87913045825063563 ) ) ;
#22922=B_SPLINE_CURVE_WITH_KNOTS ( 'NONE', 3,
 ( #74945, #48550, #72823, #48014, #80924, #32940, #99768, #56642, #99221, #81439, #16189, #57694, #90085, #33463 ),
 .UNSPECIFIED., .F., .F.,
 ( 4, 2, 2, 2, 2, 2, 4 ),
 ( -2.637499479246189856E-05, 0.003621852776081119999, 0.007270080546954701961, 0.009094194432391494026, 0.01091830831782828436, 0.01274242220326507642, 0.01456653608870186675 ),
 .UNSPECIFIED. ) ;
#22944=ORIENTED_EDGE ( 'NONE', *, *, #78118, .F. ) ;
#22957=CARTESIAN_POINT ( 'NONE',  ( 10.92337230437442841, 2.452739325026194628, 14.79856046833763727 ) ) ;
#22969=FILL_AREA_STYLE_COLOUR ( '', #12448 ) ;
#22974=CARTESIAN_POINT ( 'NONE',  ( -3.932591042162086215, -69.40053737951669177, 13.56259061519041964 ) ) ;
#22994=( LENGTH_UNIT ( ) NAMED_UNIT ( * ) SI_UNIT ( .MILLI., .METRE. ) );
#23026=CARTESIAN_POINT ( 'NONE',  ( 0.3074911254280547346, -69.98475940929637318, 12.98938480846820909 ) ) ;
#23038=DIRECTION ( 'NONE',  ( 0.000000000000000000, -0.9371777605526921961, -0.3488521823429527879 ) ) ;
#23045=AXIS2_PLACEMENT_3D ( 'NONE', #71279, #6006, #38930 ) ;
#23073=( LENGTH_UNIT ( ) NAMED_UNIT ( * ) SI_UNIT ( .MILLI., .METRE. ) );
#23090=CIRCLE ( 'NONE', #17989, 4.000000000000002665 ) ;
#23120=CARTESIAN_POINT ( 'NONE',  ( -3.668358303306872958, -48.89638946469894876, 104.6014313550541175 ) ) ;
#23130=( LENGTH_UNIT ( ) NAMED_UNIT ( * ) SI_UNIT ( .MILLI., .METRE. ) );
#23153=( LENGTH_UNIT ( ) NAMED_UNIT ( * ) SI_UNIT ( .MILLI., .METRE. ) );
#23156=TOROIDAL_SURFACE ( 'NONE', #35242, 8.000000000000000000, 4.000000000000000000 ) ;
#23175=CARTESIAN_POINT ( 'NONE',  ( -5.990115786909033346, -12.91256367767457647, 13.08452859117697642 ) ) ;
#23197=STYLED_ITEM ( 'NONE', ( #17050 ), #55728 ) ;
#23241=CARTESIAN_POINT ( 'NONE',  ( -9.612665144396085992, -50.98869060647467677, 29.76292019730385618 ) ) ;
#23264=CARTESIAN_POINT ( 'NONE',  ( -4.781335833249817036, -47.33012453287045673, 102.4226025779373401 ) ) ;
#23269=UNCERTAINTY_MEASURE_WITH_UNIT (LENGTH_MEASURE( 1.000000000000000082E-05 ), #62595, 'distance_accuracy_value', 'NONE');
#23272=COLOUR_RGB ( '', 0.31764706, 0.68627451, 0.89019608) ;
#23295=CARTESIAN_POINT ( 'NONE',  ( -12.14072642854974760, 2.000560067487730631, 14.86685304370069538 ) ) ;
#23328=CARTESIAN_POINT ( 'NONE',  ( -3.396360046677147970, -0.8468429378656776585, 103.9790200242172062 ) ) ;
#23333=CARTESIAN_POINT ( 'NONE',  ( 5.000000000000000000, -14.29136116388517941, -6.556186629969792179 ) ) ;
#23361=CARTESIAN_POINT ( 'NONE',  ( -5.000000000000000888, -46.00000000000000000, 42.58845726811989607 ) ) ;
#23411=CARTESIAN_POINT ( 'NONE',  ( -4.825525552038038235, -47.21979206537751139, 40.34253552477181159 ) ) ;
#23432=SURFACE_STYLE_USAGE ( .BOTH. , #57875 ) ;
#23464=CARTESIAN_POINT ( 'NONE',  ( 0.000000000000000000, -4.000000000000000000, 27.00000000000000000 ) ) ;
#23487=FILL_AREA_STYLE ('',( #97333 ) ) ;
#23489=SURFACE_STYLE_USAGE ( .BOTH. , #103841 ) ;
#23505=CARTESIAN_POINT ( 'NONE',  ( -3.578772014706478544, -68.26502216367026676, 13.09484892523241228 ) ) ;
#23518=TOROIDAL_SURFACE ( 'NONE', #83744, 17.00000000000000000, 2.000000000000000000 ) ;
#23529=B_SPLINE_CURVE_WITH_KNOTS ( 'NONE', 3,
 ( #79313, #5436, #15633, #42039, #48526, #25916, #9128, #74920, #8074, #24300, #24821, #33443, #99198, #81417, #57673, #57149, #40446, #91669, #7528, #40982, #90596, #16706, #90062, #73326 ),
 .UNSPECIFIED., .F., .F.,
 ( 4, 2, 2, 2, 2, 2, 2, 2, 2, 2, 2, 4 ),
 ( 2.213902055206457488E-15, 0.002700571958308535525, 0.004050857937461695667, 0.005401143916614856676, 0.006751429895768016817, 0.007426572885344616404, 0.008101715874921215990, 0.008776858864497815577, 0.009452001854074415163, 0.009789573348862707150, 0.01012714484365099567, 0.01080228783322758311 ),
 .UNSPECIFIED. ) ;
#23565=( NAMED_UNIT ( * ) SI_UNIT ( $, .STERADIAN. ) SOLID_ANGLE_UNIT ( ) );
#23577=COLOUR_RGB ( '', 0.31764706, 0.68627451, 0.89019608) ;
#23608=CARTESIAN_POINT ( 'NONE',  ( -2.720100412697608494, -69.18718729000897838, 12.97654704113952384 ) ) ;
#23609=CARTESIAN_POINT ( 'NONE',  ( -5.000000000000000000, -32.50000000000000000, 13.00000000000000178 ) ) ;
#23614=CARTESIAN_POINT ( 'NONE',  ( 4.642888266381832274, -47.65716784818645380, 102.5319024079573751 ) ) ;
#23623=EDGE_CURVE ( 'NONE', #102776, #214, #45893, .T. ) ;
#23640=CARTESIAN_POINT ( 'NONE',  ( -4.642888266381816287, -47.65716784818648222, 102.5319024079587393 ) ) ;
#23673=CARTESIAN_POINT ( 'NONE',  ( -5.833333333333328596, -46.00000000000000000, 103.8776713793258608 ) ) ;
#23682=LINE ( 'NONE', #88923, #45769 ) ;
#23706=( GEOMETRIC_REPRESENTATION_CONTEXT ( 3 ) GLOBAL_UNCERTAINTY_ASSIGNED_CONTEXT ( ( #59125 ) ) GLOBAL_UNIT_ASSIGNED_CONTEXT ( ( #25521, #50792, #51336 ) ) REPRESENTATION_CONTEXT ( 'NONE', 'WORKASPACE' ) );
#23711=CARTESIAN_POINT ( 'NONE',  ( -5.000000000000000000, -14.98862091075374003, 12.50620160667438263 ) ) ;
#23719=CARTESIAN_POINT ( 'NONE',  ( 2.103764093714755923, -49.85092038520011215, 102.1576470924498210 ) ) ;
#23761=ORIENTED_EDGE ( 'NONE', *, *, #64252, .F. ) ;
#23779=CARTESIAN_POINT ( 'NONE',  ( 27.99999999999999645, 0.000000000000000000, 0.000000000000000000 ) ) ;
#23783=AXIS2_PLACEMENT_3D ( 'NONE', #5614, #42757, #9309 ) ;
#23793=CARTESIAN_POINT ( 'NONE',  ( 5.232798140227933104, -48.02337292624942222, 104.1190344879413914 ) ) ;
#23838=( NAMED_UNIT ( * ) PLANE_ANGLE_UNIT ( ) SI_UNIT ( $, .RADIAN. ) );
#23851=CARTESIAN_POINT ( 'NONE',  ( 8.572527594031475162E-16, -4.000000000000003553, 105.0000000000000000 ) ) ;
#23868=( GEOMETRIC_REPRESENTATION_CONTEXT ( 3 ) GLOBAL_UNCERTAINTY_ASSIGNED_CONTEXT ( ( #82853 ) ) GLOBAL_UNIT_ASSIGNED_CONTEXT ( ( #93826, #79222, #53364 ) ) REPRESENTATION_CONTEXT ( 'NONE', 'WORKASPACE' ) );
#23874=CARTESIAN_POINT ( 'NONE',  ( 9.269408785705698151, -55.04596499575451674, 23.24750950774772562 ) ) ;
#23881=FILL_AREA_STYLE ('',( #7638 ) ) ;
#23905=CARTESIAN_POINT ( 'NONE',  ( -5.559241731430971889, -51.12552554554342521, 39.84970532565870371 ) ) ;
#23908=ORIENTED_EDGE ( 'NONE', *, *, #95507, .F. ) ;
#23912=CARTESIAN_POINT ( 'NONE',  ( -9.442395496852061143, -56.44162292811314074, 30.29618450995123169 ) ) ;
#23925=CARTESIAN_POINT ( 'NONE',  ( 4.448407490268952991, -1.969035902430321894, 102.6871849564181360 ) ) ;
#24044=CARTESIAN_POINT ( 'NONE',  ( -6.125000000000000000, -60.71953810597579348, 14.41094225130411033 ) ) ;
#24045=STYLED_ITEM ( 'NONE', ( #47889 ), #90435 ) ;
#24056=ADVANCED_FACE ( 'NONE', ( #84242 ), #59994, .T. ) ;
#24101=CARTESIAN_POINT ( 'NONE',  ( 5.000000000001647571, -60.71953810597887014, 13.86359191440508809 ) ) ;
#24109=CARTESIAN_POINT ( 'NONE',  ( 4.781335833249817036, -47.33012453287044252, 102.4226025779373259 ) ) ;
#24122=CARTESIAN_POINT ( 'NONE',  ( -4.586789253316293724, -2.224716758486289692, 102.5764008378948091 ) ) ;
#24149=CARTESIAN_POINT ( 'NONE',  ( 6.022743854525181462, -12.63762613047081196, 12.76172509297427027 ) ) ;
#24154=CARTESIAN_POINT ( 'NONE',  ( 5.437321008177347537, -47.65716784822890162, 104.0362115404844729 ) ) ;
#24183=CARTESIAN_POINT ( 'NONE',  ( -4.551587301587289858, -48.79941684889506348, 104.4018401814738013 ) ) ;
#24187=CARTESIAN_POINT ( 'NONE',  ( 1.234146493305849468, -49.99999999999999289, 101.3393031322932245 ) ) ;
#24198=DIRECTION ( 'NONE',  ( 0.8257009859295948440, 0.000000000000000000, -0.5641080409238066196 ) ) ;
#24205=AXIS2_PLACEMENT_3D ( 'NONE', #18984, #101978, #87932 ) ;
#24248=CARTESIAN_POINT ( 'NONE',  ( -4.999999999999960032, -13.35938963217072128, 12.71467713436390667 ) ) ;
#24278=EDGE_CURVE ( 'NONE', #41862, #104941, #28849, .T. ) ;
#24300=CARTESIAN_POINT ( 'NONE',  ( 3.958819230456402050, -67.57662422979727523, 13.13288867614480182 ) ) ;
#24307=ORIENTED_EDGE ( 'NONE', *, *, #28464, .F. ) ;
#24339=EDGE_CURVE ( 'NONE', #47025, #102776, #90847, .T. ) ;
#24354=CIRCLE ( 'NONE', #79450, 2.000000000000001332 ) ;
#24366=CARTESIAN_POINT ( 'NONE',  ( -13.81782546013763024, 1.033440728989090340, 14.96496143817082647 ) ) ;
#24375=ORIENTED_EDGE ( 'NONE', *, *, #96113, .T. ) ;
#24406=FILL_AREA_STYLE ('',( #97709 ) ) ;
#24413=CARTESIAN_POINT ( 'NONE',  ( 14.04065140978712911, -8.435331075557439107, 12.41598592279226310 ) ) ;
#24420=CARTESIAN_POINT ( 'NONE',  ( -1.509171067930827448, -49.97508125504521814, 101.6143504438094283 ) ) ;
#24442=CARTESIAN_POINT ( 'NONE',  ( -2.404214652066591906, -53.72754880671013211, 40.79389177775365738 ) ) ;
#24448=CARTESIAN_POINT ( 'NONE',  ( -3.347995242091437174, -48.90830061040438181, 104.4601902487057998 ) ) ;
#24457=CARTESIAN_POINT ( 'NONE',  ( 4.861072549008416566, -2.920843450830509891, 102.3606070684416807 ) ) ;
#24499=STYLED_ITEM ( 'NONE', ( #79632 ), #104485 ) ;
#24512=CARTESIAN_POINT ( 'NONE',  ( -4.744389013293895729, -1.372925465831638769, 104.3204960233004357 ) ) ;
#24572=CARTESIAN_POINT ( 'NONE',  ( -5.000000000000000000, -60.71953810597472767, 12.61250543006392988 ) ) ;
#24622=CARTESIAN_POINT ( 'NONE',  ( 6.393725729381808165, -15.50592724712675086, 14.54168635664702514 ) ) ;
#24632=COLOUR_RGB ( '', 0.40784314, 0.44705882, 0.49803922) ;
#24646=UNCERTAINTY_MEASURE_WITH_UNIT (LENGTH_MEASURE( 1.000000000000000082E-05 ), #17419, 'distance_accuracy_value', 'NONE');
#24653=CARTESIAN_POINT ( 'NONE',  ( 6.282481257750461623, -11.96849729169402998, 11.22390784433575206 ) ) ;
#24671=CARTESIAN_POINT ( 'NONE',  ( 10.51384838036216784, -0.8794359877124720004, 20.22631812719205868 ) ) ;
#24703=CARTESIAN_POINT ( 'NONE',  ( -4.586789253316107207, -47.77528324151405315, 102.5764008378948091 ) ) ;
#24712=UNCERTAINTY_MEASURE_WITH_UNIT (LENGTH_MEASURE( 1.000000000000000082E-05 ), #85782, 'distance_accuracy_value', 'NONE');
#24743=STYLED_ITEM ( 'NONE', ( #61916 ), #84820 ) ;
#24770=CARTESIAN_POINT ( 'NONE',  ( -4.999999999999921840, -12.28614229754770193, 10.41767341469734376 ) ) ;
#24790=CARTESIAN_POINT ( 'NONE',  ( 15.31300439044785655, -0.5304010509286816166, 14.99217175782056444 ) ) ;
#24821=CARTESIAN_POINT ( 'NONE',  ( 3.858655471090992162, -67.78341364078379172, 13.12478365188160367 ) ) ;
#24827=SURFACE_SIDE_STYLE ('',( #89546 ) ) ;
#24829=CARTESIAN_POINT ( 'NONE',  ( 9.204646778667628482, -52.70222288520290022, 30.90975160907398234 ) ) ;
#24830=( NAMED_UNIT ( * ) SI_UNIT ( $, .STERADIAN. ) SOLID_ANGLE_UNIT ( ) );
#24840=ORIENTED_EDGE ( 'NONE', *, *, #49869, .F. ) ;
#24842=CARTESIAN_POINT ( 'NONE',  ( 5.371950044183567030, -47.79483119409569980, 104.0625755208173473 ) ) ;
#24878=DIRECTION ( 'NONE',  ( -0.000000000000000000, -1.000000000000000000, -0.000000000000000000 ) ) ;
#24891=MECHANICAL_DESIGN_GEOMETRIC_PRESENTATION_REPRESENTATION('',(#97153),#98841);
#24920=STYLED_ITEM ( 'NONE', ( #74172 ), #18564 ) ;
#24922=CARTESIAN_POINT ( 'NONE',  ( 9.677640526858340309, -57.01362214985471155, 24.47418066717162333 ) ) ;
#24928=CARTESIAN_POINT ( 'NONE',  ( 5.000000000000000888, -32.16482459200685184, -4.060956965592712464 ) ) ;
#24930=SURFACE_STYLE_USAGE ( .BOTH. , #32497 ) ;
#24938=CARTESIAN_POINT ( 'NONE',  ( -3.870939636683351726, -48.78526580464421869, 104.2727580839183190 ) ) ;
#24955=CARTESIAN_POINT ( 'NONE',  ( -4.210633177350923795, -52.69376427780586170, 40.35640560465288473 ) ) ;
#24967=CARTESIAN_POINT ( 'NONE',  ( -3.505888691173200566, -0.8815391977514219768, 103.6125332151819975 ) ) ;
#24972=MECHANICAL_DESIGN_GEOMETRIC_PRESENTATION_REPRESENTATION('',(#28454),#102409);
#24982=AXIS2_PLACEMENT_3D ( 'NONE', #38623, #61298, #62368 ) ;
#25030=CARTESIAN_POINT ( 'NONE',  ( -4.524610880512274669, -11.34578236400882112, -9.835134842096833196 ) ) ;
#25077=EDGE_LOOP ( 'NONE', ( #42233, #105740, #57018, #55842 ) ) ;
#25080=CARTESIAN_POINT ( 'NONE',  ( -15.79974202274673090, -1.614185661296035468, 14.91351826467123587 ) ) ;
#25083=CARTESIAN_POINT ( 'NONE',  ( 6.999999999999999112, 0.000000000000000000, 0.000000000000000000 ) ) ;
#25089=SURFACE_STYLE_USAGE ( .BOTH. , #81160 ) ;
#25094=CARTESIAN_POINT ( 'NONE',  ( -4.410865297923724171, -68.79849255806507813, 13.71221591202026246 ) ) ;
#25102=( NAMED_UNIT ( * ) SI_UNIT ( $, .STERADIAN. ) SOLID_ANGLE_UNIT ( ) );
#25113=B_SPLINE_CURVE_WITH_KNOTS ( 'NONE', 3,
 ( #30148, #7419, #64624, #39297, #81306, #23120, #63032, #54914 ),
 .UNSPECIFIED., .F., .F.,
 ( 4, 2, 2, 4 ),
 ( 0.000000000000000000, 0.0002494395879357617159, 0.0004988791758715234318, 0.0009977583517430481646 ),
 .UNSPECIFIED. ) ;
#25130=FACE_OUTER_BOUND ( 'NONE', #72917, .T. ) ;
#25134=CARTESIAN_POINT ( 'NONE',  ( -5.000000000000000888, -51.57177412348296031, 8.340224860101702831 ) ) ;
#25147=CARTESIAN_POINT ( 'NONE',  ( -1.000000000001111777, -69.59657292934927852, 12.76848391599230759 ) ) ;
#25157=CARTESIAN_POINT ( 'NONE',  ( 0.000000000000000000, -80.00000000000000000, 41.00000000000000000 ) ) ;
#25159=CARTESIAN_POINT ( 'NONE',  ( 1.372706959323941156, -69.65664221933762690, 12.80275162964094804 ) ) ;
#25188=CARTESIAN_POINT ( 'NONE',  ( 5.978750298146925601, -13.03636037196968367, 13.21647969580668480 ) ) ;
#25202=COLOUR_RGB ( '', 0.72549020, 0.75294118, 0.79215686) ;
#25205=AXIS2_PLACEMENT_3D ( 'NONE', #7624, #99840, #65356 ) ;
#25211=VERTEX_POINT ( 'NONE', #144 ) ;
#25212=CARTESIAN_POINT ( 'NONE',  ( 4.526657684027820316, -47.90665221903877580, 103.5746540667394555 ) ) ;
#25229=CYLINDRICAL_SURFACE ( 'NONE', #81080, 9.999999999999998224 ) ;
#25243=CARTESIAN_POINT ( 'NONE',  ( -5.688569873206840377, -47.04879514976369137, 103.9352763293500743 ) ) ;
#25250=CARTESIAN_POINT ( 'NONE',  ( 27.99999999999999645, 0.000000000000000000, 0.000000000000000000 ) ) ;
#25256=FILL_AREA_STYLE ('',( #90493 ) ) ;
#25264=CIRCLE ( 'NONE', #21809, 9.999999999999998224 ) ;
#25309=CARTESIAN_POINT ( 'NONE',  ( 0.7777777777777741264, -54.00000000000000711, 40.97837836547555668 ) ) ;
#25312=CARTESIAN_POINT ( 'NONE',  ( -3.857142857142847880, -48.79941684889506348, 103.1763305333244318 ) ) ;
#25328=CARTESIAN_POINT ( 'NONE',  ( 12.82656847843611203, 1.661299769047218655, 14.90831243661676631 ) ) ;
#25338=( BOUNDED_SURFACE ( )  B_SPLINE_SURFACE ( 3, 2, ( 
 ( #82613, #48630, #97191 ),
 ( #64837, #38980, #57 ),
 ( #56176, #90172, #15747 ),
 ( #65893, #40556, #73439 ),
 ( #7115, #89116, #41093 ),
 ( #15213, #106333, #22814 ),
 ( #16275, #40031, #55648 ),
 ( #24413, #14665, #47575 ),
 ( #57252, #39515, #105294 ),
 ( #31440, #9239, #58885 ),
 ( #83655, #43221, #67502 ),
 ( #76104, #92279, #50750 ),
 ( #2744, #9769, #2205 ),
 ( #19523, #35153, #26546 ),
 ( #83142, #10825, #58334 ),
 ( #59959, #27077, #51290 ),
 ( #84210, #10305, #68022 ),
 ( #74507, #91776, #27612 ),
 ( #66972, #100909, #42682 ),
 ( #100384, #42144, #91257 ) ),
 .UNSPECIFIED., .F., .F., .F. ) 
 B_SPLINE_SURFACE_WITH_KNOTS ( ( 4, 2, 2, 2, 2, 2, 2, 2, 2, 4 ),
 ( 3, 3 ),
 ( 0.06021901822288649314, 0.06247022664829056382, 0.06472143507369462756, 0.06697264349909869130, 0.06922385192450275504, 0.07147506034990681878, 0.07260066456260885759, 0.07372626877531088252, 0.07597747720071496014, 0.07822868562611902388 ),
 ( 0.000000000000000000, 1.000000000000000000 ),
 .UNSPECIFIED. ) 
 GEOMETRIC_REPRESENTATION_ITEM ( )  RATIONAL_B_SPLINE_SURFACE ( (
 ( 1.000000000000000000, 0.5207636911093219689, 1.000000000000000000),
 ( 1.000000000000000000, 0.5185382483914372509, 1.000000000000000000),
 ( 1.000000000000000000, 0.5157170609726789978, 1.000000000000000000),
 ( 1.000000000000000000, 0.5095464177491236812, 1.000000000000000000),
 ( 1.000000000000000000, 0.5062011784965128047, 1.000000000000000000),
 ( 1.000000000000000000, 0.4995824849051648808, 1.000000000000000000),
 ( 1.000000000000000000, 0.4963024291608688077, 1.000000000000000000),
 ( 1.000000000000000000, 0.4905153737246681911, 1.000000000000000000),
 ( 1.000000000000000000, 0.4880809317982532369, 1.000000000000000000),
 ( 1.000000000000000000, 0.4846011406799364818, 1.000000000000000000),
 ( 1.000000000000000000, 0.4835584709197799369, 1.000000000000000000),
 ( 1.000000000000000000, 0.4832073097951730123, 1.000000000000000000),
 ( 1.000000000000000000, 0.4832927473445461919, 1.000000000000000000),
 ( 1.000000000000000000, 0.4838416877134147365, 1.000000000000000000),
 ( 1.000000000000000000, 0.4843037014696224829, 1.000000000000000000),
 ( 1.000000000000000000, 0.4861738658104473587, 1.000000000000000000),
 ( 1.000000000000000000, 0.4880704143552366814, 1.000000000000000000),
 ( 1.000000000000000000, 0.4926074442002630338, 1.000000000000000000),
 ( 1.000000000000000000, 0.4952473214787204703, 1.000000000000000000),
 ( 1.000000000000000000, 0.4978121763378770548, 1.000000000000000000) ) ) 
 REPRESENTATION_ITEM ( '' )  SURFACE ( )  );
#25341=SURFACE_SIDE_STYLE ('',( #99179 ) ) ;
#25378=CARTESIAN_POINT ( 'NONE',  ( 7.000000000000000000, -14.21727251090713828, 9.320362779989000757 ) ) ;
#25397=CARTESIAN_POINT ( 'NONE',  ( -9.118966701651679330, -0.3497226616077714345, 19.74305553042258055 ) ) ;
#25416=VERTEX_POINT ( 'NONE', #7070 ) ;
#25461=ORIENTED_EDGE ( 'NONE', *, *, #32033, .F. ) ;
#25482=( NAMED_UNIT ( * ) PLANE_ANGLE_UNIT ( ) SI_UNIT ( $, .RADIAN. ) );
#25518=EDGE_CURVE ( 'NONE', #87879, #34686, #78657, .T. ) ;
#25521=( LENGTH_UNIT ( ) NAMED_UNIT ( * ) SI_UNIT ( .MILLI., .METRE. ) );
#25537=AXIS2_PLACEMENT_3D ( 'NONE', #40904, #16092, #73789 ) ;
#25539=FILL_AREA_STYLE_COLOUR ( '', #13349 ) ;
#25579=CARTESIAN_POINT ( 'NONE',  ( -5.833333333333328596, -4.000000000000003553, 103.8776713793258608 ) ) ;
#25588=CARTESIAN_POINT ( 'NONE',  ( 3.454253436624935336, -0.8414180287960453253, 103.7259032015043232 ) ) ;
#25606=CARTESIAN_POINT ( 'NONE',  ( 1.116646360188462639, -0.001721104702690063248, 101.1925744066307402 ) ) ;
#25609=CARTESIAN_POINT ( 'NONE',  ( 27.99999999999999645, 0.000000000000000000, 9.000000000000000000 ) ) ;
#25614=SURFACE_SIDE_STYLE ('',( #8843 ) ) ;
#25625=SURFACE_STYLE_USAGE ( .BOTH. , #68166 ) ;
#25628=MECHANICAL_DESIGN_GEOMETRIC_PRESENTATION_REPRESENTATION('',(#11788),#4955);
#25632=SURFACE_SIDE_STYLE ('',( #33700 ) ) ;
#25661=FACE_OUTER_BOUND ( 'NONE', #66673, .T. ) ;
#25682=FILL_AREA_STYLE ('',( #17024 ) ) ;
#25684=CARTESIAN_POINT ( 'NONE',  ( -4.999999999999999112, -46.02080548338511790, 5.909847384900872136 ) ) ;
#25687=COLOUR_RGB ( '', 0.31764706, 0.68627451, 0.89019608) ;
#25712=CARTESIAN_POINT ( 'NONE',  ( 4.899502675980784261, -65.60435911681314280, 13.86139633465681698 ) ) ;
#25715=( LENGTH_UNIT ( ) NAMED_UNIT ( * ) SI_UNIT ( .MILLI., .METRE. ) );
#25743=CARTESIAN_POINT ( 'NONE',  ( 5.000000000000000000, -15.62228920881129746, 12.61250543006183733 ) ) ;
#25797=ORIENTED_EDGE ( 'NONE', *, *, #105393, .F. ) ;
#25799=CARTESIAN_POINT ( 'NONE',  ( 4.551587301587304957, -1.200583151104947843, 104.4018401814738155 ) ) ;
#25820=LINE ( 'NONE', #67822, #9321 ) ;
#25854=DIRECTION ( 'NONE',  ( -2.742080092235280244E-17, 0.000000000000000000, 1.000000000000000000 ) ) ;
#25863=VERTEX_POINT ( 'NONE', #95436 ) ;
#25905=EDGE_CURVE ( 'NONE', #33663, #85296, #31266, .T. ) ;
#25916=CARTESIAN_POINT ( 'NONE',  ( 4.671142383340135318, -65.18523764613235016, 13.09013483307534464 ) ) ;
#25919=EDGE_CURVE ( 'NONE', #101089, #6033, #103006, .T. ) ;
#25976=DIRECTION ( 'NONE',  ( 0.000000000000000000, 0.000000000000000000, 1.000000000000000000 ) ) ;
#25979=CARTESIAN_POINT ( 'NONE',  ( -3.857142857142847880, -48.79941684889506348, 103.1763305333244176 ) ) ;
#25999=CARTESIAN_POINT ( 'NONE',  ( -5.000000000000000888, -15.25486520280274050, 12.58693527119031330 ) ) ;
#26016=CARTESIAN_POINT ( 'NONE',  ( -3.405129524038740474, -1.148734789949058976, 104.5473292663561864 ) ) ;
#26021=DIRECTION ( 'NONE',  ( 0.000000000000000000, 1.000000000000000000, 0.000000000000000000 ) ) ;
#26030=FILL_AREA_STYLE_COLOUR ( '', #49025 ) ;
#26046=CARTESIAN_POINT ( 'NONE',  ( 5.000000000000000000, -34.80405935700601816, 1.298618523705024952 ) ) ;
#26049=CARTESIAN_POINT ( 'NONE',  ( -6.312904226987146927, -49.68714783853175732, 39.49778964097281175 ) ) ;
#26068=CARTESIAN_POINT ( 'NONE',  ( -4.284822031654962338, -1.092833614412279220, 104.4267991316945086 ) ) ;
#26086=EDGE_CURVE ( 'NONE', #88866, #3905, #59826, .T. ) ;
#26119=CARTESIAN_POINT ( 'NONE',  ( 1.000000000000000000, -56.57158839599533451, 6.200363299250661875 ) ) ;
#26122=CARTESIAN_POINT ( 'NONE',  ( -6.547363650393914547, -12.76646305665534342, -7.895817423510182564 ) ) ;
#26137=CARTESIAN_POINT ( 'NONE',  ( 15.68577251487070612, -4.397129302180654342, 14.34458040922159583 ) ) ;
#26150=UNCERTAINTY_MEASURE_WITH_UNIT (LENGTH_MEASURE( 1.000000000000000082E-05 ), #82847, 'distance_accuracy_value', 'NONE');
#26153=CARTESIAN_POINT ( 'NONE',  ( -3.396360046677566746, -49.15315706213335289, 103.9790200242205032 ) ) ;
#26172=EDGE_LOOP ( 'NONE', ( #39564, #71684, #92179, #19403 ) ) ;
#26191=CARTESIAN_POINT ( 'NONE',  ( 3.567967761885403544, -49.07022467159661971, 103.4762329555118612 ) ) ;
#26201=CIRCLE ( 'NONE', #50243, 2.000000000000000000 ) ;
#26217=SURFACE_SIDE_STYLE ('',( #99507 ) ) ;
#26242=CARTESIAN_POINT ( 'NONE',  ( 3.096124615231415245, -69.43176308602586744, 13.34236499254138408 ) ) ;
#26250=CIRCLE ( 'NONE', #39985, 2.000000000000000000 ) ;
#26270=CARTESIAN_POINT ( 'NONE',  ( 5.962730926219388827, -13.90752838006108227, 13.89020537730394622 ) ) ;
#26281=( GEOMETRIC_REPRESENTATION_CONTEXT ( 3 ) GLOBAL_UNCERTAINTY_ASSIGNED_CONTEXT ( ( #56931 ) ) GLOBAL_UNIT_ASSIGNED_CONTEXT ( ( #49252, #47663, #16362 ) ) REPRESENTATION_CONTEXT ( 'NONE', 'WORKASPACE' ) );
#26302=EDGE_LOOP ( 'NONE', ( #92538, #73179, #29945, #11326 ) ) ;
#26304=VERTEX_POINT ( 'NONE', #37116 ) ;
#26346=DIRECTION ( 'NONE',  ( 0.000000000000000000, 1.000000000000000000, 0.000000000000000000 ) ) ;
#26354=CARTESIAN_POINT ( 'NONE',  ( 0.000000000000000000, -50.00000000000000000, 112.0000000000000000 ) ) ;
#26365=ORIENTED_EDGE ( 'NONE', *, *, #27257, .T. ) ;
#26385=CARTESIAN_POINT ( 'NONE',  ( -3.991107381396968634, -1.050392363564321307, 104.5611067885113386 ) ) ;
#26409=CARTESIAN_POINT ( 'NONE',  ( 10.79499483409554550, -1.039388583189924775, 20.32137925714343751 ) ) ;
#26465=CARTESIAN_POINT ( 'NONE',  ( -9.480263010783763988, -0.4492663453375149163, 19.86871132324680289 ) ) ;
#26491=FACE_OUTER_BOUND ( 'NONE', #55277, .T. ) ;
#26536=TOROIDAL_SURFACE ( 'NONE', #98767, 11.00000000000000533, 4.000000000000000000 ) ;
#26538=CARTESIAN_POINT ( 'NONE',  ( -3.707709148203271354, -1.099523832062968998, 104.5934084724869564 ) ) ;
#26541=LINE ( 'NONE', #49703, #27174 ) ;
#26546=CARTESIAN_POINT ( 'NONE',  ( 8.659875471883962561, -13.99571786196214340, 15.99679319869066418 ) ) ;
#26575=CARTESIAN_POINT ( 'NONE',  ( 2.519529083135078729, -49.57861714554732657, 103.1541576364171817 ) ) ;
#26588=DIRECTION ( 'NONE',  ( 0.000000000000000000, 1.000000000000000000, 0.000000000000000000 ) ) ;
#26632=MECHANICAL_DESIGN_GEOMETRIC_PRESENTATION_REPRESENTATION('',(#55826),#76553);
#26635=EDGE_CURVE ( 'NONE', #64161, #90150, #74367, .T. ) ;
#26636=CARTESIAN_POINT ( 'NONE',  ( 3.626288723285810534, -1.044241108143921126, 104.3502830461760880 ) ) ;
#26651=CARTESIAN_POINT ( 'NONE',  ( 9.865311185090694934, -11.68002284843480787, 9.419147808596591176 ) ) ;
#26673=SURFACE_STYLE_USAGE ( .BOTH. , #6313 ) ;
#26678=CARTESIAN_POINT ( 'NONE',  ( 0.000000000000000000, -46.00000000000000000, 112.0000000000000000 ) ) ;
#26693=( GEOMETRIC_REPRESENTATION_CONTEXT ( 3 ) GLOBAL_UNCERTAINTY_ASSIGNED_CONTEXT ( ( #104097 ) ) GLOBAL_UNIT_ASSIGNED_CONTEXT ( ( #60796, #85605, #4144 ) ) REPRESENTATION_CONTEXT ( 'NONE', 'WORKASPACE' ) );
#26717=ADVANCED_FACE ( 'NONE', ( #64168 ), #104598, .T. ) ;
#26719=CARTESIAN_POINT ( 'NONE',  ( 0.7777777777777733492, -50.00000000000000711, 40.97837836547554957 ) ) ;
#26767=CARTESIAN_POINT ( 'NONE',  ( 3.583116682864208258, -68.97239290731430117, 13.45661401736036211 ) ) ;
#26786=( BOUNDED_SURFACE ( )  B_SPLINE_SURFACE ( 3, 2, ( 
 ( #40548, #17358, #83134 ),
 ( #73432, #65361, #80993 ),
 ( #9231, #64312, #97184 ),
 ( #23328, #41084, #56169 ),
 ( #89110, #15206, #59952 ),
 ( #11348, #20048, #60485 ),
 ( #68015, #42674, #93365 ),
 ( #76097, #19517, #68567 ),
 ( #52352, #69096, #26538 ),
 ( #2198, #44280, #75573 ),
 ( #2737, #26016, #50742 ),
 ( #100901, #27069, #101969 ) ),
 .UNSPECIFIED., .F., .F., .F. ) 
 B_SPLINE_SURFACE_WITH_KNOTS ( ( 4, 2, 2, 2, 2, 4 ),
 ( 3, 3 ),
 ( 6.260183343931302602E-16, 0.0007735885786028768403, 0.001547177157205127662, 0.001933971446506253019, 0.002320765735807378376, 0.003094354314409629089 ),
 ( 0.000000000000000000, 1.000000000000000000 ),
 .UNSPECIFIED. ) 
 GEOMETRIC_REPRESENTATION_ITEM ( )  RATIONAL_B_SPLINE_SURFACE ( (
 ( 1.000000000000000000, 0.9603284238771461201, 1.000000000000000000),
 ( 1.000000000000000000, 0.9628724889915971641, 1.000000000000000000),
 ( 1.000000000000000000, 0.9663306537745371960, 1.000000000000000000),
 ( 1.000000000000000000, 0.9744563874113795210, 1.000000000000000000),
 ( 1.000000000000000000, 0.9789903143387164164, 1.000000000000000000),
 ( 1.000000000000000000, 0.9855527733005580160, 1.000000000000000000),
 ( 1.000000000000000000, 0.9877025284828774288, 1.000000000000000000),
 ( 1.000000000000000000, 0.9916277982505475874, 1.000000000000000000),
 ( 1.000000000000000000, 0.9934221110298016022, 1.000000000000000000),
 ( 1.000000000000000000, 0.9980179737616281521, 1.000000000000000000),
 ( 1.000000000000000000, 1.000016370385754083, 1.000000000000000000),
 ( 1.000000000000000000, 1.000000000000000000, 1.000000000000000000) ) ) 
 REPRESENTATION_ITEM ( '' )  SURFACE ( )  );
#26796=CARTESIAN_POINT ( 'NONE',  ( 6.038222094115994310, -12.57840291894174989, 12.65816746961330885 ) ) ;
#26810=CARTESIAN_POINT ( 'NONE',  ( 6.840078058529589278, -12.20617675668042601, 8.820020145246234122 ) ) ;
#26860=CARTESIAN_POINT ( 'NONE',  ( 1.000000000000000222, -5.000000000000000000, -14.14213562373095101 ) ) ;
#26877=DIRECTION ( 'NONE',  ( 0.000000000000000000, 1.000000000000000000, 0.000000000000000000 ) ) ;
#26896=VERTEX_POINT ( 'NONE', #25312 ) ;
#26924=CARTESIAN_POINT ( 'NONE',  ( 0.000000000000000000, -54.00000000000000711, 45.00000000000000000 ) ) ;
#26936=CARTESIAN_POINT ( 'NONE',  ( 11.91633406602797685, -2.062723235127855492, 20.64923308538431712 ) ) ;
#26940=CARTESIAN_POINT ( 'NONE',  ( 3.384215095276664531, -49.13301901873818878, 104.0501775326194576 ) ) ;
#26954=ORIENTED_EDGE ( 'NONE', *, *, #26086, .F. ) ;
#26960=CARTESIAN_POINT ( 'NONE',  ( 4.312270534946733846, -9.512596744310483743, -11.64851190995536712 ) ) ;
#26970=ORIENTED_EDGE ( 'NONE', *, *, #42584, .F. ) ;
#27052=CARTESIAN_POINT ( 'NONE',  ( -5.000000000000000000, -14.90044762032552228, 12.47949281813645861 ) ) ;
#27069=CARTESIAN_POINT ( 'NONE',  ( -3.352941176470594975, -1.200583151104953616, 104.5794940929807524 ) ) ;
#27077=CARTESIAN_POINT ( 'NONE',  ( 5.332775234344524939, -8.148154046107340065, 13.71400129111602517 ) ) ;
#27095=CARTESIAN_POINT ( 'NONE',  ( 4.999999999999993783, -4.000000000000003553, 102.2532056551910387 ) ) ;
#27100=SURFACE_STYLE_FILL_AREA ( #2773 ) ;
#27117=CARTESIAN_POINT ( 'NONE',  ( -3.857142857142855874, -1.200583151104943180, 103.1763305333244318 ) ) ;
#27120=ORIENTED_EDGE ( 'NONE', *, *, #2172, .T. ) ;
#27127=FILL_AREA_STYLE_COLOUR ( '', #43445 ) ;
#27129=VECTOR ( 'NONE', #62039, 1000.000000000000000 ) ;
#27133=DIRECTION ( 'NONE',  ( 0.000000000000000000, 0.000000000000000000, -1.000000000000000000 ) ) ;
#27167=CARTESIAN_POINT ( 'NONE',  ( 3.558939058151947776, -1.060970281106177859, 104.4181685828942108 ) ) ;
#27174=VECTOR ( 'NONE', #51286, 1000.000000000000000 ) ;
#27187=ORIENTED_EDGE ( 'NONE', *, *, #43815, .T. ) ;
#27203=CARTESIAN_POINT ( 'NONE',  ( 5.603804764709383157, -2.702239074867123669, 103.9691152301460875 ) ) ;
#27206=CARTESIAN_POINT ( 'NONE',  ( -3.423905177083530038, -49.17202489992615000, 103.8439100969724507 ) ) ;
#27210=DIRECTION ( 'NONE',  ( 0.000000000000000000, 0.000000000000000000, 1.000000000000000000 ) ) ;
#27247=ORIENTED_EDGE ( 'NONE', *, *, #47748, .F. ) ;
#27255=CARTESIAN_POINT ( 'NONE',  ( 4.867809078344842888, -47.05361238721339134, 42.73860010202603377 ) ) ;
#27257=EDGE_CURVE ( 'NONE', #76134, #80842, #73728, .T. ) ;
#27259=( BOUNDED_SURFACE ( )  B_SPLINE_SURFACE ( 3, 2, ( 
 ( #1078, #34054, #25979 ),
 ( #58840, #91733, #69589 ),
 ( #53909, #101935, #13971 ),
 ( #54962, #102479, #86841 ) ),
 .UNSPECIFIED., .F., .F., .F. ) 
 B_SPLINE_SURFACE_WITH_KNOTS ( ( 4, 4 ),
 ( 3, 3 ),
 ( 1.084202172485504434E-18, 0.0009823161607563541970 ),
 ( 0.000000000000000000, 1.000000000000000000 ),
 .UNSPECIFIED. ) 
 GEOMETRIC_REPRESENTATION_ITEM ( )  RATIONAL_B_SPLINE_SURFACE ( (
 ( 1.000000000000000000, 0.9359444767143320076, 1.000000000000000000),
 ( 1.000000000000000000, 0.9457608441872440430, 1.000000000000000000),
 ( 1.000000000000000000, 0.9551386542018457382, 1.000000000000000000),
 ( 1.000000000000000000, 0.9603284238771502279, 1.000000000000000000) ) ) 
 REPRESENTATION_ITEM ( '' )  SURFACE ( )  );
#27270=CARTESIAN_POINT ( 'NONE',  ( -12.37144696128342147, -4.000000000000003553, 20.44658103856077602 ) ) ;
#27293=DIRECTION ( 'NONE',  ( 0.000000000000000000, 0.000000000000000000, -1.000000000000000000 ) ) ;
#27340=CARTESIAN_POINT ( 'NONE',  ( 6.019773438520846121, -12.68390881199739439, 12.80591459027740520 ) ) ;
#27341=VECTOR ( 'NONE', #21572, 1000.000000000000000 ) ;
#27354=CARTESIAN_POINT ( 'NONE',  ( -14.00172459590632457, -58.00011126645020454, 26.85642925593120722 ) ) ;
#27387=ORIENTED_EDGE ( 'NONE', *, *, #54089, .F. ) ;
#27397=CARTESIAN_POINT ( 'NONE',  ( -4.022544416453470717, -1.369395410676483849, 103.0357414394656246 ) ) ;
#27419=CARTESIAN_POINT ( 'NONE',  ( 1.258203773053022889, -53.99999999999999289, 40.95164674802879290 ) ) ;
#27481=CARTESIAN_POINT ( 'NONE',  ( -1.885326977220364242, -7.100374495473466219, -13.29788260066169414 ) ) ;
#27504=CARTESIAN_POINT ( 'NONE',  ( 4.293150003526390535, -12.96978500885370345, -9.455099716441868196 ) ) ;
#27525=CARTESIAN_POINT ( 'NONE',  ( -27.99999999999999645, 0.000000000000000000, 0.000000000000000000 ) ) ;
#27560=CARTESIAN_POINT ( 'NONE',  ( 0.000000000000000000, -80.00000000000000000, 27.00000000000000000 ) ) ;
#27570=PRESENTATION_STYLE_ASSIGNMENT (( #100340 ) ) ;
#27607=CARTESIAN_POINT ( 'NONE',  ( 30.00000000000000000, 0.000000000000000000, 15.00000000000000000 ) ) ;
#27611=SURFACE_STYLE_FILL_AREA ( #84209 ) ;
#27612=CARTESIAN_POINT ( 'NONE',  ( 6.407477497206921058, -15.51226555635960480, 14.54000465036871503 ) ) ;
#27621=ORIENTED_EDGE ( 'NONE', *, *, #18093, .T. ) ;
#27637=CARTESIAN_POINT ( 'NONE',  ( 3.035724950089529361, -49.45330424012770720, 103.2067224559505974 ) ) ;
#27665=CARTESIAN_POINT ( 'NONE',  ( 8.413542354226143161, -1.106381881529997724, 15.48637553561542113 ) ) ;
#27671=CARTESIAN_POINT ( 'NONE',  ( -5.000000000000000888, -68.69775162920400646, 12.24814655256842855 ) ) ;
#27706=CARTESIAN_POINT ( 'NONE',  ( 3.883877898720808908, -1.065320993063007426, 104.5781496044265566 ) ) ;
#27711=CARTESIAN_POINT ( 'NONE',  ( -10.89098046483293558, -11.19508265682690151, 9.990606830166543162 ) ) ;
#27712=CARTESIAN_POINT ( 'NONE',  ( -5.990573850131388767, -14.42843120744228536, 14.14171987952404130 ) ) ;
#27726=CARTESIAN_POINT ( 'NONE',  ( 13.86010052718616947, -8.688880844539829340, 12.24034105654405913 ) ) ;
#27732=SURFACE_STYLE_USAGE ( .BOTH. , #84327 ) ;
#27737=DIRECTION ( 'NONE',  ( -2.742080092235280244E-17, -0.000000000000000000, 1.000000000000000000 ) ) ;
#27751=VERTEX_POINT ( 'NONE', #25609 ) ;
#27782=VERTEX_POINT ( 'NONE', #86493 ) ;
#27787=CARTESIAN_POINT ( 'NONE',  ( 5.000000000000000000, -60.71953810597794643, 12.61250543007074931 ) ) ;
#27790=COLOUR_RGB ( '', 0.09019608, 0.27058824, 0.51372549) ;
#27793=CARTESIAN_POINT ( 'NONE',  ( 3.914937639300730687, -48.74218602603162509, 43.65505948954400850 ) ) ;
#27797=ORIENTED_EDGE ( 'NONE', *, *, #71867, .F. ) ;
#27804=CARTESIAN_POINT ( 'NONE',  ( 0.8750000000000016653, -70.58759490697437400, 13.02737050516260098 ) ) ;
#27809=ADVANCED_FACE ( 'NONE', ( #37417 ), #62726, .F. ) ;
#27815=CARTESIAN_POINT ( 'NONE',  ( -3.642721895236043395, -49.00544355537606833, 43.86825576446273089 ) ) ;
#27844=EDGE_CURVE ( 'NONE', #80842, #82136, #62841, .T. ) ;
#27854=ORIENTED_EDGE ( 'NONE', *, *, #95773, .T. ) ;
#27893=FACE_OUTER_BOUND ( 'NONE', #81232, .T. ) ;
#27931=PRESENTATION_STYLE_ASSIGNMENT (( #77500 ) ) ;
#27945=CARTESIAN_POINT ( 'NONE',  ( 5.000000000000000000, -14.89995766649703590, 12.47930207026080751 ) ) ;
#27947=ADVANCED_FACE ( 'NONE', ( #73974 ), #25338, .F. ) ;
#27954=CARTESIAN_POINT ( 'NONE',  ( 6.999999999999997335, -46.47786565829922978, 39.12435565298215323 ) ) ;
#28021=ORIENTED_EDGE ( 'NONE', *, *, #74454, .F. ) ;
#28031=CARTESIAN_POINT ( 'NONE',  ( 4.698242434196062689, -14.20142765657284123, -8.220922734483856686 ) ) ;
#28033=DIRECTION ( 'NONE',  ( 0.8257009859296333687, 0.000000000000000000, 0.5641080409237501092 ) ) ;
#28075=SURFACE_SIDE_STYLE ('',( #11295 ) ) ;
#28077=CARTESIAN_POINT ( 'NONE',  ( -7.416346432021269308, -0.5927586397820543418, 15.44415232864270671 ) ) ;
#28129=CARTESIAN_POINT ( 'NONE',  ( -0.9999999999999943379, 0.000000000000000000, 101.0455488498966758 ) ) ;
#28144=DIRECTION ( 'NONE',  ( 0.000000000000000000, 0.000000000000000000, 1.000000000000000000 ) ) ;
#28163=FILL_AREA_STYLE_COLOUR ( '', #25202 ) ;
#28179=DIRECTION ( 'NONE',  ( -1.000000000000000000, -0.000000000000000000, -0.000000000000000000 ) ) ;
#28180=ORIENTED_EDGE ( 'NONE', *, *, #66628, .F. ) ;
#28230=CARTESIAN_POINT ( 'NONE',  ( 3.707709148203173655, -1.099523832062987871, 104.5934084724869564 ) ) ;
#28233=B_SPLINE_CURVE_WITH_KNOTS ( 'NONE', 3,
 ( #101787, #27419, #44092, #94240, #100718, #35495, #43556, #43027, #92630, #36040, #3095, #69959, #102319, #51091, #77522, #76437, #60298, #2017, #28470, #68912, #27954, #18787 ),
 .UNSPECIFIED., .F., .F.,
 ( 4, 2, 2, 2, 2, 2, 2, 2, 2, 2, 4 ),
 ( 0.000000000000000000, 0.001418111674391761513, 0.002127167511587641727, 0.002836223348783521725, 0.003545279185979403024, 0.004254335023175285189, 0.005672446697567033909, 0.007090558371958782628, 0.008508670046350530480, 0.009926781720742280934, 0.01134489339513402965 ),
 .UNSPECIFIED. ) ;
#28235=CARTESIAN_POINT ( 'NONE',  ( -5.979482036612522755, -14.26481676427878398, 14.07238976267243835 ) ) ;
#28247=DIRECTION ( 'NONE',  ( -0.000000000000000000, -1.000000000000000000, -0.000000000000000000 ) ) ;
#28268=CARTESIAN_POINT ( 'NONE',  ( 4.526657684027824757, -2.093347780961849036, 103.5746540667394555 ) ) ;
#28279=CARTESIAN_POINT ( 'NONE',  ( 4.681380154937392568, -50.73787295680594411, 103.7259032015043090 ) ) ;
#28308=CARTESIAN_POINT ( 'NONE',  ( 2.268390192474211364, -49.89683323521570202, 40.92072922013065295 ) ) ;
#28327=CARTESIAN_POINT ( 'NONE',  ( -4.009756559019359123, -48.64709516568132130, 43.57946810439663210 ) ) ;
#28336=CARTESIAN_POINT ( 'NONE',  ( 1.284594766674681532, -49.99999999999997868, 44.94053020278990118 ) ) ;
#28454=STYLED_ITEM ( 'NONE', ( #55382 ), #41599 ) ;
#28464=EDGE_CURVE ( 'NONE', #45005, #51662, #101033, .T. ) ;
#28470=CARTESIAN_POINT ( 'NONE',  ( 6.836057901778168855, -47.88509835587553454, 39.21777279280524908 ) ) ;
#28533=SURFACE_STYLE_FILL_AREA ( #59815 ) ;
#28535=( GEOMETRIC_REPRESENTATION_CONTEXT ( 3 ) GLOBAL_UNCERTAINTY_ASSIGNED_CONTEXT ( ( #63126 ) ) GLOBAL_UNIT_ASSIGNED_CONTEXT ( ( #1729, #91826, #43270 ) ) REPRESENTATION_CONTEXT ( 'NONE', 'WORKASPACE' ) );
#28566=DIRECTION ( 'NONE',  ( 0.000000000000000000, 1.000000000000000000, 0.000000000000000000 ) ) ;
#28589=CARTESIAN_POINT ( 'NONE',  ( 1.257641187073857525, -2.476915083462004360E-10, 101.3278948774975561 ) ) ;
#28606=CARTESIAN_POINT ( 'NONE',  ( -13.57352674565050776, 1.209266042179385936, 14.95197387114457399 ) ) ;
#28631=CIRCLE ( 'NONE', #59567, 15.00000000000000000 ) ;
#28635=CARTESIAN_POINT ( 'NONE',  ( -6.923875968562938965, -12.36264606019533474, 8.501481527782761560 ) ) ;
#28664=SURFACE_SIDE_STYLE ('',( #27611 ) ) ;
#28682=( GEOMETRIC_REPRESENTATION_CONTEXT ( 3 ) GLOBAL_UNCERTAINTY_ASSIGNED_CONTEXT ( ( #62167 ) ) GLOBAL_UNIT_ASSIGNED_CONTEXT ( ( #43860, #76219, #60603 ) ) REPRESENTATION_CONTEXT ( 'NONE', 'WORKASPACE' ) );
#28719=( NAMED_UNIT ( * ) SI_UNIT ( $, .STERADIAN. ) SOLID_ANGLE_UNIT ( ) );
#28787=CARTESIAN_POINT ( 'NONE',  ( 13.38090213880806978, -54.00000000000000711, 31.11721482942554928 ) ) ;
#28800=STYLED_ITEM ( 'NONE', ( #93648 ), #101096 ) ;
#28802=CARTESIAN_POINT ( 'NONE',  ( 3.857142857142850101, -48.79941684889506348, 103.1763305333244176 ) ) ;
#28809=SURFACE_SIDE_STYLE ('',( #43352 ) ) ;
#28816=SURFACE_STYLE_USAGE ( .BOTH. , #49297 ) ;
#28823=VECTOR ( 'NONE', #92633, 1000.000000000000000 ) ;
#28837=ORIENTED_EDGE ( 'NONE', *, *, #10979, .F. ) ;
#28849=CIRCLE ( 'NONE', #44347, 2.000000000000000000 ) ;
#28857=CARTESIAN_POINT ( 'NONE',  ( 1.918196553303399110, -49.89542747347661589, 44.77704491145068744 ) ) ;
#28867=CARTESIAN_POINT ( 'NONE',  ( 0.5846921733595837889, -70.55117423362948159, 13.00919072386916397 ) ) ;
#28877=CARTESIAN_POINT ( 'NONE',  ( -12.31568180227341891, -4.628506154427563857, 20.34130839979936312 ) ) ;
#28878=ORIENTED_EDGE ( 'NONE', *, *, #45394, .F. ) ;
#28879=CARTESIAN_POINT ( 'NONE',  ( -6.358572135259356273, -49.57572298635458452, 39.47396800149780205 ) ) ;
#28918=EDGE_LOOP ( 'NONE', ( #51134, #10444, #90988, #85874, #990 ) ) ;
#28975=CARTESIAN_POINT ( 'NONE',  ( -1.366857229432719700, -69.63343833532438509, 12.80410507582288560 ) ) ;
#29016=CARTESIAN_POINT ( 'NONE',  ( 13.64640293162734785, -51.35851448446996415, 30.13230102324352799 ) ) ;
#29017=CARTESIAN_POINT ( 'NONE',  ( 5.000000000000000000, -15.43641607416063266, 12.61250543006137725 ) ) ;
#29048=SURFACE_SIDE_STYLE ('',( #53270 ) ) ;
#29083=CARTESIAN_POINT ( 'NONE',  ( -14.85144930561877175, -6.995911484127552704, 13.28113257175721706 ) ) ;
#29095=CIRCLE ( 'NONE', #3241, 8.000000000000000000 ) ;
#29114=ORIENTED_EDGE ( 'NONE', *, *, #23623, .F. ) ;
#29152=CARTESIAN_POINT ( 'NONE',  ( -12.39018079436049113, -3.230755885516240156, 20.63706837319177723 ) ) ;
#29163=AXIS2_PLACEMENT_3D ( 'NONE', #41283, #9427, #253 ) ;
#29164=CARTESIAN_POINT ( 'NONE',  ( -5.833333333333329485, -50.00000000000000000, 103.8776713793258608 ) ) ;
#29183=FACE_OUTER_BOUND ( 'NONE', #5637, .T. ) ;
#29190=CARTESIAN_POINT ( 'NONE',  ( -13.48753244636324489, -52.95794048676148691, 23.24642415514733429 ) ) ;
#29208=FILL_AREA_STYLE ('',( #70677 ) ) ;
#29220=MECHANICAL_DESIGN_GEOMETRIC_PRESENTATION_REPRESENTATION('',(#34359),#42948);
#29249=CARTESIAN_POINT ( 'NONE',  ( 0.000000000000000000, -46.00000000000000000, 122.0000000000000000 ) ) ;
#29261=CARTESIAN_POINT ( 'NONE',  ( -5.000000000000000888, -48.53184174324966449, 2.645245988191155639 ) ) ;
#29268=CARTESIAN_POINT ( 'NONE',  ( 0.000000000000000000, -4.000000000000003553, 112.0000000000000000 ) ) ;
#29273=DIRECTION ( 'NONE',  ( 0.9921085174016837094, -0.1089071661329407970, 0.06212824529894127312 ) ) ;
#29286=SURFACE_STYLE_FILL_AREA ( #6011 ) ;
#29294=FILL_AREA_STYLE ('',( #37384 ) ) ;
#29295=CARTESIAN_POINT ( 'NONE',  ( 1.000000000000000000, -63.14890303518984638, 9.346194641690638960 ) ) ;
#29314=CARTESIAN_POINT ( 'NONE',  ( 3.433097715925975013, -49.17502020225290948, 103.8029788753759703 ) ) ;
#29367=( LENGTH_UNIT ( ) NAMED_UNIT ( * ) SI_UNIT ( .MILLI., .METRE. ) );
#29376=ADVANCED_BREP_SHAPE_REPRESENTATION ( '', ( #90230, #10728 ), #7340 ) ;
#29382=CIRCLE ( 'NONE', #39680, 2.000000000000000000 ) ;
#29393=ORIENTED_EDGE ( 'NONE', *, *, #26635, .T. ) ;
#29394=CARTESIAN_POINT ( 'NONE',  ( -3.559384062307034302, -53.17517428501233212, 40.54544626083967529 ) ) ;
#29400=ADVANCED_FACE ( 'NONE', ( #49692 ), #44305, .T. ) ;
#29458=CARTESIAN_POINT ( 'NONE',  ( 5.140490343214302094, -10.64767277737062301, -10.57915202476631578 ) ) ;
#29462=AXIS2_PLACEMENT_3D ( 'NONE', #9372, #2356, #16970 ) ;
#29472=CARTESIAN_POINT ( 'NONE',  ( 14.63297776001217798, 0.3240115842722206541, 14.99725733981229325 ) ) ;
#29478=CIRCLE ( 'NONE', #89722, 9.999999999999994671 ) ;
#29492=FILL_AREA_STYLE_COLOUR ( '', #4250 ) ;
#29506=ORIENTED_EDGE ( 'NONE', *, *, #86051, .T. ) ;
#29515=SURFACE_STYLE_FILL_AREA ( #53224 ) ;
#29526=CARTESIAN_POINT ( 'NONE',  ( 13.50905259634051170, -52.70511631464653846, 23.32354201833150853 ) ) ;
#29527=CARTESIAN_POINT ( 'NONE',  ( 5.000000000000000000, -14.73352921087159295, 12.39872608460982661 ) ) ;
#29570=ORIENTED_EDGE ( 'NONE', *, *, #55075, .F. ) ;
#29593=CARTESIAN_POINT ( 'NONE',  ( -6.408521271130449115, -15.51162931541124124, 14.54064475688238822 ) ) ;
#29623=PRESENTATION_STYLE_ASSIGNMENT (( #5318 ) ) ;
#29642=CARTESIAN_POINT ( 'NONE',  ( 3.857142857142854542, -1.200583151104942070, 103.1763305333244318 ) ) ;
#29654=CARTESIAN_POINT ( 'NONE',  ( 3.363648053944605198, -1.214821636234522995, 104.5995868353016505 ) ) ;
#29667=CARTESIAN_POINT ( 'NONE',  ( -12.30573667306818031, 1.921380894879668233, 14.87702195164505348 ) ) ;
#29673=B_SPLINE_CURVE_WITH_KNOTS ( 'NONE', 3,
 ( #103551, #80314, #31286, #23719, #70656, #38314, #15057, #29701, #63098, #95458 ),
 .UNSPECIFIED., .F., .F.,
 ( 4, 2, 2, 2, 4 ),
 ( 0.0005274614566083536769, 0.002396735553633655511, 0.003331372602146292008, 0.003798691126402609607, 0.004266009650658927205 ),
 .UNSPECIFIED. ) ;
#29685=CARTESIAN_POINT ( 'NONE',  ( 6.999999999999997335, -80.00000000000000000, 39.12435565298213902 ) ) ;
#29693=CARTESIAN_POINT ( 'NONE',  ( -1.919652159211370224, -70.56598577336447420, 13.12977962495732420 ) ) ;
#29694=( NAMED_UNIT ( * ) SI_UNIT ( $, .STERADIAN. ) SOLID_ANGLE_UNIT ( ) );
#29701=CARTESIAN_POINT ( 'NONE',  ( 1.226852121894917547, -49.99514363866957467, 101.2646212623072870 ) ) ;
#29711=EDGE_LOOP ( 'NONE', ( #68008, #99420, #38575, #73143, #75102, #85770, #98200, #95692, #89679, #42419, #72305 ) ) ;
#29725=UNCERTAINTY_MEASURE_WITH_UNIT (LENGTH_MEASURE( 1.000000000000000082E-05 ), #4652, 'distance_accuracy_value', 'NONE');
#29771=DIRECTION ( 'NONE',  ( 1.000000000000000000, -0.000000000000000000, 1.224646799147353207E-16 ) ) ;
#29803=( NAMED_UNIT ( * ) PLANE_ANGLE_UNIT ( ) SI_UNIT ( $, .RADIAN. ) );
#29811=CARTESIAN_POINT ( 'NONE',  ( -4.284822031654912600, -48.90716638558775031, 104.4267991316945228 ) ) ;
#29849=DIRECTION ( 'NONE',  ( 0.000000000000000000, 0.000000000000000000, 1.000000000000000000 ) ) ;
#29857=ORIENTED_EDGE ( 'NONE', *, *, #36388, .F. ) ;
#29866=CARTESIAN_POINT ( 'NONE',  ( -4.846576637897429762, -47.10533319821855258, 42.76191327062164049 ) ) ;
#29886=CARTESIAN_POINT ( 'NONE',  ( 0.000000000000000000, -78.00000000000000000, 27.00000000000000000 ) ) ;
#29945=ORIENTED_EDGE ( 'NONE', *, *, #7312, .T. ) ;
#29962=( NAMED_UNIT ( * ) PLANE_ANGLE_UNIT ( ) SI_UNIT ( $, .RADIAN. ) );
#30011=ORIENTED_EDGE ( 'NONE', *, *, #75288, .T. ) ;
#30042=ADVANCED_FACE ( 'NONE', ( #66030 ), #4801, .T. ) ;
#30061=CARTESIAN_POINT ( 'NONE',  ( -1.458873328850117668, -49.96632135588456691, 101.6361877027969740 ) ) ;
#30105=CARTESIAN_POINT ( 'NONE',  ( -7.553239908583639028, -6.016880836006652800, 14.04797252150881981 ) ) ;
#30148=CARTESIAN_POINT ( 'NONE',  ( -4.284822031654912600, -48.90716638558775031, 104.4267991316945228 ) ) ;
#30154=B_SPLINE_CURVE_WITH_KNOTS ( 'NONE', 3,
 ( #64767, #32953, #7048, #106262, #97124, #57183, #104688, #23264, #96610, #14595, #65822, #41021 ),
 .UNSPECIFIED., .F., .F.,
 ( 4, 2, 2, 2, 2, 4 ),
 ( 0.000000000000000000, 0.0008138854558913282463, 0.001220828183837001151, 0.001627770911782673840, 0.002441656367674002303, 0.003255541823565330332 ),
 .UNSPECIFIED. ) ;
#30174=CARTESIAN_POINT ( 'NONE',  ( -10.31289488289771406, 2.633976217239669904, 14.76805301559119954 ) ) ;
#30206=CARTESIAN_POINT ( 'NONE',  ( -6.846801517543320337, -12.21872792266663588, 8.794481130079006448 ) ) ;
#30220=ORIENTED_EDGE ( 'NONE', *, *, #25518, .F. ) ;
#30235=CARTESIAN_POINT ( 'NONE',  ( 4.551587301587293410, -48.79941684889506348, 104.4018401814738013 ) ) ;
#30282=ORIENTED_EDGE ( 'NONE', *, *, #88929, .T. ) ;
#30296=CARTESIAN_POINT ( 'NONE',  ( -5.000000000000000888, -26.68136363036281722, -6.178889730593319030 ) ) ;
#30299=EDGE_CURVE ( 'NONE', #101089, #57615, #20339, .T. ) ;
#30321=SURFACE_SIDE_STYLE ('',( #29286 ) ) ;
#30322=PRESENTATION_STYLE_ASSIGNMENT (( #53521 ) ) ;
#30327=COLOUR_RGB ( '', 0.09019608, 0.27058824, 0.51372549) ;
#30348=VERTEX_POINT ( 'NONE', #60500 ) ;
#30349=CARTESIAN_POINT ( 'NONE',  ( 13.93074145947618447, -57.79372918398592418, 28.41232622077120595 ) ) ;
#30470=SURFACE_STYLE_FILL_AREA ( #102747 ) ;
#30503=( GEOMETRIC_REPRESENTATION_CONTEXT ( 3 ) GLOBAL_UNCERTAINTY_ASSIGNED_CONTEXT ( ( #97666 ) ) GLOBAL_UNIT_ASSIGNED_CONTEXT ( ( #85512, #49263, #41191 ) ) REPRESENTATION_CONTEXT ( 'NONE', 'WORKASPACE' ) );
#30525=STYLED_ITEM ( 'NONE', ( #36322 ), #15527 ) ;
#30538=ORIENTED_EDGE ( 'NONE', *, *, #55932, .F. ) ;
#30569=CARTESIAN_POINT ( 'NONE',  ( 13.44288011066907096, -52.70710939378555793, 30.91149535780206747 ) ) ;
#30574=AXIS2_PLACEMENT_3D ( 'NONE', #106700, #98084, #32851 ) ;
#30583=SURFACE_STYLE_FILL_AREA ( #95833 ) ;
#30612=CARTESIAN_POINT ( 'NONE',  ( -5.164787682159484916, -1.887557197826900124, 104.1470044518084990 ) ) ;
#30623=( NAMED_UNIT ( * ) SI_UNIT ( $, .STERADIAN. ) SOLID_ANGLE_UNIT ( ) );
#30643=CARTESIAN_POINT ( 'NONE',  ( -8.451132639193684071, -14.18294114141584039, 15.83549708304340164 ) ) ;
#30670=CARTESIAN_POINT ( 'NONE',  ( -0.9999999999999943379, -50.00000000000000000, 101.0455488498966758 ) ) ;
#30678=CARTESIAN_POINT ( 'NONE',  ( 2.723995404495900718, -0.3641544584862766443, 102.8348527318366052 ) ) ;
#30718=TOROIDAL_SURFACE ( 'NONE', #77200, 11.00000000000000533, 4.000000000000000000 ) ;
#30749=CARTESIAN_POINT ( 'NONE',  ( -3.339154757874568169, -69.93519652824339516, 13.40218433671247134 ) ) ;
#30758=CARTESIAN_POINT ( 'NONE',  ( -13.97222917066916992, -50.12745207469774300, 26.08167946173673002 ) ) ;
#30814=CARTESIAN_POINT ( 'NONE',  ( -9.960739174314243272, -50.12849100989416939, 26.07695415532590033 ) ) ;
#30843=CIRCLE ( 'NONE', #36020, 8.857142857142855874 ) ;
#30863=CARTESIAN_POINT ( 'NONE',  ( -2.120783755321927533, -0.2152620591958233909, 102.5525762030299859 ) ) ;
#30865=PRESENTATION_STYLE_ASSIGNMENT (( #63210 ) ) ;
#30877=PRESENTATION_STYLE_ASSIGNMENT (( #14105 ) ) ;
#30907=CARTESIAN_POINT ( 'NONE',  ( 1.000000000000000000, -70.02076148470871431, 13.01198664878534750 ) ) ;
#30914=VERTEX_POINT ( 'NONE', #95371 ) ;
#30980=CARTESIAN_POINT ( 'NONE',  ( -11.70587015981644186, -8.262194459278509484, 19.31689096126753924 ) ) ;
#30982=DIRECTION ( 'NONE',  ( 0.000000000000000000, 0.000000000000000000, 1.000000000000000000 ) ) ;
#31033=EDGE_LOOP ( 'NONE', ( #15354, #91600, #32166, #103228, #71721, #93595 ) ) ;
#31125=VECTOR ( 'NONE', #7405, 1000.000000000000000 ) ;
#31129=CARTESIAN_POINT ( 'NONE',  ( 0.3289898188424446035, -69.52447499062914460, 12.72735422194733879 ) ) ;
#31135=FILL_AREA_STYLE_COLOUR ( '', #16394 ) ;
#31145=ORIENTED_EDGE ( 'NONE', *, *, #91225, .F. ) ;
#31151=EDGE_LOOP ( 'NONE', ( #25461, #29393, #40198 ) ) ;
#31176=CARTESIAN_POINT ( 'NONE',  ( 6.079546931269272925, -62.81856771641567150, 14.38824559419034799 ) ) ;
#31184=CARTESIAN_POINT ( 'NONE',  ( -9.283512820355584338, -2.882884900155469943, 14.75241131180710319 ) ) ;
#31215=ADVANCED_FACE ( 'NONE', ( #90068 ), #55521, .F. ) ;
#31263=VECTOR ( 'NONE', #27737, 1000.000000000000000 ) ;
#31266=LINE ( 'NONE', #15034, #90840 ) ;
#31279=CARTESIAN_POINT ( 'NONE',  ( -6.386171959437410450, -11.88579060466480364, 10.72108492130440460 ) ) ;
#31286=CARTESIAN_POINT ( 'NONE',  ( 2.723997317187916156, -49.63584449629185968, 102.8348549799726612 ) ) ;
#31309=UNCERTAINTY_MEASURE_WITH_UNIT (LENGTH_MEASURE( 1.000000000000000082E-05 ), #15740, 'distance_accuracy_value', 'NONE');
#31425=CARTESIAN_POINT ( 'NONE',  ( 13.77155591953703961, -57.01367568605869707, 24.47427385584959225 ) ) ;
#31440=CARTESIAN_POINT ( 'NONE',  ( 12.98335800805550022, -9.687644989897647108, 11.46374983418961691 ) ) ;
#31451=EDGE_LOOP ( 'NONE', ( #105694, #33577, #7712 ) ) ;
#31461=B_SPLINE_CURVE_WITH_KNOTS ( 'NONE', 3,
 ( #63783, #20718, #14659, #86487, #98252, #72899, #16813, #82604, #106323, #49700, #98769, #57244, #8708, #99297, #56718, #105809, #32490, #41616, #31949, #64830, #33021, #48094, #90164, #7110, #24922, #40026, #16268, #42136, #1120, #75022, #23874, #74500, #48623, #8178 ),
 .UNSPECIFIED., .F., .F.,
 ( 4, 2, 2, 2, 2, 2, 2, 2, 2, 2, 2, 2, 2, 2, 2, 2, 4 ),
 ( 0.01263964810480761557, 0.01342907106096845327, 0.01421849401712929097, 0.01500791697329012866, 0.01579733992945096810, 0.01658676288561180406, 0.01737618584177264350, 0.01816560879793347946, 0.01895503175409431890, 0.01974445471025515486, 0.02053387766641599430, 0.02132330062257683373, 0.02211272357873766969, 0.02290214653489850566, 0.02369156949105934509, 0.02448099244722018453, 0.02527041540338102049 ),
 .UNSPECIFIED. ) ;
#31470=CARTESIAN_POINT ( 'NONE',  ( -9.113097280746996987, -54.00000000000000711, 31.11721482942554928 ) ) ;
#31492=STYLED_ITEM ( 'NONE', ( #6371 ), #95952 ) ;
#31503=CARTESIAN_POINT ( 'NONE',  ( -1.000000000000000000, -10.50453238069492912, -12.19598953690579535 ) ) ;
#31509=CARTESIAN_POINT ( 'NONE',  ( -6.999999999318260890, -46.53316735177592278, 39.12435565337574417 ) ) ;
#31591=ORIENTED_EDGE ( 'NONE', *, *, #76974, .F. ) ;
#31592=PRESENTATION_STYLE_ASSIGNMENT (( #25089 ) ) ;
#31597=CARTESIAN_POINT ( 'NONE',  ( -2.752434797705083369, -69.16112139175940854, 12.98102957303667182 ) ) ;
#31614=( NAMED_UNIT ( * ) PLANE_ANGLE_UNIT ( ) SI_UNIT ( $, .RADIAN. ) );
#31626=DIRECTION ( 'NONE',  ( 0.000000000000000000, 1.000000000000000000, 0.000000000000000000 ) ) ;
#31695=CARTESIAN_POINT ( 'NONE',  ( -1.451822140657068827, -69.63589226600636550, 12.81290273743130292 ) ) ;
#31744=CIRCLE ( 'NONE', #102324, 15.00000000000000000 ) ;
#31770=( NAMED_UNIT ( * ) SI_UNIT ( $, .STERADIAN. ) SOLID_ANGLE_UNIT ( ) );
#31778=FILL_AREA_STYLE_COLOUR ( '', #5479 ) ;
#31793=CARTESIAN_POINT ( 'NONE',  ( -4.999999999999960032, -14.45898243498580271, 13.52154848218615335 ) ) ;
#31795=( NAMED_UNIT ( * ) PLANE_ANGLE_UNIT ( ) SI_UNIT ( $, .RADIAN. ) );
#31811=STYLED_ITEM ( 'NONE', ( #49801 ), #55970 ) ;
#31818=CARTESIAN_POINT ( 'NONE',  ( -9.000000000000001776, -4.000000000000003553, 42.58845726811989607 ) ) ;
#31856=CARTESIAN_POINT ( 'NONE',  ( 9.378256585906134646, -52.21653903096282789, 23.52725134406122720 ) ) ;
#31863=DIRECTION ( 'NONE',  ( 0.000000000000000000, 1.000000000000000000, 0.000000000000000000 ) ) ;
#31877=FILL_AREA_STYLE_COLOUR ( '', #43440 ) ;
#31890=( GEOMETRIC_REPRESENTATION_CONTEXT ( 3 ) GLOBAL_UNCERTAINTY_ASSIGNED_CONTEXT ( ( #37371 ) ) GLOBAL_UNIT_ASSIGNED_CONTEXT ( ( #63636, #3798, #36735 ) ) REPRESENTATION_CONTEXT ( 'NONE', 'WORKASPACE' ) );
#31912=CARTESIAN_POINT ( 'NONE',  ( 30.00000000000000000, 4.000000000000000000, 18.57417562100670949 ) ) ;
#31913=CARTESIAN_POINT ( 'NONE',  ( -14.64132442749376573, 0.3341158548789989191, 15.00000000000002132 ) ) ;
#31949=CARTESIAN_POINT ( 'NONE',  ( 9.995361331467700339, -57.97514824717608661, 26.59863933490087362 ) ) ;
#31953=CARTESIAN_POINT ( 'NONE',  ( 5.000000000000000888, -26.67919295183293116, -6.179716592092315608 ) ) ;
#31988=CARTESIAN_POINT ( 'NONE',  ( -9.286995370816610418, -55.77767719873747154, 30.70990524772856034 ) ) ;
#32001=( NAMED_UNIT ( * ) SI_UNIT ( $, .STERADIAN. ) SOLID_ANGLE_UNIT ( ) );
#32021=CARTESIAN_POINT ( 'NONE',  ( -1.000000000000000222, -15.98920185053290588, -10.19345919381858145 ) ) ;
#32025=SHAPE_DEFINITION_REPRESENTATION ( #100850, #49395 ) ;
#32033=EDGE_CURVE ( 'NONE', #64161, #10296, #72437, .T. ) ;
#32048=FILL_AREA_STYLE ('',( #56269 ) ) ;
#32091=ORIENTED_EDGE ( 'NONE', *, *, #3471, .F. ) ;
#32103=CARTESIAN_POINT ( 'NONE',  ( 0.000000000000000000, -1.550510257216834331, 112.0000000000000000 ) ) ;
#32105=LINE ( 'NONE', #48780, #1901 ) ;
#32110=DIRECTION ( 'NONE',  ( 1.000000000000000000, 0.000000000000000000, 0.000000000000000000 ) ) ;
#32114=CARTESIAN_POINT ( 'NONE',  ( -5.000000000001306510, -60.71953810597504742, 13.86359191440492467 ) ) ;
#32161=CARTESIAN_POINT ( 'NONE',  ( 27.99999999999999645, 0.000000000000000000, 0.000000000000000000 ) ) ;
#32166=ORIENTED_EDGE ( 'NONE', *, *, #89921, .T. ) ;
#32168=CARTESIAN_POINT ( 'NONE',  ( 10.99833518290787815, -10.49270544111268144, 18.32972597813727589 ) ) ;
#32177=AXIS2_PLACEMENT_3D ( 'NONE', #98360, #48204, #90273 ) ;
#32254=CARTESIAN_POINT ( 'NONE',  ( -4.973317752991197160, -46.53140123174669895, 102.2736751349651456 ) ) ;
#32258=CARTESIAN_POINT ( 'NONE',  ( -5.000000000000000000, -14.21727251091160404, 9.320362779991915758 ) ) ;
#32268=COLOUR_RGB ( '', 0.08235294, 0.09019608, 0.10196078) ;
#32280=( NAMED_UNIT ( * ) PLANE_ANGLE_UNIT ( ) SI_UNIT ( $, .RADIAN. ) );
#32292=CARTESIAN_POINT ( 'NONE',  ( 3.991107381396987730, -48.94960763643569379, 104.5611067885112959 ) ) ;
#32305=DIRECTION ( 'NONE',  ( 0.000000000000000000, 0.000000000000000000, 1.000000000000000000 ) ) ;
#32323=CARTESIAN_POINT ( 'NONE',  ( -3.348056043397916071, -1.092793117426783089, 104.4613933532584440 ) ) ;
#32334=CARTESIAN_POINT ( 'NONE',  ( -5.000000000000000000, -14.65803281199242036, 12.34559804589020260 ) ) ;
#32354=STYLED_ITEM ( 'NONE', ( #32676 ), #38990 ) ;
#32367=CIRCLE ( 'NONE', #70227, 13.00000000000000000 ) ;
#32405=AXIS2_PLACEMENT_3D ( 'NONE', #54436, #77154, #3270 ) ;
#32433=ORIENTED_EDGE ( 'NONE', *, *, #98877, .T. ) ;
#32453=CARTESIAN_POINT ( 'NONE',  ( -6.250885388987164504, 3.157894736842104866, 14.66382285868950675 ) ) ;
#32490=CARTESIAN_POINT ( 'NONE',  ( 9.995943316031024040, -57.99951415928671850, 27.38809334239569182 ) ) ;
#32497=SURFACE_SIDE_STYLE ('',( #90711 ) ) ;
#32525=TOROIDAL_SURFACE ( 'NONE', #3238, 18.00000000000000355, 4.000000000000000000 ) ;
#32535=EDGE_LOOP ( 'NONE', ( #75413, #39346, #69543, #5420 ) ) ;
#32553=AXIS2_PLACEMENT_3D ( 'NONE', #35196, #85317, #3871 ) ;
#32608=ORIENTED_EDGE ( 'NONE', *, *, #39839, .F. ) ;
#32617=LINE ( 'NONE', #62207, #90644 ) ;
#32661=CARTESIAN_POINT ( 'NONE',  ( -5.045023136152173571, -61.23904260837603175, 13.88549718443812964 ) ) ;
#32670=CARTESIAN_POINT ( 'NONE',  ( 3.454253436624922013, -49.15858197120396511, 103.7259032015043090 ) ) ;
#32676=PRESENTATION_STYLE_ASSIGNMENT (( #17540 ) ) ;
#32681=SHAPE_REPRESENTATION_RELATIONSHIP ( 'NONE' , 'NONE' ,  #49395, #29376 ) ;
#32683=CIRCLE ( 'NONE', #3328, 8.857142857142855874 ) ;
#32709=CARTESIAN_POINT ( 'NONE',  ( -0.9330442100819067441, -70.05675763226155084, 13.03100537459362407 ) ) ;
#32718=CARTESIAN_POINT ( 'NONE',  ( 2.914316916059087603, -69.03253091208547687, 13.00441016735022437 ) ) ;
#32749=CARTESIAN_POINT ( 'NONE',  ( 4.999999999999843681, -12.25926108426882166, 9.485372419963775670 ) ) ;
#32773=DIRECTION ( 'NONE',  ( 0.000000000000000000, 1.000000000000000000, 0.000000000000000000 ) ) ;
#32797=CARTESIAN_POINT ( 'NONE',  ( -5.833333333391548692, -46.26205164321604002, 103.8776713793676834 ) ) ;
#32801=EDGE_LOOP ( 'NONE', ( #36247, #27387, #105533, #56456 ) ) ;
#32802=CARTESIAN_POINT ( 'NONE',  ( 3.352941176470589646, -48.79941684889505638, 104.5794940929807524 ) ) ;
#32825=CARTESIAN_POINT ( 'NONE',  ( 4.225130582364226228, -48.93881382677318470, 104.4756880579354998 ) ) ;
#32851=DIRECTION ( 'NONE',  ( 0.000000000000000000, 0.2105263157894738946, -0.9775881905793005755 ) ) ;
#32864=CARTESIAN_POINT ( 'NONE',  ( -6.187404903417438540, -12.10572765818576357, 11.71902858906391032 ) ) ;
#32875=CIRCLE ( 'NONE', #105146, 2.000000000000000000 ) ;
#32884=CARTESIAN_POINT ( 'NONE',  ( 12.08709333886138459, -2.335920665582410294, 20.67766530190866447 ) ) ;
#32922=CARTESIAN_POINT ( 'NONE',  ( 10.00248409573528896, -49.99966751047049485, 26.85804522429446095 ) ) ;
#32940=CARTESIAN_POINT ( 'NONE',  ( 3.730566219500684344, -11.49691612730111245, -10.68061658281946080 ) ) ;
#32946=SURFACE_SIDE_STYLE ('',( #58248 ) ) ;
#32951=CIRCLE ( 'NONE', #93216, 2.000000000000001776 ) ;
#32953=CARTESIAN_POINT ( 'NONE',  ( -4.022544416453469829, -48.63060458932351793, 103.0357414394655962 ) ) ;
#32959=CARTESIAN_POINT ( 'NONE',  ( 4.506320246070899316, -1.182860540001308802, 104.3949652630312670 ) ) ;
#33021=CARTESIAN_POINT ( 'NONE',  ( 9.933618426942553370, -57.79423783648532265, 25.82409549033520690 ) ) ;
#33033=CARTESIAN_POINT ( 'NONE',  ( -3.303250429861293469, -49.28697031698179387, 103.9470740044689308 ) ) ;
#33067=ORIENTED_EDGE ( 'NONE', *, *, #69560, .T. ) ;
#33076=DIRECTION ( 'NONE',  ( 0.000000000000000000, 0.000000000000000000, 1.000000000000000000 ) ) ;
#33114=CARTESIAN_POINT ( 'NONE',  ( 0.000000000000000000, -80.00000000000000000, 27.00000000000000000 ) ) ;
#33122=CARTESIAN_POINT ( 'NONE',  ( -5.683639242321874896, -2.934261738049319224, 103.9372442403038548 ) ) ;
#33156=CARTESIAN_POINT ( 'NONE',  ( -3.365451957726314447, -49.06858650466291749, 104.1992105446094001 ) ) ;
#33162=CARTESIAN_POINT ( 'NONE',  ( 0.000000000000000000, -78.00000000000000000, 27.00000000000000000 ) ) ;
#33179=FACE_OUTER_BOUND ( 'NONE', #52447, .T. ) ;
#33186=CARTESIAN_POINT ( 'NONE',  ( -5.558262485387479579, -66.13834130795673616, 14.15003227941667241 ) ) ;
#33187=FACE_OUTER_BOUND ( 'NONE', #2730, .T. ) ;
#33225=CARTESIAN_POINT ( 'NONE',  ( 15.55105613542228404, -0.9527306383815096202, 14.97181131753247918 ) ) ;
#33235=ORIENTED_EDGE ( 'NONE', *, *, #70224, .F. ) ;
#33242=CARTESIAN_POINT ( 'NONE',  ( 4.177104036897216766, -67.05129264954501878, 13.14325999856157701 ) ) ;
#33250=CARTESIAN_POINT ( 'NONE',  ( 4.999999999999993783, -46.00000000000000000, 102.2532056551910387 ) ) ;
#33257=DIRECTION ( 'NONE',  ( 0.000000000000000000, -0.000000000000000000, 1.000000000000000000 ) ) ;
#33268=EDGE_CURVE ( 'NONE', #85394, #11109, #30843, .T. ) ;
#33273=CARTESIAN_POINT ( 'NONE',  ( 6.187404903406283019, -12.10572765818970709, 11.71902858905958134 ) ) ;
#33287=SURFACE_SIDE_STYLE ('',( #323 ) ) ;
#33291=CARTESIAN_POINT ( 'NONE',  ( 5.603804764709609643, -47.29776092513240826, 103.9691152301460022 ) ) ;
#33308=CARTESIAN_POINT ( 'NONE',  ( -6.931098304924008247, -13.59560219465957154, -6.365424046575419048 ) ) ;
#33335=SURFACE_SIDE_STYLE ('',( #11137 ) ) ;
#33391=CARTESIAN_POINT ( 'NONE',  ( -5.000000000000000000, -14.08559933050952928, 11.75736354680345741 ) ) ;
#33412=CARTESIAN_POINT ( 'NONE',  ( 12.03234183921365563, 2.057523246211587775, 14.86059839350262912 ) ) ;
#33426=AXIS2_PLACEMENT_3D ( 'NONE', #11341, #59946, #93884 ) ;
#33443=CARTESIAN_POINT ( 'NONE',  ( 3.634575668430249706, -68.17834049427936804, 13.10158581207672057 ) ) ;
#33451=CARTESIAN_POINT ( 'NONE',  ( 9.864331116128868260, -50.40680126009896611, 25.34043079474438898 ) ) ;
#33463=CARTESIAN_POINT ( 'NONE',  ( 5.000000000000000000, -15.93202192939576634, -5.930487099830193287 ) ) ;
#33475=CYLINDRICAL_SURFACE ( 'NONE', #13421, 4.000000000000000000 ) ;
#33497=( GEOMETRIC_REPRESENTATION_CONTEXT ( 3 ) GLOBAL_UNCERTAINTY_ASSIGNED_CONTEXT ( ( #35826 ) ) GLOBAL_UNIT_ASSIGNED_CONTEXT ( ( #40720, #16448, #68747 ) ) REPRESENTATION_CONTEXT ( 'NONE', 'WORKASPACE' ) );
#33513=DIRECTION ( 'NONE',  ( -1.000000000000000000, -0.000000000000000000, -0.000000000000000000 ) ) ;
#33526=EDGE_CURVE ( 'NONE', #76134, #41710, #32683, .T. ) ;
#33539=AXIS2_PLACEMENT_3D ( 'NONE', #39182, #31626, #7307 ) ;
#33577=ORIENTED_EDGE ( 'NONE', *, *, #2172, .F. ) ;
#33579=SURFACE_STYLE_USAGE ( .BOTH. , #1157 ) ;
#33645=FILL_AREA_STYLE_COLOUR ( '', #32268 ) ;
#33663=VERTEX_POINT ( 'NONE', #42565 ) ;
#33664=CARTESIAN_POINT ( 'NONE',  ( 7.299581481787712711, -12.47920354261283649, 8.323684855074615641 ) ) ;
#33684=CARTESIAN_POINT ( 'NONE',  ( -3.454253436624944662, -49.15858197120394379, 103.7259032015042095 ) ) ;
#33700=SURFACE_STYLE_FILL_AREA ( #66575 ) ;
#33722=VERTEX_POINT ( 'NONE', #37177 ) ;
#33743=( NAMED_UNIT ( * ) PLANE_ANGLE_UNIT ( ) SI_UNIT ( $, .RADIAN. ) );
#33777=CARTESIAN_POINT ( 'NONE',  ( 4.279808479562545287, -69.01068216744177164, 13.66703314698427363 ) ) ;
#33784=CARTESIAN_POINT ( 'NONE',  ( 4.628159615119683323, -47.68919827030615721, 102.5435725457685976 ) ) ;
#33806=CARTESIAN_POINT ( 'NONE',  ( 6.124999999999992006, -15.62228920881126015, 14.41094225130410322 ) ) ;
#33808=EDGE_CURVE ( 'NONE', #53428, #82494, #51097, .T. ) ;
#33819=MECHANICAL_DESIGN_GEOMETRIC_PRESENTATION_REPRESENTATION('',(#85466),#67139);
#33831=CARTESIAN_POINT ( 'NONE',  ( 4.980618096941788586, -46.46097021954796702, 103.2912570477108858 ) ) ;
#33844=EDGE_LOOP ( 'NONE', ( #18933, #76907, #38125, #43561 ) ) ;
#33854=EDGE_CURVE ( 'NONE', #19188, #71499, #49806, .T. ) ;
#33879=AXIS2_PLACEMENT_3D ( 'NONE', #104821, #80002, #72448 ) ;
#33902=STYLED_ITEM ( 'NONE', ( #84773 ), #24056 ) ;
#33916=ORIENTED_EDGE ( 'NONE', *, *, #16474, .T. ) ;
#33956=CARTESIAN_POINT ( 'NONE',  ( 12.28004307584039623, -2.771121092977573586, 20.68249676638044932 ) ) ;
#33959=AXIS2_PLACEMENT_3D ( 'NONE', #63303, #5056, #12073 ) ;
#33966=SURFACE_STYLE_USAGE ( .BOTH. , #25341 ) ;
#34031=CARTESIAN_POINT ( 'NONE',  ( 4.284822031654965890, -1.092833614412281218, 104.4267991316945086 ) ) ;
#34033=COLOUR_RGB ( '', 0.66274510, 0.83137255, 0.94901961) ;
#34054=CARTESIAN_POINT ( 'NONE',  ( -4.051286199644062336, -48.60127012969241633, 103.8758286790404810 ) ) ;
#34073=CARTESIAN_POINT ( 'NONE',  ( -13.93074145947618447, -50.20627081601409714, 28.41232622077120595 ) ) ;
#34074=CARTESIAN_POINT ( 'NONE',  ( -5.000000000000000000, -14.08124958900141621, 11.76357069870068628 ) ) ;
#34087=CARTESIAN_POINT ( 'NONE',  ( 0.000000000000000000, -48.44948974278317877, 112.0000000000000000 ) ) ;
#34097=SURFACE_STYLE_FILL_AREA ( #43217 ) ;
#34099=CARTESIAN_POINT ( 'NONE',  ( 5.000000000000000000, -8.791602747472031965, -8.558960929452199551 ) ) ;
#34133=AXIS2_PLACEMENT_3D ( 'NONE', #103029, #62571, #84710 ) ;
#34189=( NAMED_UNIT ( * ) SI_UNIT ( $, .STERADIAN. ) SOLID_ANGLE_UNIT ( ) );
#34191=FACE_OUTER_BOUND ( 'NONE', #31451, .T. ) ;
#34225=PRESENTATION_STYLE_ASSIGNMENT (( #99437 ) ) ;
#34245=( NAMED_UNIT ( * ) SI_UNIT ( $, .STERADIAN. ) SOLID_ANGLE_UNIT ( ) );
#34262=DIRECTION ( 'NONE',  ( 0.000000000000000000, 0.000000000000000000, 1.000000000000000000 ) ) ;
#34295=CARTESIAN_POINT ( 'NONE',  ( -5.000000000000000000, -23.50454593378518453, -3.099858002006805613 ) ) ;
#34300=CARTESIAN_POINT ( 'NONE',  ( 2.464820640578141209, -49.72436178699376086, 44.56749791512065428 ) ) ;
#34321=CARTESIAN_POINT ( 'NONE',  ( 4.394945503249887864, -66.37976763068485297, 13.13806607437854446 ) ) ;
#34353=CARTESIAN_POINT ( 'NONE',  ( 5.000000000000000000, -14.30429124282204079, 12.05126107871916297 ) ) ;
#34359=STYLED_ITEM ( 'NONE', ( #105472 ), #90230 ) ;
#34368=CARTESIAN_POINT ( 'NONE',  ( 5.960000261375881792, -13.79916237020871073, 13.82526581198426108 ) ) ;
#34375=DIRECTION ( 'NONE',  ( -1.000000000000000000, -0.000000000000000000, -0.000000000000000000 ) ) ;
#34465=FILL_AREA_STYLE_COLOUR ( '', #1515 ) ;
#34498=CARTESIAN_POINT ( 'NONE',  ( 13.80788977721196886, 1.043589425646265889, 14.96468393437554845 ) ) ;
#34544=CARTESIAN_POINT ( 'NONE',  ( -27.99999999999999645, 0.000000000000000000, 0.000000000000000000 ) ) ;
#34590=FILL_AREA_STYLE ('',( #35653 ) ) ;
#34609=CARTESIAN_POINT ( 'NONE',  ( -5.000000000000000000, -13.83000330156203006, 11.07490067672335066 ) ) ;
#34616=MECHANICAL_DESIGN_GEOMETRIC_PRESENTATION_REPRESENTATION('',(#79541),#39207);
#34677=ORIENTED_EDGE ( 'NONE', *, *, #92997, .F. ) ;
#34686=VERTEX_POINT ( 'NONE', #53638 ) ;
#34690=CARTESIAN_POINT ( 'NONE',  ( -5.000000000000000000, -57.63307216814066436, 11.09944177371828289 ) ) ;
#34691=CARTESIAN_POINT ( 'NONE',  ( 0.000000000000000000, -1.200583151104953394, 112.0000000000000000 ) ) ;
#34723=EDGE_CURVE ( 'NONE', #88009, #103713, #29382, .T. ) ;
#34725=CARTESIAN_POINT ( 'NONE',  ( 3.787335548950983899, -1.092153040503932582, 104.1352136098632997 ) ) ;
#34732=CARTESIAN_POINT ( 'NONE',  ( -5.958501008717178138, -13.50719282745122563, 13.62690037880521920 ) ) ;
#34760=UNCERTAINTY_MEASURE_WITH_UNIT (LENGTH_MEASURE( 1.000000000000000082E-05 ), #76236, 'distance_accuracy_value', 'NONE');
#34772=( NAMED_UNIT ( * ) SI_UNIT ( $, .STERADIAN. ) SOLID_ANGLE_UNIT ( ) );
#34776=DIRECTION ( 'NONE',  ( 0.000000000000000000, -1.000000000000000000, 0.000000000000000000 ) ) ;
#34781=( BOUNDED_SURFACE ( )  B_SPLINE_SURFACE ( 3, 2, ( 
 ( #84343, #102108, #103187 ),
 ( #94581, #51957, #19657 ),
 ( #3957, #35285, #20187 ),
 ( #10436, #28268, #69756 ),
 ( #61137, #18566, #53039 ),
 ( #86498, #20729, #2344 ),
 ( #59548, #84872, #78364 ),
 ( #12557, #101049, #27203 ),
 ( #45496, #60093, #10957 ),
 ( #37423, #4486, #92415 ),
 ( #60620, #19119, #76769 ),
 ( #52489, #43874, #85409 ) ),
 .UNSPECIFIED., .F., .F., .F. ) 
 B_SPLINE_SURFACE_WITH_KNOTS ( ( 4, 2, 2, 2, 2, 4 ),
 ( 3, 3 ),
 ( -6.938893903907228378E-18, 0.001187588843296126778, 0.001781383264944193636, 0.002375177686592260494, 0.003562766529888394210, 0.004750355373184527927 ),
 ( 0.000000000000000000, 1.000000000000000000 ),
 .UNSPECIFIED. ) 
 GEOMETRIC_REPRESENTATION_ITEM ( )  RATIONAL_B_SPLINE_SURFACE ( (
 ( 1.000000000000000000, 0.9359444767143315635, 1.000000000000000000),
 ( 1.000000000000000000, 0.9295581727144293094, 1.000000000000000000),
 ( 1.000000000000000000, 0.9234593375675015370, 1.000000000000000000),
 ( 1.000000000000000000, 0.9150808072273350913, 1.000000000000000000),
 ( 1.000000000000000000, 0.9124161408737814227, 1.000000000000000000),
 ( 1.000000000000000000, 0.9074047588826392730, 1.000000000000000000),
 ( 1.000000000000000000, 0.9050663310860352917, 1.000000000000000000),
 ( 1.000000000000000000, 0.8987692007139010952, 1.000000000000000000),
 ( 1.000000000000000000, 0.8954627112850603865, 1.000000000000000000),
 ( 1.000000000000000000, 0.8909338199771259514, 1.000000000000000000),
 ( 1.000000000000000000, 0.8897377579433781714, 1.000000000000000000),
 ( 1.000000000000000000, 0.8897565210026093796, 1.000000000000000000) ) ) 
 REPRESENTATION_ITEM ( '' )  SURFACE ( )  );
#34807=CARTESIAN_POINT ( 'NONE',  ( 2.406968675509042921, -53.72544228834411939, 40.79299294490898831 ) ) ;
#34808=CARTESIAN_POINT ( 'NONE',  ( 3.202579070477590495, -48.99829897912727006, 104.2977202916031700 ) ) ;
#34853=CARTESIAN_POINT ( 'NONE',  ( 2.437998975427489778, -69.36002461153142917, 12.93669399823944133 ) ) ;
#34858=COLOUR_RGB ( '', 0.08235294, 0.09019608, 0.10196078) ;
#34868=CARTESIAN_POINT ( 'NONE',  ( 0.000000000000000000, -50.00000000000000000, 27.00000000000000000 ) ) ;
#34880=CARTESIAN_POINT ( 'NONE',  ( 4.999999999999960032, -13.68989806552482946, 13.02619096221374129 ) ) ;
#34903=CARTESIAN_POINT ( 'NONE',  ( -5.833333333333328596, -4.000000000000003553, 103.8776713793258608 ) ) ;
#34973=VERTEX_POINT ( 'NONE', #94798 ) ;
#34986=SURFACE_STYLE_FILL_AREA ( #91611 ) ;
#34991=CARTESIAN_POINT ( 'NONE',  ( -4.284822031654928587, -1.092833614412262122, 104.4267991316945370 ) ) ;
#34993=CIRCLE ( 'NONE', #103789, 9.999999999999998224 ) ;
#35021=CARTESIAN_POINT ( 'NONE',  ( 9.784980416533748837, -3.383375863471970391, 15.02393414357561596 ) ) ;
#35068=( LENGTH_UNIT ( ) NAMED_UNIT ( * ) SI_UNIT ( .MILLI., .METRE. ) );
#35070=FILL_AREA_STYLE_COLOUR ( '', #102045 ) ;
#35095=CARTESIAN_POINT ( 'NONE',  ( -9.301034387593361430, -2.623043302277163313, 14.76518561301066867 ) ) ;
#35131=CARTESIAN_POINT ( 'NONE',  ( -5.000000000000000000, -14.03205060597777809, 9.639947695590496579 ) ) ;
#35149=ADVANCED_FACE ( 'NONE', ( #62947 ), #90197, .F. ) ;
#35153=CARTESIAN_POINT ( 'NONE',  ( 5.849799967470243445, -7.702454342450949731, 13.78846266272944554 ) ) ;
#35159=UNCERTAINTY_MEASURE_WITH_UNIT (LENGTH_MEASURE( 1.000000000000000082E-05 ), #1533, 'distance_accuracy_value', 'NONE');
#35186=SURFACE_STYLE_FILL_AREA ( #51321 ) ;
#35196=CARTESIAN_POINT ( 'NONE',  ( 0.000000000000000000, -78.00000000000000000, 39.00000000000000000 ) ) ;
#35205=CARTESIAN_POINT ( 'NONE',  ( 5.385673916453011856, 3.157894736842103534, 14.66382285868950852 ) ) ;
#35210=FACE_OUTER_BOUND ( 'NONE', #50689, .T. ) ;
#35242=AXIS2_PLACEMENT_3D ( 'NONE', #66342, #59870, #9156 ) ;
#35245=CARTESIAN_POINT ( 'NONE',  ( 3.604576940039115218, -1.047841513645711764, 104.3731177596920787 ) ) ;
#35252=CARTESIAN_POINT ( 'NONE',  ( -15.18610346951687440, -6.148569791254295147, 13.68542098333100299 ) ) ;
#35276=CARTESIAN_POINT ( 'NONE',  ( 0.9999999999999940048, 0.000000000000000000, 101.0455488498966758 ) ) ;
#35285=CARTESIAN_POINT ( 'NONE',  ( 4.348929473936389734, -1.784082633676211449, 103.6864098602936082 ) ) ;
#35289=ORIENTED_EDGE ( 'NONE', *, *, #86962, .F. ) ;
#35291=( GEOMETRIC_REPRESENTATION_CONTEXT ( 3 ) GLOBAL_UNCERTAINTY_ASSIGNED_CONTEXT ( ( #68153 ) ) GLOBAL_UNIT_ASSIGNED_CONTEXT ( ( #106514, #59050, #25102 ) ) REPRESENTATION_CONTEXT ( 'NONE', 'WORKASPACE' ) );
#35337=CARTESIAN_POINT ( 'NONE',  ( 2.994908303143255957, -49.57328227368260087, 40.82351491602005211 ) ) ;
#35340=AXIS2_PLACEMENT_3D ( 'NONE', #76549, #60407, #37743 ) ;
#35364=CARTESIAN_POINT ( 'NONE',  ( 3.645564603016916649, -49.01020369241541630, 43.86897233032998145 ) ) ;
#35377=COLOUR_RGB ( '', 0.66274510, 0.83137255, 0.94901961) ;
#35429=CARTESIAN_POINT ( 'NONE',  ( -13.66195738444678831, -56.44203391523139146, 23.93843443166228724 ) ) ;
#35432=CARTESIAN_POINT ( 'NONE',  ( 9.112177013564760841, -0.3479193102801454995, 19.74070280225997109 ) ) ;
#35433=EDGE_LOOP ( 'NONE', ( #15896, #90418, #57944, #27854 ) ) ;
#35434=CYLINDRICAL_SURFACE ( 'NONE', #44229, 15.00000000000000000 ) ;
#35495=CARTESIAN_POINT ( 'NONE',  ( 3.048295934048691258, -53.45399299688504868, 40.66583558471658932 ) ) ;
#35552=ORIENTED_EDGE ( 'NONE', *, *, #5219, .T. ) ;
#35586=VERTEX_POINT ( 'NONE', #102611 ) ;
#35596=DIRECTION ( 'NONE',  ( 0.000000000000000000, 1.000000000000000000, 0.000000000000000000 ) ) ;
#35610=AXIS2_PLACEMENT_3D ( 'NONE', #4948, #78290, #62663 ) ;
#35636=SURFACE_STYLE_USAGE ( .BOTH. , #52300 ) ;
#35653=FILL_AREA_STYLE_COLOUR ( '', #18503 ) ;
#35715=CARTESIAN_POINT ( 'NONE',  ( 0.000000000000000000, -1.200583151104947843, 112.0000000000000000 ) ) ;
#35733=ADVANCED_FACE ( 'NONE', ( #22778 ), #62179, .T. ) ;
#35743=CARTESIAN_POINT ( 'NONE',  ( 0.000000000000000000, -50.00000000000000000, 122.0000000000000000 ) ) ;
#35750=CARTESIAN_POINT ( 'NONE',  ( 8.439582558336111262, -0.2091310867994085887, 19.51128387820496002 ) ) ;
#35769=ORIENTED_EDGE ( 'NONE', *, *, #14896, .F. ) ;
#35794=SURFACE_SIDE_STYLE ('',( #42238 ) ) ;
#35796=CARTESIAN_POINT ( 'NONE',  ( -13.50676536913941028, -9.130490673981565664, 11.91195374128086115 ) ) ;
#35797=CARTESIAN_POINT ( 'NONE',  ( -5.983613182656017493, -12.98062839397022294, 13.15810238988803071 ) ) ;
#35826=UNCERTAINTY_MEASURE_WITH_UNIT (LENGTH_MEASURE( 1.000000000000000082E-05 ), #40720, 'distance_accuracy_value', 'NONE');
#35830=CARTESIAN_POINT ( 'NONE',  ( -3.350247031702008993, -48.92879585575168022, 104.4269854689288053 ) ) ;
#35876=CARTESIAN_POINT ( 'NONE',  ( 3.552225580476869649, -53.17955991417163375, 40.54727264511482332 ) ) ;
#35888=CARTESIAN_POINT ( 'NONE',  ( 0.2916160024871935486, -70.53271932724192084, 13.00000000000000000 ) ) ;
#35891=CARTESIAN_POINT ( 'NONE',  ( -3.857142857142850989, -1.200583151104938517, 103.1763305333244318 ) ) ;
#35899=CARTESIAN_POINT ( 'NONE',  ( -2.757402973851224903, -49.69848065189508191, 40.86068941039670221 ) ) ;
#35967=TOROIDAL_SURFACE ( 'NONE', #46235, 8.499999999999992895, 0.5000000000000000000 ) ;
#35972=CARTESIAN_POINT ( 'NONE',  ( -13.48739679499482058, -55.04004794677399559, 23.24594036347893677 ) ) ;
#36020=AXIS2_PLACEMENT_3D ( 'NONE', #81019, #72922, #52377 ) ;
#36031=CARTESIAN_POINT ( 'NONE',  ( 5.000000000000000000, -13.80294717155101125, 10.52286356750360241 ) ) ;
#36037=ADVANCED_FACE ( 'NONE', ( #66936 ), #90672, .F. ) ;
#36040=CARTESIAN_POINT ( 'NONE',  ( 4.196261321702323244, -52.69005874581856119, 40.35766667076264014 ) ) ;
#36092=ORIENTED_EDGE ( 'NONE', *, *, #33808, .F. ) ;
#36100=SURFACE_SIDE_STYLE ('',( #68970 ) ) ;
#36104=CARTESIAN_POINT ( 'NONE',  ( -4.247379606276268760, -12.84324797163533383, -9.569866633816575430 ) ) ;
#36127=CARTESIAN_POINT ( 'NONE',  ( 1.000000000000000000, -5.000000000000015099, -14.14213562373094923 ) ) ;
#36128=AXIS2_PLACEMENT_3D ( 'NONE', #5245, #62952, #23038 ) ;
#36148=CARTESIAN_POINT ( 'NONE',  ( -30.00000000000000000, 1.714505518806294441E-15, 13.00000000000000000 ) ) ;
#36161=SURFACE_STYLE_FILL_AREA ( #77102 ) ;
#36202=CARTESIAN_POINT ( 'NONE',  ( -4.551587301587304957, -1.200583151104947843, 104.4018401814738155 ) ) ;
#36232=( LENGTH_UNIT ( ) NAMED_UNIT ( * ) SI_UNIT ( .MILLI., .METRE. ) );
#36247=ORIENTED_EDGE ( 'NONE', *, *, #74940, .T. ) ;
#36260=CIRCLE ( 'NONE', #96500, 8.142857142857131691 ) ;
#36289=SURFACE_STYLE_USAGE ( .BOTH. , #44338 ) ;
#36312=EDGE_CURVE ( 'NONE', #26304, #41710, #93321, .T. ) ;
#36321=CYLINDRICAL_SURFACE ( 'NONE', #7282, 4.000000000000000000 ) ;
#36322=PRESENTATION_STYLE_ASSIGNMENT (( #44371 ) ) ;
#36330=CARTESIAN_POINT ( 'NONE',  ( 4.003587701499093043, -1.050376533302863180, 104.5574048719304301 ) ) ;
#36334=( LENGTH_UNIT ( ) NAMED_UNIT ( * ) SI_UNIT ( .MILLI., .METRE. ) );
#36336=CARTESIAN_POINT ( 'NONE',  ( -6.999999999999975131, -12.54465221550630183, 8.223849511754991681 ) ) ;
#36349=CARTESIAN_POINT ( 'NONE',  ( 13.64654340589911818, -56.64216131223533779, 30.13167154758286159 ) ) ;
#36369=FACE_OUTER_BOUND ( 'NONE', #36773, .T. ) ;
#36378=CIRCLE ( 'NONE', #17472, 11.00000000000001066 ) ;
#36379=DIRECTION ( 'NONE',  ( 0.000000000000000000, 1.000000000000000000, 0.000000000000000000 ) ) ;
#36388=EDGE_CURVE ( 'NONE', #91492, #64161, #56037, .T. ) ;
#36398=CARTESIAN_POINT ( 'NONE',  ( -9.423567810130279554, -56.01223787097960383, 23.65038982378345622 ) ) ;
#36413=CARTESIAN_POINT ( 'NONE',  ( 5.823258015267495757, -50.68891529089922443, 39.73205700961069908 ) ) ;
#36434=CARTESIAN_POINT ( 'NONE',  ( -0.9278645722921005090, -50.01492575961955822, 40.97002731333736847 ) ) ;
#36481=ORIENTED_EDGE ( 'NONE', *, *, #105830, .F. ) ;
#36482=UNCERTAINTY_MEASURE_WITH_UNIT (LENGTH_MEASURE( 1.000000000000000082E-05 ), #97775, 'distance_accuracy_value', 'NONE');
#36503=CARTESIAN_POINT ( 'NONE',  ( -13.69901872062297166, -56.64640036516345134, 24.10656755472290769 ) ) ;
#36507=ORIENTED_EDGE ( 'NONE', *, *, #62702, .T. ) ;
#36520=EDGE_LOOP ( 'NONE', ( #91345, #43733, #28180, #48763 ) ) ;
#36548=CYLINDRICAL_SURFACE ( 'NONE', #49030, 4.000000000000000000 ) ;
#36595=( LENGTH_UNIT ( ) NAMED_UNIT ( * ) SI_UNIT ( .MILLI., .METRE. ) );
#36603=ORIENTED_EDGE ( 'NONE', *, *, #37199, .F. ) ;
#36605=DIRECTION ( 'NONE',  ( -0.000000000000000000, -1.000000000000000000, -0.000000000000000000 ) ) ;
#36631=CARTESIAN_POINT ( 'NONE',  ( -3.730558560396409096, -11.49689693085219311, -10.68063119932392802 ) ) ;
#36654=CARTESIAN_POINT ( 'NONE',  ( 6.163128221575932209, -12.12876728480159372, -8.844179776184985187 ) ) ;
#36660=COLOUR_RGB ( '', 0.31764706, 0.68627451, 0.89019608) ;
#36670=AXIS2_PLACEMENT_3D ( 'NONE', #23779, #66868, #99755 ) ;
#36673=EDGE_CURVE ( 'NONE', #47025, #87124, #16132, .T. ) ;
#36691=CARTESIAN_POINT ( 'NONE',  ( 1.545731922506520251, -0.02842019995825076015, 101.5782547351753351 ) ) ;
#36704=CARTESIAN_POINT ( 'NONE',  ( -15.31606227096485817, -0.5350865456626047179, 14.99202647884761852 ) ) ;
#36708=EDGE_CURVE ( 'NONE', #53428, #39260, #106099, .T. ) ;
#36713=CARTESIAN_POINT ( 'NONE',  ( 1.000000000000000444, -15.98025244997938721, -10.26003014047063822 ) ) ;
#36717=CARTESIAN_POINT ( 'NONE',  ( 0.000000000000000000, -4.000000000000003553, 122.0000000000000000 ) ) ;
#36735=( NAMED_UNIT ( * ) SI_UNIT ( $, .STERADIAN. ) SOLID_ANGLE_UNIT ( ) );
#36736=DIRECTION ( 'NONE',  ( 0.000000000000000000, 0.000000000000000000, 1.000000000000000000 ) ) ;
#36773=EDGE_LOOP ( 'NONE', ( #336, #3698, #11650, #90457 ) ) ;
#36786=EDGE_CURVE ( 'NONE', #33722, #99731, #71738, .T. ) ;
#36811=CARTESIAN_POINT ( 'NONE',  ( 6.520166676877810374, -0.2361713054966709524, 15.39474435275100284 ) ) ;
#36862=B_SPLINE_CURVE_WITH_KNOTS ( 'NONE', 3,
 ( #64007, #7316, #259, #48833, #90375, #14881, #33225, #105498, #40755, #49908 ),
 .UNSPECIFIED., .F., .F.,
 ( 4, 2, 2, 2, 4 ),
 ( 0.000000000000000000, 0.0008538222887801227108, 0.001707644577560245422, 0.002561466866340368024, 0.003415289155120490843 ),
 .UNSPECIFIED. ) ;
#36868=EDGE_LOOP ( 'NONE', ( #88102, #98609, #39020, #5812, #62278, #82446, #44997, #95065 ) ) ;
#36879=CARTESIAN_POINT ( 'NONE',  ( 0.9999999999999940048, -50.00000000000000000, 103.3397459621556180 ) ) ;
#36933=CARTESIAN_POINT ( 'NONE',  ( 2.047337005717745129, -49.86272114439862690, 44.73384807164315902 ) ) ;
#36950=CARTESIAN_POINT ( 'NONE',  ( -2.045670083595537037, -49.95306077403387945, 40.93770280784608673 ) ) ;
#36985=DIRECTION ( 'NONE',  ( 0.000000000000000000, 0.000000000000000000, -1.000000000000000000 ) ) ;
#36993=COLOUR_RGB ( '', 0.31764706, 0.68627451, 0.89019608) ;
#37046=SURFACE_SIDE_STYLE ('',( #12721 ) ) ;
#37057=EDGE_CURVE ( 'NONE', #94943, #43338, #102792, .T. ) ;
#37066=EDGE_LOOP ( 'NONE', ( #37826, #22944, #2569, #11716 ) ) ;
#37068=CARTESIAN_POINT ( 'NONE',  ( -4.571008445750557314, -2.193282516568174856, 102.5889671997070849 ) ) ;
#37069=CARTESIAN_POINT ( 'NONE',  ( -1.000000000000000444, -50.00000000000000000, 44.97220075561142494 ) ) ;
#37083=MECHANICAL_DESIGN_GEOMETRIC_PRESENTATION_REPRESENTATION('',(#42190),#93861);
#37086=SURFACE_STYLE_USAGE ( .BOTH. , #86684 ) ;
#37087=CARTESIAN_POINT ( 'NONE',  ( 5.000000000000000000, -15.62228920881129390, 12.61250543006183378 ) ) ;
#37116=CARTESIAN_POINT ( 'NONE',  ( -4.284822031654928587, -1.092833614412262122, 104.4267991316945370 ) ) ;
#37143=CARTESIAN_POINT ( 'NONE',  ( 2.182379536667797826, -70.50492906290401152, 13.16884392366768353 ) ) ;
#37152=CARTESIAN_POINT ( 'NONE',  ( -6.098092868604570782, -7.477803449953040804, 13.82040600116227758 ) ) ;
#37156=( NAMED_UNIT ( * ) PLANE_ANGLE_UNIT ( ) SI_UNIT ( $, .RADIAN. ) );
#37177=CARTESIAN_POINT ( 'NONE',  ( -5.000000000000000888, -4.000000000000000000, 42.58845726811989607 ) ) ;
#37181=CARTESIAN_POINT ( 'NONE',  ( 1.889561568099859423, -0.09386489487440055624, 101.9317830238467195 ) ) ;
#37199=EDGE_CURVE ( 'NONE', #88353, #56114, #6946, .T. ) ;
#37208=CARTESIAN_POINT ( 'NONE',  ( 1.509254614533485528, -0.02489260075662195343, 101.6144273468640336 ) ) ;
#37225=CARTESIAN_POINT ( 'NONE',  ( -9.960066834909762079, -3.067139625798588121, 15.24934138179222032 ) ) ;
#37255=CARTESIAN_POINT ( 'NONE',  ( -5.818631380449454049, -64.91365770770519816, 14.26591935523900645 ) ) ;
#37256=( NAMED_UNIT ( * ) PLANE_ANGLE_UNIT ( ) SI_UNIT ( $, .RADIAN. ) );
#37276=ORIENTED_EDGE ( 'NONE', *, *, #86051, .F. ) ;
#37286=EDGE_CURVE ( 'NONE', #82494, #74417, #61539, .T. ) ;
#37309=CIRCLE ( 'NONE', #56168, 8.857142857142855874 ) ;
#37345=CARTESIAN_POINT ( 'NONE',  ( -4.506320246070885993, -48.81713945999871385, 104.3949652630312528 ) ) ;
#37366=EDGE_CURVE ( 'NONE', #65995, #170, #51178, .T. ) ;
#37368=CARTESIAN_POINT ( 'NONE',  ( -3.677502082062779731, -1.015346567123904364, 104.5296620117540272 ) ) ;
#37371=UNCERTAINTY_MEASURE_WITH_UNIT (LENGTH_MEASURE( 1.000000000000000082E-05 ), #63636, 'distance_accuracy_value', 'NONE');
#37382=( GEOMETRIC_REPRESENTATION_CONTEXT ( 3 ) GLOBAL_UNCERTAINTY_ASSIGNED_CONTEXT ( ( #14541 ) ) GLOBAL_UNIT_ASSIGNED_CONTEXT ( ( #65980, #40117, #7733 ) ) REPRESENTATION_CONTEXT ( 'NONE', 'WORKASPACE' ) );
#37384=FILL_AREA_STYLE_COLOUR ( '', #2680 ) ;
#37388=CARTESIAN_POINT ( 'NONE',  ( -1.916513513606918240, -7.172711491781471160, -13.28747680017342248 ) ) ;
#37417=FACE_OUTER_BOUND ( 'NONE', #20713, .T. ) ;
#37423=CARTESIAN_POINT ( 'NONE',  ( 4.973317752991476048, -3.468598768254688380, 102.2736751349651456 ) ) ;
#37424=CARTESIAN_POINT ( 'NONE',  ( -3.405129524108836847, -48.85126520984761811, 104.5473292661494753 ) ) ;
#37463=FACE_OUTER_BOUND ( 'NONE', #2949, .T. ) ;
#37489=CARTESIAN_POINT ( 'NONE',  ( -1.000000000000000666, -50.00000000000000000, 44.97220075561143204 ) ) ;
#37585=CARTESIAN_POINT ( 'NONE',  ( -1.910791319121646126, -69.56563210985819978, 12.86688064138004961 ) ) ;
#37621=CARTESIAN_POINT ( 'NONE',  ( 13.93078765908243710, -50.20613146654194736, 28.41172023899451560 ) ) ;
#37625=( GEOMETRIC_REPRESENTATION_CONTEXT ( 3 ) GLOBAL_UNCERTAINTY_ASSIGNED_CONTEXT ( ( #65677 ) ) GLOBAL_UNIT_ASSIGNED_CONTEXT ( ( #83082, #101918, #91196 ) ) REPRESENTATION_CONTEXT ( 'NONE', 'WORKASPACE' ) );
#37631=MECHANICAL_DESIGN_GEOMETRIC_PRESENTATION_REPRESENTATION('',(#44528),#53147);
#37636=CARTESIAN_POINT ( 'NONE',  ( 0.9330442100808740147, -70.05675763226145136, 13.03100537459354413 ) ) ;
#37642=CARTESIAN_POINT ( 'NONE',  ( -2.106572258996926905, -49.79055979746641469, 102.5319188847123542 ) ) ;
#37662=ORIENTED_EDGE ( 'NONE', *, *, #66628, .T. ) ;
#37691=FILL_AREA_STYLE ('',( #79160 ) ) ;
#37694=CARTESIAN_POINT ( 'NONE',  ( 3.787335548944762209, -48.90784695950119243, 104.1352136098573453 ) ) ;
#37695=CARTESIAN_POINT ( 'NONE',  ( 0.8750000000000016653, -70.58759490697437400, 13.02737050516260098 ) ) ;
#37730=STYLED_ITEM ( 'NONE', ( #17938 ), #76671 ) ;
#37733=CARTESIAN_POINT ( 'NONE',  ( 0.000000000000000000, -4.000000000000003553, 27.00000000000000000 ) ) ;
#37743=DIRECTION ( 'NONE',  ( 0.000000000000000000, 0.000000000000000000, 1.000000000000000000 ) ) ;
#37749=CARTESIAN_POINT ( 'NONE',  ( 1.910332202385262690, -0.1361670080387644977, 102.2504571675851963 ) ) ;
#37760=CARTESIAN_POINT ( 'NONE',  ( -12.16150765691225999, -2.480561230130143624, 20.68473351390147386 ) ) ;
#37801=COLOUR_RGB ( '', 0.09019608, 0.27058824, 0.51372549) ;
#37826=ORIENTED_EDGE ( 'NONE', *, *, #99418, .F. ) ;
#37849=CARTESIAN_POINT ( 'NONE',  ( 8.999999999999996447, 0.000000000000000000, 42.58845726811989607 ) ) ;
#37872=( NAMED_UNIT ( * ) SI_UNIT ( $, .STERADIAN. ) SOLID_ANGLE_UNIT ( ) );
#37918=SURFACE_SIDE_STYLE ('',( #52456 ) ) ;
#37935=CARTESIAN_POINT ( 'NONE',  ( 3.386166871500281950, -49.13792346205087114, 104.0373179439116882 ) ) ;
#37947=CARTESIAN_POINT ( 'NONE',  ( 5.000000000000000888, -43.08885284240903957, 0.3536648518834484278 ) ) ;
#37976=ORIENTED_EDGE ( 'NONE', *, *, #3982, .F. ) ;
#37988=EDGE_CURVE ( 'NONE', #40622, #57919, #93132, .T. ) ;
#38017=SURFACE_STYLE_USAGE ( .BOTH. , #26217 ) ;
#38054=ADVANCED_FACE ( 'NONE', ( #78886 ), #60611, .T. ) ;
#38106=ORIENTED_EDGE ( 'NONE', *, *, #16832, .F. ) ;
#38111=COLOUR_RGB ( '', 0.08235294, 0.09019608, 0.10196078) ;
#38125=ORIENTED_EDGE ( 'NONE', *, *, #98804, .F. ) ;
#38146=CARTESIAN_POINT ( 'NONE',  ( 13.98736753405778543, -50.02671451802293490, 27.64795516495958339 ) ) ;
#38147=CARTESIAN_POINT ( 'NONE',  ( 5.000000000000000000, -13.85537367056137192, 10.16084852768616997 ) ) ;
#38199=( GEOMETRIC_REPRESENTATION_CONTEXT ( 3 ) GLOBAL_UNCERTAINTY_ASSIGNED_CONTEXT ( ( #31309 ) ) GLOBAL_UNIT_ASSIGNED_CONTEXT ( ( #15740, #90704, #66414 ) ) REPRESENTATION_CONTEXT ( 'NONE', 'WORKASPACE' ) );
#38204=CARTESIAN_POINT ( 'NONE',  ( 0.8750000000000016653, -70.58759490697437400, 13.02737050516260098 ) ) ;
#38210=CARTESIAN_POINT ( 'NONE',  ( -7.819788844806560668, -14.69552936754710792, 15.37580215694229224 ) ) ;
#38216=DIRECTION ( 'NONE',  ( 0.000000000000000000, 0.000000000000000000, -1.000000000000000000 ) ) ;
#38254=CIRCLE ( 'NONE', #3743, 14.00000000000000178 ) ;
#38270=DIRECTION ( 'NONE',  ( 1.000000000000000000, -0.000000000000000000, -0.000000000000000000 ) ) ;
#38271=CARTESIAN_POINT ( 'NONE',  ( 3.871024465589348207, -1.214821636234518998, 104.2728733527511906 ) ) ;
#38273=CARTESIAN_POINT ( 'NONE',  ( -30.00000000000000000, -54.00000000000000711, 27.11721482942554928 ) ) ;
#38281=CARTESIAN_POINT ( 'NONE',  ( -13.80956423950918754, 1.042457166890826903, 14.96477920397855854 ) ) ;
#38295=VERTEX_POINT ( 'NONE', #15367 ) ;
#38310=DIRECTION ( 'NONE',  ( 0.000000000000000000, 1.000000000000000000, 0.000000000000000000 ) ) ;
#38314=CARTESIAN_POINT ( 'NONE',  ( 1.561526116976854173, -49.96194285232682830, 101.5970966559196000 ) ) ;
#38324=CARTESIAN_POINT ( 'NONE',  ( -6.999999999999975131, -12.54465221550630183, 8.223849511754991681 ) ) ;
#38341=UNCERTAINTY_MEASURE_WITH_UNIT (LENGTH_MEASURE( 1.000000000000000082E-05 ), #10449, 'distance_accuracy_value', 'NONE');
#38391=TOROIDAL_SURFACE ( 'NONE', #84873, 8.499999999999992895, 0.5000000000000000000 ) ;
#38393=CARTESIAN_POINT ( 'NONE',  ( -1.000000000000000000, -26.68136363036562742, -6.178889730600807262 ) ) ;
#38400=DIRECTION ( 'NONE',  ( 0.000000000000000000, -1.000000000000000000, 0.000000000000000000 ) ) ;
#38416=CARTESIAN_POINT ( 'NONE',  ( -3.678498789086714016, -1.016373932518044532, 104.0112638849122959 ) ) ;
#38418=SURFACE_STYLE_FILL_AREA ( #6536 ) ;
#38422=FILL_AREA_STYLE ('',( #20682 ) ) ;
#38445=CARTESIAN_POINT ( 'NONE',  ( 13.60728112438141402, -56.44183047709488221, 30.29609480636782592 ) ) ;
#38459=CARTESIAN_POINT ( 'NONE',  ( 5.000000000000000888, -40.36147667352133084, -0.7651093971659219672 ) ) ;
#38477=CARTESIAN_POINT ( 'NONE',  ( -30.00000000000000000, 0.000000000000000000, 0.000000000000000000 ) ) ;
#38529=CARTESIAN_POINT ( 'NONE',  ( -12.06878958996594164, -6.474301304373300425, 19.90239611026824562 ) ) ;
#38575=ORIENTED_EDGE ( 'NONE', *, *, #76359, .T. ) ;
#38581=DIRECTION ( 'NONE',  ( 1.000000000000000000, -0.000000000000000000, -0.000000000000000000 ) ) ;
#38590=CARTESIAN_POINT ( 'NONE',  ( -13.38090213880806978, -54.00000000000000711, 31.11721482942554928 ) ) ;
#38601=CIRCLE ( 'NONE', #41955, 7.000000000000006217 ) ;
#38603=CARTESIAN_POINT ( 'NONE',  ( 13.64462615244698540, 1.169661571067718731, 14.95672857179070725 ) ) ;
#38607=CARTESIAN_POINT ( 'NONE',  ( -7.000000000000000000, -14.21727251091160404, 9.320362779991915758 ) ) ;
#38623=CARTESIAN_POINT ( 'NONE',  ( 6.999999999999993783, -4.000000000000005329, 102.2532056551910387 ) ) ;
#38640=( NAMED_UNIT ( * ) SI_UNIT ( $, .STERADIAN. ) SOLID_ANGLE_UNIT ( ) );
#38655=CARTESIAN_POINT ( 'NONE',  ( 13.77150638301485941, -50.98655578268471089, 24.47399976921181519 ) ) ;
#38666=CARTESIAN_POINT ( 'NONE',  ( 3.567823017641492012, -0.9316928131313192418, 103.5075034329448158 ) ) ;
#38681=DIRECTION ( 'NONE',  ( -1.000000000000000000, -0.000000000000000000, -0.000000000000000000 ) ) ;
#38715=CARTESIAN_POINT ( 'NONE',  ( 3.347764182284693746, -69.92877180609107768, 13.40431717882780305 ) ) ;
#38722=CARTESIAN_POINT ( 'NONE',  ( -4.150157478975854630, -8.979899373663997153, 13.48960253578191981 ) ) ;
#38741=CARTESIAN_POINT ( 'NONE',  ( 1.714505518806294638E-15, -80.00000000000000000, 13.00000000000000000 ) ) ;
#38754=CARTESIAN_POINT ( 'NONE',  ( -4.051286199644060559, -48.60127012969240923, 103.8758286790404952 ) ) ;
#38772=CARTESIAN_POINT ( 'NONE',  ( 3.867083106918059787, -1.182498200942901256, 103.9715359882816159 ) ) ;
#38792=CARTESIAN_POINT ( 'NONE',  ( -15.44819439224355584, -0.7587808896114125456, 14.98257521071344911 ) ) ;
#38820=TOROIDAL_SURFACE ( 'NONE', #47414, 13.00000000000000000, 2.000000000000000000 ) ;
#38822=CARTESIAN_POINT ( 'NONE',  ( -6.113204517632431667, -61.77363733626824427, 14.40517576086940643 ) ) ;
#38826=FILL_AREA_STYLE_COLOUR ( '', #89219 ) ;
#38881=FACE_OUTER_BOUND ( 'NONE', #84945, .T. ) ;
#38921=AXIS2_PLACEMENT_3D ( 'NONE', #23464, #103818, #40143 ) ;
#38930=DIRECTION ( 'NONE',  ( 0.000000000000000000, 0.000000000000000000, -1.000000000000000000 ) ) ;
#38933=FACE_OUTER_BOUND ( 'NONE', #83372, .T. ) ;
#38978=CARTESIAN_POINT ( 'NONE',  ( 5.000000000000000888, -68.69132998577062210, 12.24443901500599807 ) ) ;
#38980=CARTESIAN_POINT ( 'NONE',  ( 9.283862214035533356, -2.881445901645539820, 14.75262417026159412 ) ) ;
#38990=ADVANCED_FACE ( 'NONE', ( #25661 ), #65311, .F. ) ;
#39000=CARTESIAN_POINT ( 'NONE',  ( -4.153385784896416411, -48.47379020312671827, 43.45327407259872388 ) ) ;
#39020=ORIENTED_EDGE ( 'NONE', *, *, #99714, .T. ) ;
#39053=CARTESIAN_POINT ( 'NONE',  ( -10.99438716495651214, -10.50257049600883263, 18.32467394275776584 ) ) ;
#39142=DIRECTION ( 'NONE',  ( 0.000000000000000000, 0.000000000000000000, -1.000000000000000000 ) ) ;
#39146=FILL_AREA_STYLE ('',( #22969 ) ) ;
#39165=ADVANCED_FACE ( 'NONE', ( #50282 ), #41666, .F. ) ;
#39182=CARTESIAN_POINT ( 'NONE',  ( 0.000000000000000000, -4.000000000000003553, 112.0000000000000000 ) ) ;
#39205=CARTESIAN_POINT ( 'NONE',  ( -3.352941176470589646, -48.79941684889505638, 104.5794940929807524 ) ) ;
#39207=( GEOMETRIC_REPRESENTATION_CONTEXT ( 3 ) GLOBAL_UNCERTAINTY_ASSIGNED_CONTEXT ( ( #2748 ) ) GLOBAL_UNIT_ASSIGNED_CONTEXT ( ( #97020, #47923, #72222 ) ) REPRESENTATION_CONTEXT ( 'NONE', 'WORKASPACE' ) );
#39226=CARTESIAN_POINT ( 'NONE',  ( 3.668358303306901380, -1.103610535301068563, 104.6014313550541175 ) ) ;
#39228=CARTESIAN_POINT ( 'NONE',  ( -4.551587301587301404, -1.200583151104944513, 104.4018401814738013 ) ) ;
#39238=CARTESIAN_POINT ( 'NONE',  ( 6.611670918688536958, -11.93296314122835078, 9.735702799543512143 ) ) ;
#39246=EDGE_CURVE ( 'NONE', #76952, #8366, #84255, .T. ) ;
#39258=CARTESIAN_POINT ( 'NONE',  ( -8.830818839454250835, -4.082547224762430815, 14.50827515792006217 ) ) ;
#39260=VERTEX_POINT ( 'NONE', #2795 ) ;
#39297=CARTESIAN_POINT ( 'NONE',  ( -3.991147588110737665, -48.94961024798170257, 104.5610969444638698 ) ) ;
#39307=( NAMED_UNIT ( * ) SI_UNIT ( $, .STERADIAN. ) SOLID_ANGLE_UNIT ( ) );
#39331=CARTESIAN_POINT ( 'NONE',  ( -5.919014529058259200, -3.357354825248717523E-15, 18.71571423408288126 ) ) ;
#39343=PRESENTATION_STYLE_ASSIGNMENT (( #6405 ) ) ;
#39346=ORIENTED_EDGE ( 'NONE', *, *, #40161, .T. ) ;
#39351=LINE ( 'NONE', #29685, #75357 ) ;
#39359=CARTESIAN_POINT ( 'NONE',  ( -5.000000000000038192, -13.46492586503062050, 12.82257630554777883 ) ) ;
#39408=CIRCLE ( 'NONE', #3204, 4.000000000000003553 ) ;
#39412=ORIENTED_EDGE ( 'NONE', *, *, #83053, .T. ) ;
#39416=CARTESIAN_POINT ( 'NONE',  ( 9.981919929974880645, -50.02752553709775896, 27.65434374221348435 ) ) ;
#39420=CARTESIAN_POINT ( 'NONE',  ( -10.00250692948970865, -49.99952737940893144, 26.86088010484640165 ) ) ;
#39429=B_SPLINE_CURVE_WITH_KNOTS ( 'NONE', 3,
 ( #20496, #55433, #22045, #104524, #71622, #37181, #46825, #30678, #54356, #61981 ),
 .UNSPECIFIED., .F., .F.,
 ( 4, 2, 2, 2, 4 ),
 ( -4.786264512459483439E-05, 0.0004191110641584722693, 0.0008860847734415393121, 0.001820032192007644016, 0.003687927029139882913 ),
 .UNSPECIFIED. ) ;
#39453=CARTESIAN_POINT ( 'NONE',  ( -27.99999999999999645, 0.000000000000000000, -13.00000000000000000 ) ) ;
#39466=CARTESIAN_POINT ( 'NONE',  ( -3.037443755948696200, -0.5477000578292443578, 103.2087721268169389 ) ) ;
#39468=DIRECTION ( 'NONE',  ( 0.000000000000000000, 0.000000000000000000, 1.000000000000000000 ) ) ;
#39513=CARTESIAN_POINT ( 'NONE',  ( 4.999999999996198596, -56.64186896439935026, 6.232146447249109933 ) ) ;
#39515=CARTESIAN_POINT ( 'NONE',  ( 7.317451043433990776, -6.276491506186944846, 13.99669291930579007 ) ) ;
#39547=CARTESIAN_POINT ( 'NONE',  ( -9.934750400155193617, -57.86805517166717294, 28.16945530398552222 ) ) ;
#39564=ORIENTED_EDGE ( 'NONE', *, *, #92680, .T. ) ;
#39578=ORIENTED_EDGE ( 'NONE', *, *, #48024, .T. ) ;
#39663=DIRECTION ( 'NONE',  ( -0.000000000000000000, 0.5482566341169983204, 0.8363101477004208917 ) ) ;
#39677=CARTESIAN_POINT ( 'NONE',  ( -2.261820640632148827, -69.44553280094153536, 12.91242553541718152 ) ) ;
#39680=AXIS2_PLACEMENT_3D ( 'NONE', #92496, #18649, #51506 ) ;
#39733=ORIENTED_EDGE ( 'NONE', *, *, #13177, .F. ) ;
#39735=MECHANICAL_DESIGN_GEOMETRIC_PRESENTATION_REPRESENTATION('',(#88007),#58677);
#39763=CARTESIAN_POINT ( 'NONE',  ( 5.000000000000000000, -13.80294717177706154, 10.52286356751840479 ) ) ;
#39782=PLANE ( 'NONE',  #68207 ) ;
#39813=CARTESIAN_POINT ( 'NONE',  ( -4.844458925425546347, -47.14101111564401947, 103.3760426044494807 ) ) ;
#39831=ORIENTED_EDGE ( 'NONE', *, *, #6161, .T. ) ;
#39839=EDGE_CURVE ( 'NONE', #63106, #67261, #75597, .T. ) ;
#39844=CARTESIAN_POINT ( 'NONE',  ( 3.910135399454936600, -48.93965050918993143, 104.5757312272370712 ) ) ;
#39868=CARTESIAN_POINT ( 'NONE',  ( -3.415268428525006339, -0.8295777316436665494, 103.8819066263154411 ) ) ;
#39873=ORIENTED_EDGE ( 'NONE', *, *, #4373, .F. ) ;
#39876=CARTESIAN_POINT ( 'NONE',  ( -5.977446511990853750, -14.23238268868709611, 14.05797248976396574 ) ) ;
#39935=CARTESIAN_POINT ( 'NONE',  ( 9.286995370816610418, -52.22232280126255688, 30.70990524772856034 ) ) ;
#39937=SURFACE_SIDE_STYLE ('',( #48001 ) ) ;
#39940=CARTESIAN_POINT ( 'NONE',  ( -9.499205784528923502, -51.35693084752516313, 30.13083833152229829 ) ) ;
#39983=AXIS2_PLACEMENT_3D ( 'NONE', #10823, #93898, #100907 ) ;
#39985=AXIS2_PLACEMENT_3D ( 'NONE', #45682, #40753, #97386 ) ;
#40006=CARTESIAN_POINT ( 'NONE',  ( 0.000000000000000000, -50.00000000000000000, 27.00000000000000000 ) ) ;
#40016=CARTESIAN_POINT ( 'NONE',  ( 13.45079846400083312, -54.00000000000000711, 23.11721482942554928 ) ) ;
#40026=CARTESIAN_POINT ( 'NONE',  ( 9.574118164638793615, -56.64626512664418811, 24.10642939627973291 ) ) ;
#40031=CARTESIAN_POINT ( 'NONE',  ( 8.018229784881205191, -5.437562848952134154, 14.17839565075627739 ) ) ;
#40039=VERTEX_POINT ( 'NONE', #50556 ) ;
#40053=CARTESIAN_POINT ( 'NONE',  ( -7.000000000000000000, -46.00000000000000000, 39.12435565298213902 ) ) ;
#40075=( LENGTH_UNIT ( ) NAMED_UNIT ( * ) SI_UNIT ( .MILLI., .METRE. ) );
#40101=ORIENTED_EDGE ( 'NONE', *, *, #33268, .F. ) ;
#40102=CARTESIAN_POINT ( 'NONE',  ( -4.783461066586094823, -47.30494748504202107, 42.83084740999873219 ) ) ;
#40108=VERTEX_POINT ( 'NONE', #20405 ) ;
#40117=( NAMED_UNIT ( * ) PLANE_ANGLE_UNIT ( ) SI_UNIT ( $, .RADIAN. ) );
#40143=DIRECTION ( 'NONE',  ( 0.000000000000000000, -0.000000000000000000, 1.000000000000000000 ) ) ;
#40161=EDGE_CURVE ( 'NONE', #67261, #71609, #17441, .T. ) ;
#40184=CARTESIAN_POINT ( 'NONE',  ( -5.104025146928732326, -62.81240710122727222, 13.92109052487369603 ) ) ;
#40198=ORIENTED_EDGE ( 'NONE', *, *, #97486, .F. ) ;
#40204=SURFACE_STYLE_USAGE ( .BOTH. , #74156 ) ;
#40241=CARTESIAN_POINT ( 'NONE',  ( 9.795930887471511639, -12.69766919046054277, 16.99563166591020646 ) ) ;
#40248=FACE_OUTER_BOUND ( 'NONE', #82886, .T. ) ;
#40258=ORIENTED_EDGE ( 'NONE', *, *, #78693, .F. ) ;
#40265=CARTESIAN_POINT ( 'NONE',  ( -4.973317752991481377, -3.468598768254719911, 102.2736751349651456 ) ) ;
#40276=CARTESIAN_POINT ( 'NONE',  ( 5.000000000000000000, -12.33523449218792223, 10.71643274013084657 ) ) ;
#40305=MECHANICAL_DESIGN_GEOMETRIC_PRESENTATION_REPRESENTATION('',(#105738),#69572);
#40313=CARTESIAN_POINT ( 'NONE',  ( -6.999999999999999112, -14.05766640829038394, -5.232782735144285269 ) ) ;
#40326=CARTESIAN_POINT ( 'NONE',  ( -5.374793246923619705, -47.77528324145959715, 104.0614974883207395 ) ) ;
#40357=CARTESIAN_POINT ( 'NONE',  ( -4.999999999999993783, -4.000000000000003553, 102.2532056551910387 ) ) ;
#40362=FACE_OUTER_BOUND ( 'NONE', #68541, .T. ) ;
#40366=CARTESIAN_POINT ( 'NONE',  ( -5.385673916453011856, 3.157894736842102645, 14.66382285868951030 ) ) ;
#40393=CARTESIAN_POINT ( 'NONE',  ( -5.000000000000000000, -14.73708290047480496, 12.39211607762596401 ) ) ;
#40412=( GEOMETRIC_REPRESENTATION_CONTEXT ( 3 ) GLOBAL_UNCERTAINTY_ASSIGNED_CONTEXT ( ( #103136 ) ) GLOBAL_UNIT_ASSIGNED_CONTEXT ( ( #25715, #49929, #74728 ) ) REPRESENTATION_CONTEXT ( 'NONE', 'WORKASPACE' ) );
#40446=CARTESIAN_POINT ( 'NONE',  ( 2.539812460490211254, -69.30643486802681252, 12.95064966738993206 ) ) ;
#40454=CARTESIAN_POINT ( 'NONE',  ( 9.125013381092353271, -53.47235446719983543, 31.09113645985706142 ) ) ;
#40459=CARTESIAN_POINT ( 'NONE',  ( -9.378402013738298848, -52.21550925151184686, 23.52762072402763849 ) ) ;
#40513=CARTESIAN_POINT ( 'NONE',  ( -11.33763709711443823, 2.316981289466677918, 14.82083525685649228 ) ) ;
#40548=CARTESIAN_POINT ( 'NONE',  ( -3.454253436624959317, -0.8414180287960622007, 103.7259032015042379 ) ) ;
#40556=CARTESIAN_POINT ( 'NONE',  ( 8.826976704351871206, -4.090868165775439103, 14.50637990094349306 ) ) ;
#40560=CARTESIAN_POINT ( 'NONE',  ( -3.037443755949079005, -49.45229994217047675, 103.2087721268168252 ) ) ;
#40581=CARTESIAN_POINT ( 'NONE',  ( -5.681858674226697659, -50.93014719887724340, 39.79579700850658952 ) ) ;
#40586=CARTESIAN_POINT ( 'NONE',  ( -10.00248409573528896, -58.00033248952951936, 26.85804522429446095 ) ) ;
#40600=ORIENTED_EDGE ( 'NONE', *, *, #100251, .F. ) ;
#40622=VERTEX_POINT ( 'NONE', #85771 ) ;
#40631=( GEOMETRIC_REPRESENTATION_CONTEXT ( 3 ) GLOBAL_UNCERTAINTY_ASSIGNED_CONTEXT ( ( #79296 ) ) GLOBAL_UNIT_ASSIGNED_CONTEXT ( ( #58061, #90985, #105038 ) ) REPRESENTATION_CONTEXT ( 'NONE', 'WORKASPACE' ) );
#40651=EDGE_CURVE ( 'NONE', #5701, #41862, #49791, .T. ) ;
#40669=ORIENTED_EDGE ( 'NONE', *, *, #78625, .F. ) ;
#40699=FACE_OUTER_BOUND ( 'NONE', #97171, .T. ) ;
#40703=VERTEX_POINT ( 'NONE', #22640 ) ;
#40713=CARTESIAN_POINT ( 'NONE',  ( -5.100994920550437683, -63.33738541091079810, 13.92370273215852627 ) ) ;
#40720=( LENGTH_UNIT ( ) NAMED_UNIT ( * ) SI_UNIT ( .MILLI., .METRE. ) );
#40729=SURFACE_SIDE_STYLE ('',( #74151 ) ) ;
#40751=CARTESIAN_POINT ( 'NONE',  ( -4.999999999999999112, -34.80414770699324833, 1.298653836421715946 ) ) ;
#40753=DIRECTION ( 'NONE',  ( 0.000000000000000000, 1.000000000000000000, -5.401608413889052066E-13 ) ) ;
#40755=CARTESIAN_POINT ( 'NONE',  ( 15.10022144576333503, -0.2188905726113574979, 15.00000000000000178 ) ) ;
#40763=CARTESIAN_POINT ( 'NONE',  ( -0.8750000000009725554, -70.58759490697451611, 13.02737050516266848 ) ) ;
#40769=CARTESIAN_POINT ( 'NONE',  ( 6.655774809717873275, -15.37882222362587470, 14.67993930426211513 ) ) ;
#40773=CARTESIAN_POINT ( 'NONE',  ( 3.594139794580319069, -68.26681892886726644, 13.09870760474886531 ) ) ;
#40789=( NAMED_UNIT ( * ) PLANE_ANGLE_UNIT ( ) SI_UNIT ( $, .RADIAN. ) );
#40790=STYLED_ITEM ( 'NONE', ( #44638 ), #58421 ) ;
#40792=CARTESIAN_POINT ( 'NONE',  ( 5.232798140227935768, -1.976627073750571117, 104.1190344879414056 ) ) ;
#40794=UNCERTAINTY_MEASURE_WITH_UNIT (LENGTH_MEASURE( 1.000000000000000082E-05 ), #29367, 'distance_accuracy_value', 'NONE');
#40803=FILL_AREA_STYLE ('',( #7364 ) ) ;
#40805=DIRECTION ( 'NONE',  ( -1.000000000000000000, -0.000000000000000000, -0.000000000000000000 ) ) ;
#40817=CARTESIAN_POINT ( 'NONE',  ( 6.437509419382464237, -11.87447412552789139, 10.48822171390117930 ) ) ;
#40824=CARTESIAN_POINT ( 'NONE',  ( 4.844458925424167894, -47.14101111564401236, 103.3760426044467096 ) ) ;
#40856=CARTESIAN_POINT ( 'NONE',  ( -4.999999999999993783, -46.00000000000000000, 102.2532056551910387 ) ) ;
#40857=CARTESIAN_POINT ( 'NONE',  ( -1.000000000000000222, -5.000000000000000000, -14.14213562373095101 ) ) ;
#40862=DIRECTION ( 'NONE',  ( 0.000000000000000000, 1.000000000000000000, 0.000000000000000000 ) ) ;
#40865=UNCERTAINTY_MEASURE_WITH_UNIT (LENGTH_MEASURE( 1.000000000000000082E-05 ), #88312, 'distance_accuracy_value', 'NONE');
#40904=CARTESIAN_POINT ( 'NONE',  ( 0.000000000000000000, -4.000000000000003553, 27.00000000000000000 ) ) ;
#40927=CARTESIAN_POINT ( 'NONE',  ( -5.000000000000001776, -15.62228920881132055, 13.86359191440428873 ) ) ;
#40951=CARTESIAN_POINT ( 'NONE',  ( 9.960026500325596999, -3.066375081864128660, 15.24961307665604870 ) ) ;
#40982=CARTESIAN_POINT ( 'NONE',  ( 1.907980674488920503, -69.56148085505145673, 12.86680972871674911 ) ) ;
#40988=CARTESIAN_POINT ( 'NONE',  ( 9.819569948016248162, -50.41307743780032524, 28.90708029074982477 ) ) ;
#41021=CARTESIAN_POINT ( 'NONE',  ( -4.999999999999993783, -46.00000000000000000, 102.2532056551910387 ) ) ;
#41055=DIRECTION ( 'NONE',  ( 0.000000000000000000, 0.000000000000000000, 1.000000000000000000 ) ) ;
#41079=CIRCLE ( 'NONE', #82424, 7.000000000000006217 ) ;
#41084=CARTESIAN_POINT ( 'NONE',  ( -3.718188220749848671, -1.049015004457380495, 104.2423402216923876 ) ) ;
#41093=CARTESIAN_POINT ( 'NONE',  ( 11.87102759641705063, -7.549635373525221738, 19.57279676713838157 ) ) ;
#41098=CARTESIAN_POINT ( 'NONE',  ( -0.9999999999999941158, -50.00000000000000000, 101.0455488498966758 ) ) ;
#41123=CARTESIAN_POINT ( 'NONE',  ( -9.125013381092353271, -54.52764553280017168, 31.09113645985706142 ) ) ;
#41181=DIRECTION ( 'NONE',  ( -1.096832036894112098E-16, 0.000000000000000000, -1.000000000000000000 ) ) ;
#41191=( NAMED_UNIT ( * ) SI_UNIT ( $, .STERADIAN. ) SOLID_ANGLE_UNIT ( ) );
#41213=AXIS2_PLACEMENT_3D ( 'NONE', #27525, #43656, #76545 ) ;
#41216=( NAMED_UNIT ( * ) PLANE_ANGLE_UNIT ( ) SI_UNIT ( $, .RADIAN. ) );
#41232=CIRCLE ( 'NONE', #3361, 14.00000000000000178 ) ;
#41235=CARTESIAN_POINT ( 'NONE',  ( -15.95421105470541967, -2.592376812160994248, 14.77701819664088845 ) ) ;
#41241=ORIENTED_EDGE ( 'NONE', *, *, #71814, .T. ) ;
#41248=CARTESIAN_POINT ( 'NONE',  ( -5.043559054062717983, -67.66457034734504816, 13.93851206790711039 ) ) ;
#41257=CARTESIAN_POINT ( 'NONE',  ( 3.857142857142853209, -48.79941684889505638, 103.1763305333244176 ) ) ;
#41283=CARTESIAN_POINT ( 'NONE',  ( 30.00000000000000000, 0.000000000000000000, 0.000000000000000000 ) ) ;
#41288=CARTESIAN_POINT ( 'NONE',  ( 2.088718892540413652, -49.85129056402630709, 44.71921988607925158 ) ) ;
#41307=LINE ( 'NONE', #25157, #27341 ) ;
#41309=CARTESIAN_POINT ( 'NONE',  ( 5.881047590711852457, -64.51600253823789899, 14.29494541094543081 ) ) ;
#41321=LINE ( 'NONE', #63496, #15399 ) ;
#41323=FACE_OUTER_BOUND ( 'NONE', #14733, .T. ) ;
#41336=CARTESIAN_POINT ( 'NONE',  ( 6.158544544230133866, -12.16561743015171970, 11.88011416285994848 ) ) ;
#41357=CARTESIAN_POINT ( 'NONE',  ( 4.031080902170580238, -48.62189207507206845, 103.0284855429844555 ) ) ;
#41375=CARTESIAN_POINT ( 'NONE',  ( -7.000000000000003553, -13.84208499319765195, -5.811933785473016201 ) ) ;
#41391=CARTESIAN_POINT ( 'NONE',  ( -4.999999999999993783, -46.26205164319887331, 102.2532056550983128 ) ) ;
#41395=PRESENTATION_STYLE_ASSIGNMENT (( #362 ) ) ;
#41415=FACE_OUTER_BOUND ( 'NONE', #103710, .T. ) ;
#41424=DIRECTION ( 'NONE',  ( 0.000000000000000000, 1.000000000000000000, 0.000000000000000000 ) ) ;
#41430=CARTESIAN_POINT ( 'NONE',  ( -5.942578734303295640, -0.1159328135225491108, 15.36885066084568408 ) ) ;
#41445=VERTEX_POINT ( 'NONE', #8558 ) ;
#41455=CARTESIAN_POINT ( 'NONE',  ( -4.999999999999960920, -12.67914701491841889, 11.71967441880940797 ) ) ;
#41472=AXIS2_PLACEMENT_3D ( 'NONE', #6764, #65005, #22460 ) ;
#41477=CARTESIAN_POINT ( 'NONE',  ( 15.94101669773376884, -2.916571449501480284, 14.71579249486925889 ) ) ;
#41525=STYLED_ITEM ( 'NONE', ( #78206 ), #19125 ) ;
#41538=CARTESIAN_POINT ( 'NONE',  ( -12.16221469084096540, -2.476455199593412537, 20.68589871816672243 ) ) ;
#41546=EDGE_CURVE ( 'NONE', #88345, #92559, #84136, .T. ) ;
#41552=CARTESIAN_POINT ( 'NONE',  ( -0.3351512077620020236, -69.52513701336809504, 12.72773188590259252 ) ) ;
#41595=DIRECTION ( 'NONE',  ( 0.000000000000000000, 1.000000000000000000, 0.000000000000000000 ) ) ;
#41599=ADVANCED_FACE ( 'NONE', ( #15462 ), #79793, .F. ) ;
#41606=EDGE_LOOP ( 'NONE', ( #97772, #85, #95334, #20039 ) ) ;
#41616=CARTESIAN_POINT ( 'NONE',  ( 10.00250692948970865, -58.00047262059107567, 26.86088010484640165 ) ) ;
#41619=SURFACE_SIDE_STYLE ('',( #34097 ) ) ;
#41628=SURFACE_SIDE_STYLE ('',( #65373 ) ) ;
#41647=CARTESIAN_POINT ( 'NONE',  ( -3.848469685774049243, -52.98046562515381197, 40.46677497459211992 ) ) ;
#41666=CYLINDRICAL_SURFACE ( 'NONE', #44505, 2.000000000000001776 ) ;
#41680=VECTOR ( 'NONE', #2009, 1000.000000000000000 ) ;
#41694=EDGE_CURVE ( 'NONE', #35586, #17242, #68057, .T. ) ;
#41695=DIRECTION ( 'NONE',  ( 0.000000000000000000, 1.000000000000000000, 0.000000000000000000 ) ) ;
#41702=AXIS2_PLACEMENT_3D ( 'NONE', #33162, #56863, #42282 ) ;
#41704=STYLED_ITEM ( 'NONE', ( #79512 ), #104825 ) ;
#41710=VERTEX_POINT ( 'NONE', #85540 ) ;
#41718=CARTESIAN_POINT ( 'NONE',  ( -6.999999995588868984, -13.84708942052845870, -5.798489586938165630 ) ) ;
#41776=CARTESIAN_POINT ( 'NONE',  ( 0.9999999999999954481, -54.00000000000000711, 44.97220075561143204 ) ) ;
#41781=CARTESIAN_POINT ( 'NONE',  ( -5.414402257315187761, -66.65695130796692069, 14.08782732736250942 ) ) ;
#41788=CARTESIAN_POINT ( 'NONE',  ( -3.352941176470600304, -1.200583151104954283, 104.5794940929807524 ) ) ;
#41796=ORIENTED_EDGE ( 'NONE', *, *, #21945, .F. ) ;
#41835=CARTESIAN_POINT ( 'NONE',  ( -2.514199206790655783, -49.70878148651267026, 102.6057069765799099 ) ) ;
#41838=CARTESIAN_POINT ( 'NONE',  ( 5.044949049065960089, -67.63307031760351151, 13.94001772754543644 ) ) ;
#41844=CARTESIAN_POINT ( 'NONE',  ( 4.999999999999992006, -46.27603786271895814, 102.2532056551910387 ) ) ;
#41854=CARTESIAN_POINT ( 'NONE',  ( 5.833333333333327708, -3.728231135448883737, 103.8776713793258324 ) ) ;
#41862=VERTEX_POINT ( 'NONE', #97321 ) ;
#41867=CARTESIAN_POINT ( 'NONE',  ( 5.000000000000001776, -14.45898243499974711, 13.52154848216171068 ) ) ;
#41880=CARTESIAN_POINT ( 'NONE',  ( 5.961320375100143565, -13.36618214390661841, 13.51689209302652728 ) ) ;
#41886=CARTESIAN_POINT ( 'NONE',  ( 4.999999999999993783, -46.00000000000000000, 102.2532056551910387 ) ) ;
#41904=MECHANICAL_DESIGN_GEOMETRIC_PRESENTATION_REPRESENTATION('',(#12631),#16034);
#41927=UNCERTAINTY_MEASURE_WITH_UNIT (LENGTH_MEASURE( 1.000000000000000082E-05 ), #10877, 'distance_accuracy_value', 'NONE');
#41955=AXIS2_PLACEMENT_3D ( 'NONE', #80026, #13165, #86572 ) ;
#41974=FACE_OUTER_BOUND ( 'NONE', #31033, .T. ) ;
#41984=( BOUNDED_SURFACE ( )  B_SPLINE_SURFACE ( 3, 2, ( 
 ( #99398, #58440, #2300 ),
 ( #68114, #10920, #41718 ),
 ( #17463, #683, #1224 ),
 ( #49804, #18529, #84305 ),
 ( #66526, #43840, #26122 ),
 ( #82710, #51390, #2842 ),
 ( #50328, #83235, #98870 ),
 ( #10401, #25030, #57886 ),
 ( #67068, #74602, #99949 ),
 ( #42777, #58978, #91865 ),
 ( #17991, #75670, #3923 ),
 ( #37388, #95070, #20694 ),
 ( #13583, #53532, #53003 ),
 ( #54034, #44383, #3389 ) ),
 .UNSPECIFIED., .F., .F., .F. ) 
 B_SPLINE_SURFACE_WITH_KNOTS ( ( 4, 2, 2, 2, 2, 2, 4 ),
 ( 3, 3 ),
 ( 1.301042606982605321E-18, 0.002028361404254498158, 0.004056722808508994582, 0.006085084212763491006, 0.008113445617017987430, 0.01217016842552698028, 0.01622689123403597486 ),
 ( 0.000000000000000000, 1.000000000000000000 ),
 .UNSPECIFIED. ) 
 GEOMETRIC_REPRESENTATION_ITEM ( )  RATIONAL_B_SPLINE_SURFACE ( (
 ( 1.000000000000000000, 0.7071067811865473507, 1.000000000000000000),
 ( 1.000000000000000000, 0.7270538103684565101, 1.000000000000000000),
 ( 1.000000000000000000, 0.7474775509998854428, 1.000000000000000000),
 ( 1.000000000000000000, 0.7877120837788209595, 1.000000000000000000),
 ( 1.000000000000000000, 0.8076198138825669837, 1.000000000000000000),
 ( 1.000000000000000000, 0.8446812442347624295, 1.000000000000000000),
 ( 1.000000000000000000, 0.8620019270875391992, 1.000000000000000000),
 ( 1.000000000000000000, 0.8939173377915974328, 1.000000000000000000),
 ( 1.000000000000000000, 0.9085622752434662219, 1.000000000000000000),
 ( 1.000000000000000000, 0.9477746975872610724, 1.000000000000000000),
 ( 1.000000000000000000, 0.9672053386934328367, 1.000000000000000000),
 ( 1.000000000000000000, 0.9933317393956891950, 1.000000000000000000),
 ( 1.000000000000000000, 1.000004063029967805, 1.000000000000000000),
 ( 1.000000000000000000, 1.000000000000000000, 1.000000000000000000) ) ) 
 REPRESENTATION_ITEM ( '' )  SURFACE ( )  );
#42007=CARTESIAN_POINT ( 'NONE',  ( 15.44560561439838331, -0.7538990090809657429, 14.98284401175013336 ) ) ;
#42039=CARTESIAN_POINT ( 'NONE',  ( 4.856731536730760190, -63.85066234079124570, 12.98722588752802309 ) ) ;
#42044=VERTEX_POINT ( 'NONE', #16407 ) ;
#42067=CARTESIAN_POINT ( 'NONE',  ( -6.905560911067180285, -0.02023367412855946526, 19.00754324974943188 ) ) ;
#42080=DIRECTION ( 'NONE',  ( 0.000000000000000000, 0.000000000000000000, 1.000000000000000000 ) ) ;
#42083=CARTESIAN_POINT ( 'NONE',  ( -9.389245980427300964, -2.447416405268218131, 14.81682632889905626 ) ) ;
#42090=CARTESIAN_POINT ( 'NONE',  ( 0.000000000000000000, -4.000000000000003553, 27.00000000000000000 ) ) ;
#42096=AXIS2_PLACEMENT_3D ( 'NONE', #18608, #76806, #77887 ) ;
#42118=CARTESIAN_POINT ( 'NONE',  ( -13.38090213880806978, -54.00000000000000711, 31.11721482942554928 ) ) ;
#42124=ORIENTED_EDGE ( 'NONE', *, *, #71955, .T. ) ;
#42136=CARTESIAN_POINT ( 'NONE',  ( 9.423772032809306864, -56.01307627480206008, 23.65101655106710510 ) ) ;
#42138=DIRECTION ( 'NONE',  ( -1.000000000000000000, -0.000000000000000000, -0.000000000000000000 ) ) ;
#42139=FILL_AREA_STYLE_COLOUR ( '', #13339 ) ;
#42144=CARTESIAN_POINT ( 'NONE',  ( 3.808169938200466120, -9.155691705081260068, 13.42225449006559579 ) ) ;
#42151=CARTESIAN_POINT ( 'NONE',  ( -0.9999999999999941158, -50.00000000000000000, 101.0455488498966758 ) ) ;
#42169=CARTESIAN_POINT ( 'NONE',  ( -5.911697307506504906, -50.52686870766020633, 39.69124793001901708 ) ) ;
#42186=FILL_AREA_STYLE ('',( #92326 ) ) ;
#42190=STYLED_ITEM ( 'NONE', ( #70558 ), #86403 ) ;
#42193=CARTESIAN_POINT ( 'NONE',  ( -6.999999999999993783, -50.00000000000000000, 102.2532056551910387 ) ) ;
#42233=ORIENTED_EDGE ( 'NONE', *, *, #16509, .F. ) ;
#42238=SURFACE_STYLE_FILL_AREA ( #76729 ) ;
#42256=CARTESIAN_POINT ( 'NONE',  ( 6.999999999999998224, -12.54465221550629472, 8.223849511755000563 ) ) ;
#42282=DIRECTION ( 'NONE',  ( 0.000000000000000000, 0.000000000000000000, 1.000000000000000000 ) ) ;
#42286=SURFACE_STYLE_FILL_AREA ( #23487 ) ;
#42292=( NAMED_UNIT ( * ) PLANE_ANGLE_UNIT ( ) SI_UNIT ( $, .RADIAN. ) );
#42295=( BOUNDED_SURFACE ( )  B_SPLINE_SURFACE ( 3, 2, ( 
 ( #41098, #42151, #57789 ),
 ( #89652, #99858, #73443 ),
 ( #50755, #24420, #56729 ),
 ( #83662, #50244, #16281 ),
 ( #62, #66426, #48635 ),
 ( #9773, #58338, #99310 ),
 ( #81519, #7644, #40560 ),
 ( #83146, #33033, #65899 ),
 ( #9243, #75034, #90716 ),
 ( #74512, #98782, #24938 ) ),
 .UNSPECIFIED., .F., .F., .F. ) 
 B_SPLINE_SURFACE_WITH_KNOTS ( ( 4, 2, 2, 2, 4 ),
 ( 3, 3 ),
 ( -1.185673698477996893E-05, 0.001057471059733232615, 0.002126798856451245050, 0.003196126653169257485, 0.004265454449887269919 ),
 ( 0.000000000000000000, 1.000000000000000000 ),
 .UNSPECIFIED. ) 
 GEOMETRIC_REPRESENTATION_ITEM ( )  RATIONAL_B_SPLINE_SURFACE ( (
 ( 1.000000000000000000, 1.000000000000000000, 1.000000000000000000),
 ( 1.000000000000000000, 0.9999925199711559021, 1.000000000000000000),
 ( 1.000000000000000000, 0.9961033022470029419, 1.000000000000000000),
 ( 1.000000000000000000, 0.9800616282253082900, 1.000000000000000000),
 ( 1.000000000000000000, 0.9678427155943769566, 1.000000000000000000),
 ( 1.000000000000000000, 0.9345111840696140870, 1.000000000000000000),
 ( 1.000000000000000000, 0.9135791977930803887, 1.000000000000000000),
 ( 1.000000000000000000, 0.8625981283151610279, 1.000000000000000000),
 ( 1.000000000000000000, 0.8325406200924377886, 1.000000000000000000),
 ( 1.000000000000000000, 0.7974033994357117017, 1.000000000000000000) ) ) 
 REPRESENTATION_ITEM ( '' )  SURFACE ( )  );
#42296=CIRCLE ( 'NONE', #87059, 2.000000000000000000 ) ;
#42305=CARTESIAN_POINT ( 'NONE',  ( 0.000000000000000000, -1.200583151104953394, 120.1428571428571388 ) ) ;
#42316=VERTEX_POINT ( 'NONE', #91258 ) ;
#42327=STYLED_ITEM ( 'NONE', ( #72130 ), #11749 ) ;
#42347=CARTESIAN_POINT ( 'NONE',  ( -5.000000000000000000, -15.93202192939577344, -5.930487099830192399 ) ) ;
#42352=CARTESIAN_POINT ( 'NONE',  ( 4.769810751601300858, -47.36241918932975636, 42.84708261346381164 ) ) ;
#42371=CARTESIAN_POINT ( 'NONE',  ( 2.267203695418912091, -69.44328133798735792, 12.91314673039722294 ) ) ;
#42387=CARTESIAN_POINT ( 'NONE',  ( -27.99999999999999645, 0.000000000000000000, 0.000000000000000000 ) ) ;
#42389=STYLED_ITEM ( 'NONE', ( #2684 ), #65440 ) ;
#42397=CARTESIAN_POINT ( 'NONE',  ( 5.000000000000000000, -13.96166769376080374, 11.51022196660214370 ) ) ;
#42419=ORIENTED_EDGE ( 'NONE', *, *, #56454, .T. ) ;
#42536=CARTESIAN_POINT ( 'NONE',  ( 12.38975795024176918, -3.228398025805478078, 20.63738045662677223 ) ) ;
#42538=FILL_AREA_STYLE_COLOUR ( '', #102830 ) ;
#42565=CARTESIAN_POINT ( 'NONE',  ( 27.99999999999999645, 1.102182119232617714E-15, -9.000000000000000000 ) ) ;
#42584=EDGE_CURVE ( 'NONE', #4171, #11109, #105308, .T. ) ;
#42600=CARTESIAN_POINT ( 'NONE',  ( -12.35738183340122553, -3.035458518230857106, 20.66409048039636076 ) ) ;
#42605=AXIS2_PLACEMENT_3D ( 'NONE', #78232, #4347, #62082 ) ;
#42647=CARTESIAN_POINT ( 'NONE',  ( -4.369287899246183215, -1.129960224643866251, 104.3947014718172142 ) ) ;
#42674=CARTESIAN_POINT ( 'NONE',  ( -3.604576940039238675, -1.047841513645850098, 104.3731177596920787 ) ) ;
#42681=( NAMED_UNIT ( * ) SI_UNIT ( $, .STERADIAN. ) SOLID_ANGLE_UNIT ( ) );
#42682=CARTESIAN_POINT ( 'NONE',  ( 5.892857268295339068, -15.73409625558654135, 14.28797240113282818 ) ) ;
#42715=( NAMED_UNIT ( * ) PLANE_ANGLE_UNIT ( ) SI_UNIT ( $, .RADIAN. ) );
#42717=( GEOMETRIC_REPRESENTATION_CONTEXT ( 3 ) GLOBAL_UNCERTAINTY_ASSIGNED_CONTEXT ( ( #102247 ) ) GLOBAL_UNIT_ASSIGNED_CONTEXT ( ( #54432, #31795, #6423 ) ) REPRESENTATION_CONTEXT ( 'NONE', 'WORKASPACE' ) );
#42757=DIRECTION ( 'NONE',  ( -0.000000000000000000, -1.000000000000000000, -0.000000000000000000 ) ) ;
#42772=ADVANCED_FACE ( 'NONE', ( #453 ), #101343, .T. ) ;
#42775=CARTESIAN_POINT ( 'NONE',  ( 3.801077171203083527, -1.110903940591797090, 104.1059035333591112 ) ) ;
#42777=CARTESIAN_POINT ( 'NONE',  ( -3.208180356138712330, -10.20788741807813516, -11.61546768905594185 ) ) ;
#42796=CARTESIAN_POINT ( 'NONE',  ( 12.32179744594563608, -10.26684526391957952, 10.94526264208287181 ) ) ;
#42825=FILL_AREA_STYLE ('',( #91392 ) ) ;
#42853=SURFACE_STYLE_FILL_AREA ( #48799 ) ;
#42860=CARTESIAN_POINT ( 'NONE',  ( 6.999999998637613352, -46.54042759438532784, 39.12435565376871693 ) ) ;
#42887=EDGE_LOOP ( 'NONE', ( #8880, #56253, #73446, #87895, #100511, #104051, #56096, #68860, #14149 ) ) ;
#42892=ORIENTED_EDGE ( 'NONE', *, *, #71019, .F. ) ;
#42893=EDGE_CURVE ( 'NONE', #95128, #53428, #54813, .T. ) ;
#42912=CARTESIAN_POINT ( 'NONE',  ( 4.551278563468414085, -67.07315913433207299, 13.74478386570468658 ) ) ;
#42928=FILL_AREA_STYLE ('',( #1373 ) ) ;
#42936=ORIENTED_EDGE ( 'NONE', *, *, #74493, .T. ) ;
#42948=( GEOMETRIC_REPRESENTATION_CONTEXT ( 3 ) GLOBAL_UNCERTAINTY_ASSIGNED_CONTEXT ( ( #14010 ) ) GLOBAL_UNIT_ASSIGNED_CONTEXT ( ( #80653, #31614, #38640 ) ) REPRESENTATION_CONTEXT ( 'NONE', 'WORKASPACE' ) );
#42951=EDGE_CURVE ( 'NONE', #12254, #88009, #56371, .T. ) ;
#42968=UNCERTAINTY_MEASURE_WITH_UNIT (LENGTH_MEASURE( 1.000000000000000082E-05 ), #6246, 'distance_accuracy_value', 'NONE');
#42985=ORIENTED_EDGE ( 'NONE', *, *, #510, .F. ) ;
#42987=ORIENTED_EDGE ( 'NONE', *, *, #106389, .T. ) ;
#43027=CARTESIAN_POINT ( 'NONE',  ( 3.644838609763359827, -53.10562036962778620, 40.51873384035687309 ) ) ;
#43040=EDGE_CURVE ( 'NONE', #38295, #170, #63552, .T. ) ;
#43084=CARTESIAN_POINT ( 'NONE',  ( 9.693539536716441418, -2.245191209186759185, 15.45402435566443700 ) ) ;
#43110=CARTESIAN_POINT ( 'NONE',  ( 1.688865360071264643, -5.975540627543329819, -13.79722992720151709 ) ) ;
#43115=ORIENTED_EDGE ( 'NONE', *, *, #49507, .T. ) ;
#43141=( NAMED_UNIT ( * ) SI_UNIT ( $, .STERADIAN. ) SOLID_ANGLE_UNIT ( ) );
#43157=CARTESIAN_POINT ( 'NONE',  ( 4.370066673350165409, -1.130272197109061239, 104.3945758574409695 ) ) ;
#43160=FACE_BOUND ( 'NONE', #86788, .T. ) ;
#43201=ORIENTED_EDGE ( 'NONE', *, *, #40651, .F. ) ;
#43217=FILL_AREA_STYLE ('',( #42139 ) ) ;
#43221=CARTESIAN_POINT ( 'NONE',  ( 6.598176363461978333, -7.008098997476053249, 13.88231573857982326 ) ) ;
#43226=CIRCLE ( 'NONE', #82793, 9.000000000000000000 ) ;
#43263=CARTESIAN_POINT ( 'NONE',  ( -3.801077171203083971, -1.110903940591794203, 104.1059035333591254 ) ) ;
#43270=( NAMED_UNIT ( * ) SI_UNIT ( $, .STERADIAN. ) SOLID_ANGLE_UNIT ( ) );
#43276=CARTESIAN_POINT ( 'NONE',  ( -1.000000000000000000, -63.35894816181920675, 9.450637109072113518 ) ) ;
#43313=CARTESIAN_POINT ( 'NONE',  ( 3.460324465711511088, -1.165480915309818011, 104.5902739981127212 ) ) ;
#43316=SURFACE_STYLE_USAGE ( .BOTH. , #35794 ) ;
#43332=ORIENTED_EDGE ( 'NONE', *, *, #59334, .F. ) ;
#43338=VERTEX_POINT ( 'NONE', #96755 ) ;
#43352=SURFACE_STYLE_FILL_AREA ( #12034 ) ;
#43353=CARTESIAN_POINT ( 'NONE',  ( -4.245164436743399605, -48.92819220080404108, 104.4592797835132245 ) ) ;
#43380=DIRECTION ( 'NONE',  ( 0.000000000000000000, 0.000000000000000000, -1.000000000000000000 ) ) ;
#43400=CARTESIAN_POINT ( 'NONE',  ( 4.881492806919405680, -52.01899411372407656, 40.12243117532113956 ) ) ;
#43423=B_SPLINE_CURVE_WITH_KNOTS ( 'NONE', 3,
 ( #40053, #98798, #72927, #75053, #106359, #97737, #26049, #49188, #42169, #40581, #23905, #73999, #89673, #24955, #41647, #73461, #74531, #58359, #24442, #57274, #91278, #82089, #57810, #8208 ),
 .UNSPECIFIED., .F., .F.,
 ( 4, 2, 2, 2, 2, 2, 2, 2, 2, 2, 2, 4 ),
 ( 0.000000000000000000, 0.001423843649067600388, 0.002847687298135200776, 0.004271530947202801382, 0.004983452771736591493, 0.005695374596270383338, 0.007119218245337962693, 0.008543061894405543782, 0.009254983718939334761, 0.009966905543473125739, 0.01067882736800691672, 0.01139074919254070770 ),
 .UNSPECIFIED. ) ;
#43440=COLOUR_RGB ( '', 0.31764706, 0.68627451, 0.89019608) ;
#43445=COLOUR_RGB ( '', 0.72549020, 0.75294118, 0.79215686) ;
#43446=CARTESIAN_POINT ( 'NONE',  ( -2.714482629291888660, -49.62047324315857821, 102.8323262222670280 ) ) ;
#43476=CARTESIAN_POINT ( 'NONE',  ( 5.000000000000079048, -15.32190040641887130, 13.82401333428050627 ) ) ;
#43495=CARTESIAN_POINT ( 'NONE',  ( 8.380151598009016212, -0.1935070982757394475, 19.49075913394571558 ) ) ;
#43497=( NAMED_UNIT ( * ) PLANE_ANGLE_UNIT ( ) SI_UNIT ( $, .RADIAN. ) );
#43553=DIRECTION ( 'NONE',  ( 1.000000000000000000, 0.000000000000000000, 0.000000000000000000 ) ) ;
#43556=CARTESIAN_POINT ( 'NONE',  ( 3.252284881921470916, -53.34547930654326819, 40.61850418307594879 ) ) ;
#43561=ORIENTED_EDGE ( 'NONE', *, *, #97217, .T. ) ;
#43590=VERTEX_POINT ( 'NONE', #51897 ) ;
#43611=CARTESIAN_POINT ( 'NONE',  ( 3.396360046676563993, -49.15315706213417002, 103.9790200242190821 ) ) ;
#43628=EDGE_CURVE ( 'NONE', #96331, #17391, #100455, .T. ) ;
#43656=DIRECTION ( 'NONE',  ( 1.000000000000000000, 0.000000000000000000, 0.000000000000000000 ) ) ;
#43721=CARTESIAN_POINT ( 'NONE',  ( -5.000000000000000000, -13.86898977591626192, 11.25489781251236820 ) ) ;
#43733=ORIENTED_EDGE ( 'NONE', *, *, #48632, .T. ) ;
#43738=CARTESIAN_POINT ( 'NONE',  ( -2.514200967265426634, -0.2912192546974278762, 102.6057089534373574 ) ) ;
#43771=CARTESIAN_POINT ( 'NONE',  ( 2.068673967786704981, -49.86383299198053720, 102.1191603898000011 ) ) ;
#43815=EDGE_CURVE ( 'NONE', #10104, #2153, #58205, .T. ) ;
#43827=( NAMED_UNIT ( * ) SI_UNIT ( $, .STERADIAN. ) SOLID_ANGLE_UNIT ( ) );
#43836=CARTESIAN_POINT ( 'NONE',  ( 3.841398122528158598, -1.072224703192209416, 104.5835869663332005 ) ) ;
#43840=CARTESIAN_POINT ( 'NONE',  ( -5.136066607407661522, -12.96798121126441039, -7.569033233150490148 ) ) ;
#43842=CARTESIAN_POINT ( 'NONE',  ( -15.46327711221947609, -5.286601841950839820, 14.04103132160307688 ) ) ;
#43860=( LENGTH_UNIT ( ) NAMED_UNIT ( * ) SI_UNIT ( .MILLI., .METRE. ) );
#43874=CARTESIAN_POINT ( 'NONE',  ( 4.999999999999993783, -4.000000000000003553, 103.2791840072761858 ) ) ;
#43889=( NAMED_UNIT ( * ) PLANE_ANGLE_UNIT ( ) SI_UNIT ( $, .RADIAN. ) );
#43904=DIRECTION ( 'NONE',  ( -1.000000000000000000, -0.000000000000000000, -0.000000000000000000 ) ) ;
#43922=ORIENTED_EDGE ( 'NONE', *, *, #27844, .F. ) ;
#43923=CARTESIAN_POINT ( 'NONE',  ( 1.601898381236912305, -53.94709533814469182, 40.91400580830796230 ) ) ;
#43926=CIRCLE ( 'NONE', #104185, 14.00000000000000178 ) ;
#43928=EDGE_CURVE ( 'NONE', #40703, #77091, #32367, .T. ) ;
#44000=ORIENTED_EDGE ( 'NONE', *, *, #74454, .T. ) ;
#44015=UNCERTAINTY_MEASURE_WITH_UNIT (LENGTH_MEASURE( 1.000000000000000082E-05 ), #104759, 'distance_accuracy_value', 'NONE');
#44019=CARTESIAN_POINT ( 'NONE',  ( -13.90371668366488400, -57.59451832461709841, 25.34313603510888413 ) ) ;
#44022=CARTESIAN_POINT ( 'NONE',  ( 12.37144696128342147, -4.000000000000003553, 20.44658103856077602 ) ) ;
#44023=VERTEX_POINT ( 'NONE', #80409 ) ;
#44037=EDGE_LOOP ( 'NONE', ( #79241, #78522, #97662, #13434 ) ) ;
#44062=CARTESIAN_POINT ( 'NONE',  ( 0.000000000000000000, -46.00000000000000000, 123.0000000000000142 ) ) ;
#44064=ORIENTED_EDGE ( 'NONE', *, *, #63460, .F. ) ;
#44084=CARTESIAN_POINT ( 'NONE',  ( 5.000000000000000000, -13.99270448171187375, 11.59586337663402489 ) ) ;
#44092=CARTESIAN_POINT ( 'NONE',  ( 1.723082057455612048, -53.92950373265724551, 40.90106102219755257 ) ) ;
#44098=( GEOMETRIC_REPRESENTATION_CONTEXT ( 3 ) GLOBAL_UNCERTAINTY_ASSIGNED_CONTEXT ( ( #56966 ) ) GLOBAL_UNIT_ASSIGNED_CONTEXT ( ( #69042, #87747, #2141 ) ) REPRESENTATION_CONTEXT ( 'NONE', 'WORKASPACE' ) );
#44129=ORIENTED_EDGE ( 'NONE', *, *, #64251, .T. ) ;
#44154=CARTESIAN_POINT ( 'NONE',  ( 3.460324465709686326, -48.83451908470932779, 104.5902739980971461 ) ) ;
#44155=CARTESIAN_POINT ( 'NONE',  ( -1.000000000000000222, -5.000000000000000000, -14.14213562373095101 ) ) ;
#44178=CARTESIAN_POINT ( 'NONE',  ( 3.964214964212477099, -12.08915882607781001, -10.21564873357027281 ) ) ;
#44186=ADVANCED_FACE ( 'NONE', ( #91715 ), #50178, .F. ) ;
#44200=EDGE_LOOP ( 'NONE', ( #98757, #58971, #75188, #58165, #80006, #3166 ) ) ;
#44226=ORIENTED_EDGE ( 'NONE', *, *, #82861, .T. ) ;
#44227=SURFACE_STYLE_FILL_AREA ( #84681 ) ;
#44229=AXIS2_PLACEMENT_3D ( 'NONE', #68306, #34375, #101200 ) ;
#44238=ADVANCED_FACE ( 'NONE', ( #98597 ), #71994, .T. ) ;
#44266=CARTESIAN_POINT ( 'NONE',  ( -5.000000000000000000, -15.62228920881133298, 12.61250543006184088 ) ) ;
#44280=CARTESIAN_POINT ( 'NONE',  ( -3.459690225508090577, -1.108983740916333893, 104.5059395991341660 ) ) ;
#44303=CARTESIAN_POINT ( 'NONE',  ( 5.000000000000000000, -60.71953810597794643, 12.61250543007074931 ) ) ;
#44305=TOROIDAL_SURFACE ( 'NONE', #2938, 8.499999999999992895, 0.5000000000000000000 ) ;
#44309=EDGE_CURVE ( 'NONE', #44023, #57615, #75926, .T. ) ;
#44311=( LENGTH_UNIT ( ) NAMED_UNIT ( * ) SI_UNIT ( .MILLI., .METRE. ) );
#44338=SURFACE_SIDE_STYLE ('',( #76690 ) ) ;
#44347=AXIS2_PLACEMENT_3D ( 'NONE', #62631, #12458, #85859 ) ;
#44371=SURFACE_STYLE_USAGE ( .BOTH. , #19073 ) ;
#44381=CARTESIAN_POINT ( 'NONE',  ( 3.355892750373846933, -0.9951980364987254024, 104.3125661743353447 ) ) ;
#44383=CARTESIAN_POINT ( 'NONE',  ( -1.000000000000000000, -5.000000000000016875, -14.14213562373094746 ) ) ;
#44386=CARTESIAN_POINT ( 'NONE',  ( -6.840078058529586613, -12.20617675668041890, 8.820020145246234122 ) ) ;
#44398=CARTESIAN_POINT ( 'NONE',  ( 13.76576316043658643, -57.17837160915925665, 29.55959131405483475 ) ) ;
#44433=FACE_OUTER_BOUND ( 'NONE', #69237, .T. ) ;
#44446=CARTESIAN_POINT ( 'NONE',  ( -9.215420734788352775, -54.26735268782334742, 23.11721482942554928 ) ) ;
#44464=CARTESIAN_POINT ( 'NONE',  ( 3.010879515032809817, -49.46749084728875090, 44.29121189687241156 ) ) ;
#44479=DIRECTION ( 'NONE',  ( 0.000000000000000000, 0.000000000000000000, 1.000000000000000000 ) ) ;
#44491=CARTESIAN_POINT ( 'NONE',  ( -2.426529107808244490, -49.73926502898306268, 44.58451710260244738 ) ) ;
#44505=AXIS2_PLACEMENT_3D ( 'NONE', #42193, #67019, #33076 ) ;
#44528=STYLED_ITEM ( 'NONE', ( #66838 ), #42772 ) ;
#44564=CARTESIAN_POINT ( 'NONE',  ( -4.744389013293885071, -48.62707453416837211, 104.3204960233004357 ) ) ;
#44565=CARTESIAN_POINT ( 'NONE',  ( -13.87389654945780215, -57.47116530957473657, 25.11216171227248850 ) ) ;
#44605=ADVANCED_FACE ( 'NONE', ( #55088 ), #32525, .F. ) ;
#44607=MECHANICAL_DESIGN_GEOMETRIC_PRESENTATION_REPRESENTATION('',(#80673),#85883);
#44609=CARTESIAN_POINT ( 'NONE',  ( -4.382959417677089853, -1.862050784382271784, 102.7400018439556817 ) ) ;
#44638=PRESENTATION_STYLE_ASSIGNMENT (( #52700 ) ) ;
#44655=COLOUR_RGB ( '', 0.72549020, 0.75294118, 0.79215686) ;
#44698=CARTESIAN_POINT ( 'NONE',  ( -4.401186155046908688, -13.27308926788038690, -9.172652456351809036 ) ) ;
#44717=CARTESIAN_POINT ( 'NONE',  ( 6.547363650394499857, -12.76646305665543224, -7.895817423510056443 ) ) ;
#44768=CARTESIAN_POINT ( 'NONE',  ( -9.674956971852997967, -2.241286958287645348, 15.44908467815371722 ) ) ;
#44780=ADVANCED_FACE ( 'NONE', ( #19478 ), #54882, .T. ) ;
#44788=CARTESIAN_POINT ( 'NONE',  ( -3.454253436624930451, -0.8414180287960395521, 103.7259032015043232 ) ) ;
#44796=EDGE_LOOP ( 'NONE', ( #71728, #36603 ) ) ;
#44806=CARTESIAN_POINT ( 'NONE',  ( -13.66213079746738934, -51.55693619836885233, 23.93919572553859609 ) ) ;
#44807=CARTESIAN_POINT ( 'NONE',  ( -27.99999999999999645, 1.347111479062088405E-15, 11.00000000000000000 ) ) ;
#44826=SURFACE_STYLE_FILL_AREA ( #29208 ) ;
#44829=( NAMED_UNIT ( * ) PLANE_ANGLE_UNIT ( ) SI_UNIT ( $, .RADIAN. ) );
#44893=B_SPLINE_CURVE_WITH_KNOTS ( 'NONE', 3,
 ( #97628, #58242, #89030, #23793, #24842, #106248, #8629, #65280, #81974, #8095 ),
 .UNSPECIFIED., .F., .F.,
 ( 4, 2, 2, 2, 4 ),
 ( 8.182674270850422113E-18, 0.0008022363492415295842, 0.001604472698483051145, 0.002406709047724572489, 0.003208945396966094050 ),
 .UNSPECIFIED. ) ;
#44949=FACE_OUTER_BOUND ( 'NONE', #19243, .T. ) ;
#44961=STYLED_ITEM ( 'NONE', ( #30322 ), #105147 ) ;
#44970=( LENGTH_UNIT ( ) NAMED_UNIT ( * ) SI_UNIT ( .MILLI., .METRE. ) );
#44972=DIRECTION ( 'NONE',  ( 0.000000000000000000, 0.000000000000000000, -1.000000000000000000 ) ) ;
#44989=CARTESIAN_POINT ( 'NONE',  ( -9.574562898131892652, -56.64787618657226176, 24.10796671758935261 ) ) ;
#44997=ORIENTED_EDGE ( 'NONE', *, *, #49160, .F. ) ;
#45005=VERTEX_POINT ( 'NONE', #46362 ) ;
#45007=CARTESIAN_POINT ( 'NONE',  ( 4.788374038886465733, -47.31025204562959630, 42.82694009917617706 ) ) ;
#45029=CARTESIAN_POINT ( 'NONE',  ( -1.269730911708409238, -50.00000000000000000, 44.94218429609317411 ) ) ;
#45047=DIRECTION ( 'NONE',  ( -1.000000000000000000, 0.000000000000000000, 0.000000000000000000 ) ) ;
#45059=PRESENTATION_STYLE_ASSIGNMENT (( #63365 ) ) ;
#45087=CARTESIAN_POINT ( 'NONE',  ( 5.911949307999758041, -11.74847537023907584, -9.342369578515908657 ) ) ;
#45097=UNCERTAINTY_MEASURE_WITH_UNIT (LENGTH_MEASURE( 1.000000000000000082E-05 ), #23073, 'distance_accuracy_value', 'NONE');
#45100=CARTESIAN_POINT ( 'NONE',  ( -5.232798140227928663, -48.02337292624943643, 104.1190344879414056 ) ) ;
#45123=CARTESIAN_POINT ( 'NONE',  ( -1.116724534379475386, -70.61792054436683941, 13.04250788268058692 ) ) ;
#45157=CARTESIAN_POINT ( 'NONE',  ( 5.000000000000000000, -14.21727251090713828, 9.320362779989000757 ) ) ;
#45217=ADVANCED_FACE ( 'NONE', ( #19361 ), #75404, .T. ) ;
#45225=CARTESIAN_POINT ( 'NONE',  ( -3.808203125592111604, -9.155674645823081548, 13.42226102569178892 ) ) ;
#45228=CARTESIAN_POINT ( 'NONE',  ( 3.352941176470588758, -48.79941684889504927, 104.5794940929807524 ) ) ;
#45252=SURFACE_STYLE_FILL_AREA ( #103991 ) ;
#45265=CIRCLE ( 'NONE', #93538, 8.000000000000000000 ) ;
#45275=FILL_AREA_STYLE ('',( #53872 ) ) ;
#45295=CARTESIAN_POINT ( 'NONE',  ( -15.75694905239713783, -1.457936233759121514, 14.93097729572344790 ) ) ;
#45329=( NAMED_UNIT ( * ) PLANE_ANGLE_UNIT ( ) SI_UNIT ( $, .RADIAN. ) );
#45354=SURFACE_STYLE_USAGE ( .BOTH. , #94973 ) ;
#45374=CARTESIAN_POINT ( 'NONE',  ( 5.000000000000000000, -15.93202192939576634, -5.930487099830193287 ) ) ;
#45382=CARTESIAN_POINT ( 'NONE',  ( 3.871024465589345542, -48.78517836376548189, 104.2728733527511906 ) ) ;
#45394=EDGE_CURVE ( 'NONE', #22140, #57238, #41321, .T. ) ;
#45427=CARTESIAN_POINT ( 'NONE',  ( 1.000000000000002887, -70.58759490697437400, 11.03128057732868150 ) ) ;
#45439=DIRECTION ( 'NONE',  ( 0.000000000000000000, 1.000000000000000000, 0.000000000000000000 ) ) ;
#45451=CARTESIAN_POINT ( 'NONE',  ( -13.45079846400083312, -54.00000000000000711, 23.11721482942554928 ) ) ;
#45487=CARTESIAN_POINT ( 'NONE',  ( 1.000000000000000000, -68.69132998577646276, 12.24443901500763765 ) ) ;
#45493=AXIS2_PLACEMENT_3D ( 'NONE', #49069, #7026, #16721 ) ;
#45496=CARTESIAN_POINT ( 'NONE',  ( 4.869065774733602581, -2.951204850257813206, 102.3543991519893979 ) ) ;
#45506=DIRECTION ( 'NONE',  ( 0.000000000000000000, 0.000000000000000000, -1.000000000000000000 ) ) ;
#45509=SURFACE_STYLE_FILL_AREA ( #62236 ) ;
#45557=CARTESIAN_POINT ( 'NONE',  ( -1.626968941750977393, -50.01525831937068034, 40.95668304117249647 ) ) ;
#45585=FACE_OUTER_BOUND ( 'NONE', #26302, .T. ) ;
#45628=FILL_AREA_STYLE_COLOUR ( '', #79238 ) ;
#45643=CARTESIAN_POINT ( 'NONE',  ( -1.832167802012315994, -70.57974515660504267, 13.11834054208777189 ) ) ;
#45662=ORIENTED_EDGE ( 'NONE', *, *, #105830, .T. ) ;
#45682=CARTESIAN_POINT ( 'NONE',  ( 7.000000000000000000, -60.71953810598073886, 12.61250543006184088 ) ) ;
#45689=( NAMED_UNIT ( * ) SI_UNIT ( $, .STERADIAN. ) SOLID_ANGLE_UNIT ( ) );
#45705=DIRECTION ( 'NONE',  ( 0.000000000000000000, 0.000000000000000000, 1.000000000000000000 ) ) ;
#45713=EDGE_LOOP ( 'NONE', ( #69287, #97415 ) ) ;
#45740=CARTESIAN_POINT ( 'NONE',  ( -7.577538872965776662, -12.42143731976112875, 8.412936539037117356 ) ) ;
#45744=CARTESIAN_POINT ( 'NONE',  ( 4.195612334303191915, -48.94124001270402857, 104.4881327927250112 ) ) ;
#45769=VECTOR ( 'NONE', #64139, 1000.000000000000000 ) ;
#45770=( NAMED_UNIT ( * ) PLANE_ANGLE_UNIT ( ) SI_UNIT ( $, .RADIAN. ) );
#45802=LINE ( 'NONE', #78679, #5493 ) ;
#45803=CARTESIAN_POINT ( 'NONE',  ( 1.238781280732904611, -2.150544339304492541E-15, 101.3451024322571641 ) ) ;
#45821=CARTESIAN_POINT ( 'NONE',  ( -9.918585201507950089, -2.743081709124135070, 15.35584857294453442 ) ) ;
#45823=CIRCLE ( 'NONE', #73358, 11.00000000000000000 ) ;
#45826=ORIENTED_EDGE ( 'NONE', *, *, #106145, .F. ) ;
#45854=CARTESIAN_POINT ( 'NONE',  ( -13.90377727273328645, -50.40522912573743497, 25.34355585267129740 ) ) ;
#45893=CIRCLE ( 'NONE', #90691, 4.000000000000003553 ) ;
#45935=CARTESIAN_POINT ( 'NONE',  ( -5.000000000000000888, -43.09265016210607513, 0.3552338647229656421 ) ) ;
#45954=AXIS2_PLACEMENT_3D ( 'NONE', #82011, #24878, #16764 ) ;
#45955=COLOUR_RGB ( '', 0.66274510, 0.83137255, 0.94901961) ;
#46007=CARTESIAN_POINT ( 'NONE',  ( 1.000000000000000000, -43.08885284239458713, 0.3536648519171542993 ) ) ;
#46028=CARTESIAN_POINT ( 'NONE',  ( -1.284384921555213888, -49.99999999999999289, 44.94055355497947346 ) ) ;
#46042=STYLED_ITEM ( 'NONE', ( #76198 ), #59831 ) ;
#46112=CARTESIAN_POINT ( 'NONE',  ( 0.000000000000000000, -1.200583151104953394, 112.0000000000000000 ) ) ;
#46115=STYLED_ITEM ( 'NONE', ( #94414 ), #60434 ) ;
#46158=( NAMED_UNIT ( * ) PLANE_ANGLE_UNIT ( ) SI_UNIT ( $, .RADIAN. ) );
#46170=LINE ( 'NONE', #20356, #19256 ) ;
#46207=CARTESIAN_POINT ( 'NONE',  ( 13.83891950279925354, -50.53292902901529970, 29.12888379965242081 ) ) ;
#46226=CARTESIAN_POINT ( 'NONE',  ( -3.202918473694307266, -48.99785005461730947, 104.2983563224298109 ) ) ;
#46232=COLOUR_RGB ( '', 0.08235294, 0.09019608, 0.10196078) ;
#46235=AXIS2_PLACEMENT_3D ( 'NONE', #32103, #75728, #15899 ) ;
#46276=CARTESIAN_POINT ( 'NONE',  ( -15.82282301484858067, -3.734535164757628589, 14.53964175053558883 ) ) ;
#46324=CARTESIAN_POINT ( 'NONE',  ( 4.284822031654965890, -1.092833614412281662, 104.4267991316945086 ) ) ;
#46346=CARTESIAN_POINT ( 'NONE',  ( -9.354938227918532689, -1.847069743908760664, 15.48488176184545040 ) ) ;
#46362=CARTESIAN_POINT ( 'NONE',  ( -27.99999999999999645, 0.000000000000000000, 15.00000000000000000 ) ) ;
#46375=CARTESIAN_POINT ( 'NONE',  ( -4.420167282472111658, -68.81245422675547729, 13.71330708048197700 ) ) ;
#46384=CARTESIAN_POINT ( 'NONE',  ( -13.56235479181388115, -52.22051512849589017, 23.52533112101723844 ) ) ;
#46390=ORIENTED_EDGE ( 'NONE', *, *, #51954, .T. ) ;
#46434=FILL_AREA_STYLE ('',( #4917 ) ) ;
#46454=CARTESIAN_POINT ( 'NONE',  ( 1.347111479062088996E-15, -46.00000000000000000, 100.9999999999999858 ) ) ;
#46463=CARTESIAN_POINT ( 'NONE',  ( -1.000000000000000000, -48.53184174326406009, 2.645245988156326611 ) ) ;
#46499=CARTESIAN_POINT ( 'NONE',  ( 0.000000000000000000, -4.000000000000003553, 112.0000000000000000 ) ) ;
#46524=CARTESIAN_POINT ( 'NONE',  ( 5.000000000000000000, -49.63763114970241475, 7.479721976420974805 ) ) ;
#46525=AXIS2_PLACEMENT_3D ( 'NONE', #13231, #97334, #6195 ) ;
#46548=CARTESIAN_POINT ( 'NONE',  ( -4.764086639414292002, -47.35998716217660132, 42.85178489487338283 ) ) ;
#46556=ORIENTED_EDGE ( 'NONE', *, *, #69560, .F. ) ;
#46594=CARTESIAN_POINT ( 'NONE',  ( -9.089383533625918332, -13.56607094171270056, 16.34888743995582061 ) ) ;
#46596=CARTESIAN_POINT ( 'NONE',  ( -2.273600070709648424, -49.89527936504848782, 40.92025501607385252 ) ) ;
#46615=SURFACE_STYLE_USAGE ( .BOTH. , #13704 ) ;
#46698=FACE_OUTER_BOUND ( 'NONE', #79282, .T. ) ;
#46725=CARTESIAN_POINT ( 'NONE',  ( 13.60715398569422874, -51.55888882488000036, 30.29660545413128503 ) ) ;
#46741=CARTESIAN_POINT ( 'NONE',  ( 30.00000000000000000, 0.000000000000000000, 0.000000000000000000 ) ) ;
#46747=CARTESIAN_POINT ( 'NONE',  ( -1.115477787493043715, -50.00000000000001421, 101.1904243682835585 ) ) ;
#46766=CARTESIAN_POINT ( 'NONE',  ( -4.999999999999993783, -4.000000000000003553, 103.2791840072761858 ) ) ;
#46770=VERTEX_POINT ( 'NONE', #92825 ) ;
#46775=EDGE_CURVE ( 'NONE', #17391, #94943, #70688, .T. ) ;
#46777=CARTESIAN_POINT ( 'NONE',  ( 5.000000000000000000, -14.21727251090713473, 9.320362779988997204 ) ) ;
#46792=ORIENTED_EDGE ( 'NONE', *, *, #37988, .T. ) ;
#46798=CARTESIAN_POINT ( 'NONE',  ( -9.045860540270149741, -13.61258301273266191, 16.31186313544194277 ) ) ;
#46806=DIRECTION ( 'NONE',  ( -1.000000000000000000, -0.000000000000000000, -0.000000000000000000 ) ) ;
#46816=LINE ( 'NONE', #38741, #31125 ) ;
#46825=CARTESIAN_POINT ( 'NONE',  ( 2.103760375497109703, -0.1490785164325224010, 102.1576431125493940 ) ) ;
#46866=CARTESIAN_POINT ( 'NONE',  ( -7.819539746246620737, -0.1116068871675765933, 19.30361860283825948 ) ) ;
#46876=ORIENTED_EDGE ( 'NONE', *, *, #18511, .T. ) ;
#46880=DIRECTION ( 'NONE',  ( -0.000000000000000000, -1.000000000000000000, -0.000000000000000000 ) ) ;
#46889=CARTESIAN_POINT ( 'NONE',  ( -5.477443569834177239, -66.44117541007194916, 14.11469643991719813 ) ) ;
#46910=ORIENTED_EDGE ( 'NONE', *, *, #47748, .T. ) ;
#46923=UNCERTAINTY_MEASURE_WITH_UNIT (LENGTH_MEASURE( 1.000000000000000082E-05 ), #70827, 'distance_accuracy_value', 'NONE');
#46948=( LENGTH_UNIT ( ) NAMED_UNIT ( * ) SI_UNIT ( .MILLI., .METRE. ) );
#46951=CARTESIAN_POINT ( 'NONE',  ( -9.300615953693611715, -52.70239146822830634, 23.32435243128603730 ) ) ;
#46978=CARTESIAN_POINT ( 'NONE',  ( -5.000000000000000888, -15.67301612170649072, -10.31008658364125985 ) ) ;
#46998=CARTESIAN_POINT ( 'NONE',  ( -1.909182100399626325, -0.1358350450587593183, 102.2488568920600045 ) ) ;
#47003=FILL_AREA_STYLE_COLOUR ( '', #103108 ) ;
#47012=SURFACE_STYLE_FILL_AREA ( #29294 ) ;
#47025=VERTEX_POINT ( 'NONE', #83018 ) ;
#47087=CARTESIAN_POINT ( 'NONE',  ( 4.571008445750555538, -2.193282516568173968, 102.5889671997070849 ) ) ;
#47100=( NAMED_UNIT ( * ) SI_UNIT ( $, .STERADIAN. ) SOLID_ANGLE_UNIT ( ) );
#47109=CARTESIAN_POINT ( 'NONE',  ( -1.000000000000000222, -43.18879712711532193, 0.3952393630180867090 ) ) ;
#47147=CIRCLE ( 'NONE', #612, 2.000000000000000000 ) ;
#47208=( NAMED_UNIT ( * ) SI_UNIT ( $, .STERADIAN. ) SOLID_ANGLE_UNIT ( ) );
#47211=ORIENTED_EDGE ( 'NONE', *, *, #98698, .T. ) ;
#47262=FILL_AREA_STYLE_COLOUR ( '', #7203 ) ;
#47270=SURFACE_STYLE_FILL_AREA ( #87757 ) ;
#47285=CARTESIAN_POINT ( 'NONE',  ( -4.869065774733593699, -2.951204850257779011, 102.3543991519893979 ) ) ;
#47297=CARTESIAN_POINT ( 'NONE',  ( 6.999999999999998224, -12.54465221550629472, 8.223849511754997010 ) ) ;
#47318=CARTESIAN_POINT ( 'NONE',  ( -7.314871723833043404, -6.279301537700069602, 13.99616156953552704 ) ) ;
#47321=DIRECTION ( 'NONE',  ( 0.000000000000000000, 1.000000000000000000, 0.000000000000000000 ) ) ;
#47369=CARTESIAN_POINT ( 'NONE',  ( 3.568931636294630394, -0.9305242695747285575, 103.4741166605239471 ) ) ;
#47375=EDGE_CURVE ( 'NONE', #85296, #76782, #58756, .T. ) ;
#47381=DIRECTION ( 'NONE',  ( -1.000000000000000000, -0.000000000000000000, -0.000000000000000000 ) ) ;
#47396=B_SPLINE_CURVE_WITH_KNOTS ( 'NONE', 3,
 ( #541, #32453, #80960, #57210, #56684, #72865, #40513, #23295, #72352, #48589, #106291, #14624, #24366, #16231, #31913, #89606 ),
 .UNSPECIFIED., .F., .F.,
 ( 4, 2, 2, 2, 2, 2, 2, 4 ),
 ( 0.000000000000000000, 0.002593706636443856260, 0.005187413272887715122, 0.006484266591109646288, 0.007781119909331575719, 0.008429546568442540869, 0.009077973227553506885, 0.01037482654577543718 ),
 .UNSPECIFIED. ) ;
#47414=AXIS2_PLACEMENT_3D ( 'NONE', #84259, #59470, #67022 ) ;
#47417=CARTESIAN_POINT ( 'NONE',  ( -5.978750298146849218, -13.03636037196927511, 13.21647969580618742 ) ) ;
#47420=SURFACE_STYLE_FILL_AREA ( #15053 ) ;
#47447=CARTESIAN_POINT ( 'NONE',  ( -3.352941176470583873, -48.79941684889506348, 104.5794940929807524 ) ) ;
#47479=CARTESIAN_POINT ( 'NONE',  ( -9.337186727013605747, -51.98687375574689895, 30.58335800272115534 ) ) ;
#47496=CIRCLE ( 'NONE', #13072, 8.857142857142855874 ) ;
#47529=CARTESIAN_POINT ( 'NONE',  ( -2.679344702995778427, -0.3583992640727010626, 103.0669469696961897 ) ) ;
#47532=( NAMED_UNIT ( * ) PLANE_ANGLE_UNIT ( ) SI_UNIT ( $, .RADIAN. ) );
#47559=CARTESIAN_POINT ( 'NONE',  ( 13.50929957260945535, -55.29737542706585884, 23.32445699588452470 ) ) ;
#47573=PRESENTATION_STYLE_ASSIGNMENT (( #71326 ) ) ;
#47575=CARTESIAN_POINT ( 'NONE',  ( 10.92050665241513840, -10.68475269600504696, 18.23204539070182051 ) ) ;
#47593=CARTESIAN_POINT ( 'NONE',  ( -2.820573970604164593, -49.57105631822983582, 44.39822767282944227 ) ) ;
#47642=CARTESIAN_POINT ( 'NONE',  ( -9.275399896789910059, -13.35898335746451160, 16.51081693063991906 ) ) ;
#47644=CARTESIAN_POINT ( 'NONE',  ( -5.000000000000000888, -46.26658367591656429, 42.58845726862488590 ) ) ;
#47663=( NAMED_UNIT ( * ) PLANE_ANGLE_UNIT ( ) SI_UNIT ( $, .RADIAN. ) );
#47675=ORIENTED_EDGE ( 'NONE', *, *, #81987, .T. ) ;
#47692=COLOUR_RGB ( '', 0.09019608, 0.27058824, 0.51372549) ;
#47735=CARTESIAN_POINT ( 'NONE',  ( -4.296575424418834999, -67.78488758413351434, 13.66189604103251476 ) ) ;
#47736=DIRECTION ( 'NONE',  ( 1.000000000000000000, -0.000000000000000000, -0.000000000000000000 ) ) ;
#47744=FILL_AREA_STYLE_COLOUR ( '', #64524 ) ;
#47748=EDGE_CURVE ( 'NONE', #15547, #81100, #24354, .T. ) ;
#47818=SURFACE_SIDE_STYLE ('',( #6298 ) ) ;
#47839=CARTESIAN_POINT ( 'NONE',  ( 4.551587301587291634, -48.79941684889506348, 104.4018401814738013 ) ) ;
#47855=TOROIDAL_SURFACE ( 'NONE', #34133, 8.000000000000000000, 4.000000000000000000 ) ;
#47860=ORIENTED_EDGE ( 'NONE', *, *, #5219, .F. ) ;
#47872=CARTESIAN_POINT ( 'NONE',  ( -4.526657684027646233, -47.90665221903876869, 103.5746540667394697 ) ) ;
#47878=DIRECTION ( 'NONE',  ( 1.000000000000000000, 0.000000000000000000, 0.000000000000000000 ) ) ;
#47889=PRESENTATION_STYLE_ASSIGNMENT (( #58117 ) ) ;
#47890=CARTESIAN_POINT ( 'NONE',  ( 4.441657994896950790, -1.157544474175618676, 104.3851447015617708 ) ) ;
#47923=( NAMED_UNIT ( * ) PLANE_ANGLE_UNIT ( ) SI_UNIT ( $, .RADIAN. ) );
#47938=CARTESIAN_POINT ( 'NONE',  ( -5.000000000000000000, -14.43521912202174207, 12.17944458656183571 ) ) ;
#47941=CARTESIAN_POINT ( 'NONE',  ( 0.000000000000000000, -50.00000000000000000, 112.0000000000000000 ) ) ;
#47954=AXIS2_PLACEMENT_3D ( 'NONE', #38607, #39663, #80093 ) ;
#48000=CARTESIAN_POINT ( 'NONE',  ( 9.995225837605406838, -50.02526524736600066, 26.59626811386029743 ) ) ;
#48001=SURFACE_STYLE_FILL_AREA ( #46434 ) ;
#48004=CARTESIAN_POINT ( 'NONE',  ( -9.995361331467700339, -50.02485175282393470, 26.59863933490087362 ) ) ;
#48014=CARTESIAN_POINT ( 'NONE',  ( 2.745304562109406987, -9.118674939225453357, -12.27857983297191957 ) ) ;
#48024=EDGE_CURVE ( 'NONE', #88009, #30348, #32105, .T. ) ;
#48036=DIRECTION ( 'NONE',  ( 0.000000000000000000, 0.000000000000000000, -1.000000000000000000 ) ) ;
#48050=EDGE_CURVE ( 'NONE', #13645, #35586, #9849, .T. ) ;
#48054=UNCERTAINTY_MEASURE_WITH_UNIT (LENGTH_MEASURE( 1.000000000000000082E-05 ), #77020, 'distance_accuracy_value', 'NONE');
#48094=CARTESIAN_POINT ( 'NONE',  ( 9.864453787710772303, -57.59356044529621244, 25.34106120123098549 ) ) ;
#48147=CIRCLE ( 'NONE', #36128, 2.000000000000001332 ) ;
#48157=( NAMED_UNIT ( * ) PLANE_ANGLE_UNIT ( ) SI_UNIT ( $, .RADIAN. ) );
#48175=CARTESIAN_POINT ( 'NONE',  ( -4.894569681090269242, -46.92198688625742165, 42.70842733634118815 ) ) ;
#48178=CARTESIAN_POINT ( 'NONE',  ( -3.567823017641476468, -49.06830718686870085, 103.5075034329448016 ) ) ;
#48202=FACE_OUTER_BOUND ( 'NONE', #4625, .T. ) ;
#48204=DIRECTION ( 'NONE',  ( 1.000000000000000000, -0.000000000000000000, 2.742080092235280244E-17 ) ) ;
#48265=CARTESIAN_POINT ( 'NONE',  ( -4.946033322322218595, -62.76289455679260954, 12.87575235908490434 ) ) ;
#48275=B_SPLINE_CURVE_WITH_KNOTS ( 'NONE', 3,
 ( #52193, #100218, #1505, #67339, #26385, #59247, #84042, #34991 ),
 .UNSPECIFIED., .F., .F.,
 ( 4, 2, 2, 4 ),
 ( -1.406834188354659210E-05, 0.0004804345972576759484, 0.0007276860668282884121, 0.0009749375363989009301 ),
 .UNSPECIFIED. ) ;
#48285=FILL_AREA_STYLE_COLOUR ( '', #100350 ) ;
#48311=UNCERTAINTY_MEASURE_WITH_UNIT (LENGTH_MEASURE( 1.000000000000000082E-05 ), #53769, 'distance_accuracy_value', 'NONE');
#48333=CARTESIAN_POINT ( 'NONE',  ( 4.175533140205454075, -48.44478104465394352, 102.9090322054120747 ) ) ;
#48343=CARTESIAN_POINT ( 'NONE',  ( -4.031080902170445235, -1.378107924927794770, 103.0284855429834607 ) ) ;
#48356=CARTESIAN_POINT ( 'NONE',  ( 6.691148393531305416, -12.00380193953478702, 9.409600457876800661 ) ) ;
#48374=CARTESIAN_POINT ( 'NONE',  ( -3.068960578197905686, -68.89415226316417318, 13.02640661468439198 ) ) ;
#48448=CARTESIAN_POINT ( 'NONE',  ( -7.372046728244052716, -0.06650713447798785316, 19.15741096255421638 ) ) ;
#48475=CARTESIAN_POINT ( 'NONE',  ( -4.999999999999919176, -15.02849299145000472, 13.75080192255916067 ) ) ;
#48500=UNCERTAINTY_MEASURE_WITH_UNIT (LENGTH_MEASURE( 1.000000000000000082E-05 ), #82929, 'distance_accuracy_value', 'NONE');
#48526=CARTESIAN_POINT ( 'NONE',  ( 4.806394388394678252, -64.29623592462039028, 13.02651880581780830 ) ) ;
#48531=SURFACE_STYLE_USAGE ( .BOTH. , #24827 ) ;
#48550=CARTESIAN_POINT ( 'NONE',  ( 1.444456719620631269, -6.067207855676811867, -13.76482066788863534 ) ) ;
#48589=CARTESIAN_POINT ( 'NONE',  ( -13.09485420365440334, 1.508326549344240153, 14.92433821123424664 ) ) ;
#48623=CARTESIAN_POINT ( 'NONE',  ( 9.215420734788352775, -54.26716484181712019, 23.11721482942554928 ) ) ;
#48630=CARTESIAN_POINT ( 'NONE',  ( 9.389245980427306293, -2.447416405268217243, 14.81682632889905626 ) ) ;
#48632=EDGE_CURVE ( 'NONE', #85394, #76952, #63323, .T. ) ;
#48635=CARTESIAN_POINT ( 'NONE',  ( -2.321165800182301009, -49.78473794090700721, 102.3911379722517552 ) ) ;
#48661=CARTESIAN_POINT ( 'NONE',  ( -9.611186809632508599, -57.00672508581456555, 29.76794951015613933 ) ) ;
#48695=CARTESIAN_POINT ( 'NONE',  ( -1.000000000000000222, -51.24679913437124412, 3.817907945684937410 ) ) ;
#48701=CARTESIAN_POINT ( 'NONE',  ( -4.999999999269103768, -46.35544566583474335, 40.27905619162775253 ) ) ;
#48731=CARTESIAN_POINT ( 'NONE',  ( -0.9999999999999943379, 0.000000000000000000, 101.0455488498966758 ) ) ;
#48741=EDGE_LOOP ( 'NONE', ( #104045, #61400, #94799, #84879 ) ) ;
#48763=ORIENTED_EDGE ( 'NONE', *, *, #22339, .T. ) ;
#48780=CARTESIAN_POINT ( 'NONE',  ( -5.000000000000000000, -32.50000000000000000, 12.61250543006184088 ) ) ;
#48790=CARTESIAN_POINT ( 'NONE',  ( -4.821429483474614308, -68.14062186280141020, 13.85322958606745658 ) ) ;
#48799=FILL_AREA_STYLE ('',( #9947 ) ) ;
#48816=CARTESIAN_POINT ( 'NONE',  ( -1.000000000000002442, -4.000000000000000000, 27.00000000000000000 ) ) ;
#48825=CARTESIAN_POINT ( 'NONE',  ( -4.999999999999998224, -31.04507124266364926, -0.1867410044140281056 ) ) ;
#48833=CARTESIAN_POINT ( 'NONE',  ( 15.90423112858387711, -2.036632359883284504, 14.86380772883778789 ) ) ;
#48846=CARTESIAN_POINT ( 'NONE',  ( 12.31569210610433274, -4.628390024190414564, 20.34132785121827780 ) ) ;
#48851=CARTESIAN_POINT ( 'NONE',  ( 0.9330442100808692407, -70.05675763226146557, 13.03100537459355124 ) ) ;
#48870=CARTESIAN_POINT ( 'NONE',  ( 3.352941176470599860, -1.200583151104954061, 104.5794940929807524 ) ) ;
#48880=CARTESIAN_POINT ( 'NONE',  ( 6.386171959437453083, -11.88579060466483561, 10.72108492130595359 ) ) ;
#48895=CARTESIAN_POINT ( 'NONE',  ( 6.362732954939756880, -11.89495883945591359, 10.82964177580675980 ) ) ;
#48900=CARTESIAN_POINT ( 'NONE',  ( 3.857142857142846992, -48.79941684889506348, 103.1763305333244176 ) ) ;
#48912=ORIENTED_EDGE ( 'NONE', *, *, #77644, .T. ) ;
#48926=EDGE_CURVE ( 'NONE', #67342, #33663, #89571, .T. ) ;
#48929=CARTESIAN_POINT ( 'NONE',  ( -4.928386788250817219, -48.42812442315221944, 104.2441249819463280 ) ) ;
#48943=STYLED_ITEM ( 'NONE', ( #7814 ), #87198 ) ;
#48965=CYLINDRICAL_SURFACE ( 'NONE', #58030, 2.000000000000001776 ) ;
#48981=AXIS2_PLACEMENT_3D ( 'NONE', #18888, #35596, #91682 ) ;
#48999=CARTESIAN_POINT ( 'NONE',  ( -6.125000000000000000, -15.62228920881131700, 14.41094225130410855 ) ) ;
#49009=DIRECTION ( 'NONE',  ( 0.000000000000000000, 0.2105263157894737835, -0.9775881905793005755 ) ) ;
#49022=CARTESIAN_POINT ( 'NONE',  ( 9.389245980427297411, -2.447416405268218131, 14.81682632889905626 ) ) ;
#49025=COLOUR_RGB ( '', 0.66274510, 0.83137255, 0.94901961) ;
#49030=AXIS2_PLACEMENT_3D ( 'NONE', #61866, #20911, #69417 ) ;
#49062=CARTESIAN_POINT ( 'NONE',  ( 9.611186809632508599, -50.99327491418545577, 29.76794951015613933 ) ) ;
#49069=CARTESIAN_POINT ( 'NONE',  ( 27.99999999999999645, 1.592040838891559095E-15, 13.00000000000000000 ) ) ;
#49080=ADVANCED_FACE ( 'NONE', ( #61277 ), #106713, .T. ) ;
#49083=SURFACE_STYLE_FILL_AREA ( #98179 ) ;
#49153=FACE_OUTER_BOUND ( 'NONE', #18841, .T. ) ;
#49160=EDGE_CURVE ( 'NONE', #43590, #12840, #72520, .T. ) ;
#49187=B_SPLINE_CURVE_WITH_KNOTS ( 'NONE', 3,
 ( #83938, #12168, #87147, #54208, #93641, #20866, #45100, #70948, #44564, #101719 ),
 .UNSPECIFIED., .F., .F.,
 ( 4, 2, 2, 2, 4 ),
 ( 0.000000000000000000, 0.0008124082233779007355, 0.001624816446755801471, 0.002437224670133701990, 0.003249632893511602942 ),
 .UNSPECIFIED. ) ;
#49188=CARTESIAN_POINT ( 'NONE',  ( -6.018823944621538580, -50.31891336156137839, 39.64063426992244388 ) ) ;
#49252=( LENGTH_UNIT ( ) NAMED_UNIT ( * ) SI_UNIT ( .MILLI., .METRE. ) );
#49261=SURFACE_SIDE_STYLE ('',( #7216 ) ) ;
#49263=( NAMED_UNIT ( * ) PLANE_ANGLE_UNIT ( ) SI_UNIT ( $, .RADIAN. ) );
#49266=CARTESIAN_POINT ( 'NONE',  ( -3.352941176470600304, -1.200583151104954283, 104.5794940929807524 ) ) ;
#49295=( NAMED_UNIT ( * ) SI_UNIT ( $, .STERADIAN. ) SOLID_ANGLE_UNIT ( ) );
#49297=SURFACE_SIDE_STYLE ('',( #16417 ) ) ;
#49309=CARTESIAN_POINT ( 'NONE',  ( -14.91858118607497019, 1.255821567010171884E-17, 15.00000000000000000 ) ) ;
#49314=CIRCLE ( 'NONE', #2819, 12.00000000000000000 ) ;
#49324=CARTESIAN_POINT ( 'NONE',  ( -4.755599198601705879, -66.38001295931699985, 13.81229897532385564 ) ) ;
#49325=CARTESIAN_POINT ( 'NONE',  ( 1.238781280703658005, -50.00000000000000000, 101.3451024322821894 ) ) ;
#49332=CARTESIAN_POINT ( 'NONE',  ( 4.551587301587296075, -48.79941684889506348, 104.4018401814738155 ) ) ;
#49342=CARTESIAN_POINT ( 'NONE',  ( 4.999999999999996447, -45.99999999999997868, 40.27905619136139137 ) ) ;
#49353=( NAMED_UNIT ( * ) SI_UNIT ( $, .STERADIAN. ) SOLID_ANGLE_UNIT ( ) );
#49386=CARTESIAN_POINT ( 'NONE',  ( 4.692764267120560717, -68.34565006887950744, 13.80912607275098658 ) ) ;
#49389=FILL_AREA_STYLE_COLOUR ( '', #52421 ) ;
#49395=SHAPE_REPRESENTATION ( '3. Bracket', ( #10728 ), #7340 ) ;
#49403=AXIS2_PLACEMENT_3D ( 'NONE', #76136, #68052, #99886 ) ;
#49422=CARTESIAN_POINT ( 'NONE',  ( 5.000000000000000000, -14.90207541444466166, 12.47233211435964506 ) ) ;
#49431=CARTESIAN_POINT ( 'NONE',  ( 5.901338098438385416, -64.37119818154236839, 14.30438978747334033 ) ) ;
#49438=CARTESIAN_POINT ( 'NONE',  ( 10.00200699113076652, -0.6430754150849513628, 20.04989093843450121 ) ) ;
#49441=SURFACE_STYLE_USAGE ( .BOTH. , #88857 ) ;
#49451=EDGE_CURVE ( 'NONE', #57919, #4171, #87875, .T. ) ;
#49475=CARTESIAN_POINT ( 'NONE',  ( -4.211261491276468760, -48.41319459706108574, 103.7733746176733689 ) ) ;
#49505=CARTESIAN_POINT ( 'NONE',  ( 3.352941176470589646, -48.79941684889505638, 104.5794940929807524 ) ) ;
#49507=EDGE_CURVE ( 'NONE', #97345, #30914, #36260, .T. ) ;
#49526=MECHANICAL_DESIGN_GEOMETRIC_PRESENTATION_REPRESENTATION('',(#101220),#54680);
#49544=CARTESIAN_POINT ( 'NONE',  ( -4.999999999999999112, -12.61682532715667904, 11.58371340991526921 ) ) ;
#49566=CARTESIAN_POINT ( 'NONE',  ( 15.66776169706031396, -1.217559620640022100, 14.95230841597768290 ) ) ;
#49619=STYLED_ITEM ( 'NONE', ( #20527 ), #68261 ) ;
#49644=B_SPLINE_CURVE_WITH_KNOTS ( 'NONE', 3,
 ( #8084, #58228, #91157, #17263, #89547, #31856, #82511, #56625, #6485, #80907, #64736, #106773, #33451, #105198, #97613, #48000, #32922, #15642, #39416, #98675, #65265, #40988, #16715, #74401, #49062, #65798, #64224, #8613, #39935, #24829, #7538, #40454, #481, #90605 ),
 .UNSPECIFIED., .F., .F.,
 ( 4, 2, 2, 2, 2, 2, 2, 2, 2, 2, 2, 2, 2, 2, 2, 2, 4 ),
 ( 6.938893903907228378E-18, 0.0007899780065504824781, 0.001579956013100958017, 0.002369934019651433448, 0.003159912026201909096, 0.003949890032752384310, 0.004739868039302859958, 0.005529846045853335605, 0.006319824052403811253, 0.007109802058954286900, 0.007899780065504761681, 0.008689758072055237328, 0.009479736078605712976, 0.01026971408515618862, 0.01105969209170666427, 0.01184967009825713992, 0.01263964810480761557 ),
 .UNSPECIFIED. ) ;
#49667=ORIENTED_EDGE ( 'NONE', *, *, #12325, .F. ) ;
#49692=FACE_OUTER_BOUND ( 'NONE', #21453, .T. ) ;
#49700=CARTESIAN_POINT ( 'NONE',  ( 9.612665144396085992, -57.01130939352533744, 29.76292019730385618 ) ) ;
#49703=CARTESIAN_POINT ( 'NONE',  ( -5.000000000000000888, -4.000000000000003553, 40.07669683062201926 ) ) ;
#49707=( NAMED_UNIT ( * ) SI_UNIT ( $, .STERADIAN. ) SOLID_ANGLE_UNIT ( ) );
#49729=CARTESIAN_POINT ( 'NONE',  ( 4.999999999999995559, -46.00000000000000000, 42.58845726811989607 ) ) ;
#49741=CARTESIAN_POINT ( 'NONE',  ( -3.857142857142850989, -1.200583151104938517, 103.1763305333244318 ) ) ;
#49747=PRESENTATION_STYLE_ASSIGNMENT (( #8755 ) ) ;
#49750=FILL_AREA_STYLE ('',( #91819 ) ) ;
#49761=B_SPLINE_CURVE_WITH_KNOTS ( 'NONE', 3,
 ( #68670, #3921, #61101, #77808, #67065, #101550, #93470, #99946, #19620, #26119, #88553, #29295, #70775, #79913, #22250, #62181 ),
 .UNSPECIFIED., .F., .F.,
 ( 4, 2, 2, 2, 2, 2, 2, 4 ),
 ( 0.000000000000000000, 0.01751496934764543850, 0.03502993869529087700, 0.04378742336911359279, 0.05254490804293632245, 0.06130239271675903823, 0.06568113505367038918, 0.07005987739058174013 ),
 .UNSPECIFIED. ) ;
#49791=CIRCLE ( 'NONE', #89222, 12.00000000000000000 ) ;
#49801=PRESENTATION_STYLE_ASSIGNMENT (( #58437 ) ) ;
#49804=CARTESIAN_POINT ( 'NONE',  ( -4.805888432417104283, -14.59013712844724786, -7.778733730875007524 ) ) ;
#49806=LINE ( 'NONE', #91351, #106698 ) ;
#49826=CARTESIAN_POINT ( 'NONE',  ( 1.347111479062088207E-15, -50.00000000000000000, 100.9999999999999858 ) ) ;
#49855=DIRECTION ( 'NONE',  ( 1.000000000000000000, 0.000000000000000000, 0.000000000000000000 ) ) ;
#49867=CARTESIAN_POINT ( 'NONE',  ( -3.757130767675045835, -69.58003094729899374, 13.51214695925444609 ) ) ;
#49869=EDGE_CURVE ( 'NONE', #66555, #104368, #53037, .T. ) ;
#49875=CARTESIAN_POINT ( 'NONE',  ( 4.334722950428502308, -48.88070975476235702, 104.3859289939585864 ) ) ;
#49908=CARTESIAN_POINT ( 'NONE',  ( 14.91858118607497374, 2.271260765197548532E-16, 15.00000000000000000 ) ) ;
#49910=VECTOR ( 'NONE', #42138, 1000.000000000000000 ) ;
#49921=CARTESIAN_POINT ( 'NONE',  ( -0.9999999999999943379, -50.00000000000000000, 101.0455488498966758 ) ) ;
#49926=CARTESIAN_POINT ( 'NONE',  ( 6.075632316336291971, -62.90659182483985745, 14.38622881700373490 ) ) ;
#49929=( NAMED_UNIT ( * ) PLANE_ANGLE_UNIT ( ) SI_UNIT ( $, .RADIAN. ) );
#49939=FACE_BOUND ( 'NONE', #77657, .T. ) ;
#49943=CARTESIAN_POINT ( 'NONE',  ( 4.744389013293893065, -1.372925465831636327, 104.3204960233004357 ) ) ;
#49954=CARTESIAN_POINT ( 'NONE',  ( 5.000000000000000000, -14.73708290046165281, 12.39211607765093426 ) ) ;
#49971=CARTESIAN_POINT ( 'NONE',  ( 6.125000000000095923, -15.62228920881129390, 14.41094225130415651 ) ) ;
#49972=FACE_OUTER_BOUND ( 'NONE', #104548, .T. ) ;
#49976=CARTESIAN_POINT ( 'NONE',  ( 5.000000000093224095, -46.22753318115157128, 103.2791840072271015 ) ) ;
#49988=AXIS2_PLACEMENT_3D ( 'NONE', #38273, #87862, #71132 ) ;
#49992=CARTESIAN_POINT ( 'NONE',  ( -6.138854265193438131, -12.09086120632721872, -8.896243454972955433 ) ) ;
#49998=ADVANCED_FACE ( 'NONE', ( #99063, #59174 ), #25229, .F. ) ;
#50017=FACE_OUTER_BOUND ( 'NONE', #18595, .T. ) ;
#50025=DIRECTION ( 'NONE',  ( 1.000000000000000000, 0.000000000000000000, 0.000000000000000000 ) ) ;
#50099=CARTESIAN_POINT ( 'NONE',  ( 14.24611712352057857, 0.6929283341933295537, 14.98501566461477985 ) ) ;
#50161=CARTESIAN_POINT ( 'NONE',  ( -11.96518466135214886, -2.129975200491694753, 20.65966393205720664 ) ) ;
#50178=( BOUNDED_SURFACE ( )  B_SPLINE_SURFACE ( 3, 2, ( 
 ( #93309, #42083, #59357 ),
 ( #74971, #17836, #83601 ),
 ( #67444, #35095, #51224 ),
 ( #9706, #87348, #93837 ),
 ( #69569, #21054, #29152 ),
 ( #45295, #78174, #52839 ),
 ( #12369, #53892, #79235 ),
 ( #38792, #4293, #37760 ),
 ( #36704, #5363, #19996 ),
 ( #12893, #70624, #102992 ),
 ( #86823, #54401, #61488 ),
 ( #53380, #71662, #62023 ),
 ( #3772, #102458, #60948 ),
 ( #38281, #37225, #71144 ),
 ( #28606, #103514, #94381 ),
 ( #85764, #45821, #21562 ),
 ( #11838, #20542, #86299 ),
 ( #29667, #4825, #78691 ),
 ( #70089, #44768, #13423 ),
 ( #94918, #54944, #62537 ),
 ( #95424, #46346, #104034 ),
 ( #30174, #77658, #63066 ),
 ( #95965, #22090, #79762 ),
 ( #87872, #13956, #46866 ),
 ( #5868, #28077, #48448 ),
 ( #82427, #7994, #57070 ),
 ( #65714, #41430, #39331 ),
 ( #40366, #89465, #15558 ) ),
 .UNSPECIFIED., .F., .F., .F. ) 
 B_SPLINE_SURFACE_WITH_KNOTS ( ( 4, 2, 2, 2, 2, 2, 2, 2, 2, 2, 2, 2, 2, 4 ),
 ( 3, 3 ),
 ( 0.008123433161209985681, 0.009051127437186799740, 0.009978821713163612064, 0.01090651598914042439, 0.01183421026511723845, 0.01276190454109405077, 0.01368959881707086310, 0.01461729309304767715, 0.01554498736902448948, 0.01647268164500130180, 0.01740037592097811586, 0.01925576447293174051, 0.02111115302488536516, 0.02296654157683899328 ),
 ( 0.000000000000000000, 1.000000000000000000 ),
 .UNSPECIFIED. ) 
 GEOMETRIC_REPRESENTATION_ITEM ( )  RATIONAL_B_SPLINE_SURFACE ( (
 ( 1.000000000000000000, 0.5207636911093219689, 1.000000000000000000),
 ( 1.000000000000000000, 0.5178187716629953918, 1.000000000000000000),
 ( 1.000000000000000000, 0.5159244862375357288, 1.000000000000000000),
 ( 1.000000000000000000, 0.5142886050002780651, 1.000000000000000000),
 ( 1.000000000000000000, 0.5145473390822793425, 1.000000000000000000),
 ( 1.000000000000000000, 0.5172493923475872668, 1.000000000000000000),
 ( 1.000000000000000000, 0.5196793001234910614, 1.000000000000000000),
 ( 1.000000000000000000, 0.5263251517290957748, 1.000000000000000000),
 ( 1.000000000000000000, 0.5305477076593381192, 1.000000000000000000),
 ( 1.000000000000000000, 0.5405083355075952500, 1.000000000000000000),
 ( 1.000000000000000000, 0.5462226599306142516, 1.000000000000000000),
 ( 1.000000000000000000, 0.5585066026749704315, 1.000000000000000000),
 ( 1.000000000000000000, 0.5651105631668802420, 1.000000000000000000),
 ( 1.000000000000000000, 0.5789734458161401864, 1.000000000000000000),
 ( 1.000000000000000000, 0.5862399530452739871, 1.000000000000000000),
 ( 1.000000000000000000, 0.6008664520152333655, 1.000000000000000000),
 ( 1.000000000000000000, 0.6082721003052478093, 1.000000000000000000),
 ( 1.000000000000000000, 0.6231433865265936234, 1.000000000000000000),
 ( 1.000000000000000000, 0.6306097951832441151, 1.000000000000000000),
 ( 1.000000000000000000, 0.6455317574246466350, 1.000000000000000000),
 ( 1.000000000000000000, 0.6530101251172123478, 1.000000000000000000),
 ( 1.000000000000000000, 0.6749576138080563004, 1.000000000000000000),
 ( 1.000000000000000000, 0.6890737998548138732, 1.000000000000000000),
 ( 1.000000000000000000, 0.7163646493011636140, 1.000000000000000000),
 ( 1.000000000000000000, 0.7295941717914107283, 1.000000000000000000),
 ( 1.000000000000000000, 0.7548878312893493314, 1.000000000000000000),
 ( 1.000000000000000000, 0.7668601322836052780, 1.000000000000000000),
 ( 1.000000000000000000, 0.7779866052154993383, 1.000000000000000000) ) ) 
 REPRESENTATION_ITEM ( '' )  SURFACE ( )  );
#50185=( LENGTH_UNIT ( ) NAMED_UNIT ( * ) SI_UNIT ( .MILLI., .METRE. ) );
#50195=CARTESIAN_POINT ( 'NONE',  ( -30.00000000000000000, -54.00000000000000711, 23.11721482942554928 ) ) ;
#50200=CIRCLE ( 'NONE', #96727, 9.000000000000000000 ) ;
#50232=SURFACE_STYLE_USAGE ( .BOTH. , #57776 ) ;
#50237=CARTESIAN_POINT ( 'NONE',  ( 5.000000000000000000, -3.274104202382571494, -10.50969124766998952 ) ) ;
#50243=AXIS2_PLACEMENT_3D ( 'NONE', #44807, #77696, #63101 ) ;
#50244=CARTESIAN_POINT ( 'NONE',  ( -1.992238869817497093, -49.88365665291251361, 102.1880563748276955 ) ) ;
#50270=FILL_AREA_STYLE_COLOUR ( '', #23577 ) ;
#50280=VERTEX_POINT ( 'NONE', #97891 ) ;
#50282=FACE_OUTER_BOUND ( 'NONE', #14260, .T. ) ;
#50293=CARTESIAN_POINT ( 'NONE',  ( -1.000000000000000000, -67.36501624957764989, 11.52273887415191922 ) ) ;
#50328=CARTESIAN_POINT ( 'NONE',  ( -4.293150003527051339, -12.96978500885295738, -9.455099716441258906 ) ) ;
#50391=ORIENTED_EDGE ( 'NONE', *, *, #78918, .F. ) ;
#50429=( GEOMETRIC_REPRESENTATION_CONTEXT ( 3 ) GLOBAL_UNCERTAINTY_ASSIGNED_CONTEXT ( ( #83800 ) ) GLOBAL_UNIT_ASSIGNED_CONTEXT ( ( #3972, #43889, #70304 ) ) REPRESENTATION_CONTEXT ( 'NONE', 'WORKASPACE' ) );
#50448=CARTESIAN_POINT ( 'NONE',  ( 2.760661874148076844, -69.15507977559171593, 12.98220749377402683 ) ) ;
#50451=DIRECTION ( 'NONE',  ( 0.000000000000000000, 0.000000000000000000, -1.000000000000000000 ) ) ;
#50531=( GEOMETRIC_REPRESENTATION_CONTEXT ( 3 ) GLOBAL_UNCERTAINTY_ASSIGNED_CONTEXT ( ( #65645 ) ) GLOBAL_UNIT_ASSIGNED_CONTEXT ( ( #94094, #85479, #86561 ) ) REPRESENTATION_CONTEXT ( 'NONE', 'WORKASPACE' ) );
#50556=CARTESIAN_POINT ( 'NONE',  ( -30.00000000000000000, 1.347111479062088405E-15, 11.00000000000000000 ) ) ;
#50578=( LENGTH_UNIT ( ) NAMED_UNIT ( * ) SI_UNIT ( .MILLI., .METRE. ) );
#50596=DIRECTION ( 'NONE',  ( 0.000000000000000000, 0.000000000000000000, -1.000000000000000000 ) ) ;
#50608=CARTESIAN_POINT ( 'NONE',  ( 11.81783007639908334, -1.930264526412683868, 20.62761066482512717 ) ) ;
#50665=CARTESIAN_POINT ( 'NONE',  ( -10.52454070266728792, -0.8718843809977038228, 20.23127905671319837 ) ) ;
#50671=DIRECTION ( 'NONE',  ( 1.000000000000000000, -0.000000000000000000, -0.000000000000000000 ) ) ;
#50678=CARTESIAN_POINT ( 'NONE',  ( -1.000000000000000000, -69.59657292933731298, 12.76848391598547394 ) ) ;
#50679=CARTESIAN_POINT ( 'NONE',  ( 4.324913936355947008, -1.111773959251803445, 104.4044995709989934 ) ) ;
#50689=EDGE_LOOP ( 'NONE', ( #58953, #27120, #31145, #66595 ) ) ;
#50692=ORIENTED_EDGE ( 'NONE', *, *, #92792, .F. ) ;
#50712=COLOUR_RGB ( '', 0.40784314, 0.44705882, 0.49803922) ;
#50714=CARTESIAN_POINT ( 'NONE',  ( -4.302760725356050919, -1.102344419738585879, 104.4121068519184945 ) ) ;
#50723=CARTESIAN_POINT ( 'NONE',  ( -13.87268571384243465, -50.40938940377537847, 28.89968788215285755 ) ) ;
#50742=CARTESIAN_POINT ( 'NONE',  ( -3.460324465708875863, -1.165480915299198728, 104.5902739981059426 ) ) ;
#50745=( NAMED_UNIT ( * ) PLANE_ANGLE_UNIT ( ) SI_UNIT ( $, .RADIAN. ) );
#50750=CARTESIAN_POINT ( 'NONE',  ( 9.241147685141145374, -13.39842114471960066, 16.48049835958764575 ) ) ;
#50755=CARTESIAN_POINT ( 'NONE',  ( -1.468752096361391368, -49.97154544718587488, 101.6458968146044697 ) ) ;
#50762=DIRECTION ( 'NONE',  ( 0.000000000000000000, 0.000000000000000000, 1.000000000000000000 ) ) ;
#50768=DIRECTION ( 'NONE',  ( -0.000000000000000000, -1.000000000000000000, -0.000000000000000000 ) ) ;
#50792=( NAMED_UNIT ( * ) PLANE_ANGLE_UNIT ( ) SI_UNIT ( $, .RADIAN. ) );
#50805=FILL_AREA_STYLE_COLOUR ( '', #50712 ) ;
#50812=CARTESIAN_POINT ( 'NONE',  ( -4.999999999997459810, -63.35894816178143429, 9.450637109162125071 ) ) ;
#50839=FILL_AREA_STYLE_COLOUR ( '', #70148 ) ;
#50849=CARTESIAN_POINT ( 'NONE',  ( 3.685905252136449928, -1.041089327947708032, 104.2837900504744510 ) ) ;
#50855=CARTESIAN_POINT ( 'NONE',  ( -1.000000000000000888, -4.000000000000000000, 42.58845726811989607 ) ) ;
#50870=CARTESIAN_POINT ( 'NONE',  ( 11.39273938773877326, -10.91116184185876037, 10.30307882325512558 ) ) ;
#50881=CARTESIAN_POINT ( 'NONE',  ( 2.505816879450918577, -0.4130341807012217203, 103.1328224996094747 ) ) ;
#50891=FILL_AREA_STYLE_COLOUR ( '', #54748 ) ;
#50931=EDGE_CURVE ( 'NONE', #99036, #62818, #105542, .T. ) ;
#50978=CARTESIAN_POINT ( 'NONE',  ( 5.560201442585154474, -66.10109771767969278, 14.15124469594628387 ) ) ;
#51007=CARTESIAN_POINT ( 'NONE',  ( 5.000000000000041744, -12.81882114895618052, 11.98449427368572451 ) ) ;
#51032=ORIENTED_EDGE ( 'NONE', *, *, #76974, .T. ) ;
#51058=MECHANICAL_DESIGN_GEOMETRIC_PRESENTATION_REPRESENTATION('',(#95896),#2868);
#51091=CARTESIAN_POINT ( 'NONE',  ( 5.687306430306777294, -50.94086591487122462, 39.79591033833035141 ) ) ;
#51097=B_SPLINE_CURVE_WITH_KNOTS ( 'NONE', 3,
 ( #92921, #84839, #84309, #99951, #59512, #27711, #10404, #68120, #75672, #35796, #9331, #67602, #76733, #2304, #58443, #76201, #35252, #101016, #43842, #68674, #17466, #1773 ),
 .UNSPECIFIED., .F., .F.,
 ( 4, 2, 2, 2, 2, 2, 2, 2, 2, 2, 4 ),
 ( 0.002104729445818187550, 0.004038629005729561100, 0.005972528565640933783, 0.007906428125552308200, 0.009840327685463680016, 0.01177422724537505357, 0.01274117702533074208, 0.01370812680528642885, 0.01467507658524211736, 0.01564202636519780587, 0.01757592592510918289 ),
 .UNSPECIFIED. ) ;
#51115=ORIENTED_EDGE ( 'NONE', *, *, #99714, .F. ) ;
#51134=ORIENTED_EDGE ( 'NONE', *, *, #15787, .T. ) ;
#51151=CARTESIAN_POINT ( 'NONE',  ( 9.285924700174383872, -2.939022340138890410, 14.74017746627012571 ) ) ;
#51174=MECHANICAL_DESIGN_GEOMETRIC_PRESENTATION_REPRESENTATION('',(#40790),#4630);
#51178=CIRCLE ( 'NONE', #78663, 2.000000000000000000 ) ;
#51179=CARTESIAN_POINT ( 'NONE',  ( 5.000000000000000000, -15.63336956925477672, -6.409577599286647498 ) ) ;
#51219=DIRECTION ( 'NONE',  ( -0.000000000000000000, -1.000000000000000000, -0.000000000000000000 ) ) ;
#51224=CARTESIAN_POINT ( 'NONE',  ( -12.41115067335719147, -3.692203772662941752, 20.54117717663471510 ) ) ;
#51286=DIRECTION ( 'NONE',  ( -1.096832036894112098E-16, -0.000000000000000000, -1.000000000000000000 ) ) ;
#51290=CARTESIAN_POINT ( 'NONE',  ( 7.824046388961988896, -14.69261508678956929, 15.37861778814678537 ) ) ;
#51317=( NAMED_UNIT ( * ) SI_UNIT ( $, .STERADIAN. ) SOLID_ANGLE_UNIT ( ) );
#51321=FILL_AREA_STYLE ('',( #50270 ) ) ;
#51336=( NAMED_UNIT ( * ) SI_UNIT ( $, .STERADIAN. ) SOLID_ANGLE_UNIT ( ) );
#51348=FILL_AREA_STYLE ('',( #27127 ) ) ;
#51354=CARTESIAN_POINT ( 'NONE',  ( -1.000000000000000000, -68.69775162920851130, 12.24814655257177343 ) ) ;
#51379=CIRCLE ( 'NONE', #4910, 13.00000000000000000 ) ;
#51387=CARTESIAN_POINT ( 'NONE',  ( 3.423905177084556328, -0.8279751000742714417, 103.8439100969722375 ) ) ;
#51390=CARTESIAN_POINT ( 'NONE',  ( -4.962899348969606272, -12.37352932398175298, -8.506080509220907970 ) ) ;
#51410=CARTESIAN_POINT ( 'NONE',  ( 12.74530331293310681, -9.910444218107741676, 11.27135949044345686 ) ) ;
#51430=CARTESIAN_POINT ( 'NONE',  ( -4.284822031655012076, -48.90716638558769347, 104.4267991316944375 ) ) ;
#51434=( NAMED_UNIT ( * ) PLANE_ANGLE_UNIT ( ) SI_UNIT ( $, .RADIAN. ) );
#51458=CARTESIAN_POINT ( 'NONE',  ( -5.000000000000000888, -46.00000000000000000, 42.58845726811989607 ) ) ;
#51476=CARTESIAN_POINT ( 'NONE',  ( 3.703334511254893879, -49.04702021385453037, 40.67780616083587120 ) ) ;
#51503=CARTESIAN_POINT ( 'NONE',  ( 4.969648522638418164, -46.56352935199780774, 42.62389940716953163 ) ) ;
#51506=DIRECTION ( 'NONE',  ( 0.000000000000000000, 2.775557561562891351E-13, -1.000000000000000000 ) ) ;
#51553=CARTESIAN_POINT ( 'NONE',  ( 4.999999999999961808, -13.16121988547497246, 12.48675270919411595 ) ) ;
#51563=UNCERTAINTY_MEASURE_WITH_UNIT (LENGTH_MEASURE( 1.000000000000000082E-05 ), #92316, 'distance_accuracy_value', 'NONE');
#51568=CARTESIAN_POINT ( 'NONE',  ( -13.76566278825922574, -57.17796501950922305, 29.56014984665260670 ) ) ;
#51571=CARTESIAN_POINT ( 'NONE',  ( 8.011576988516077691, -0.1388693685375959608, 19.36711618773636445 ) ) ;
#51629=B_SPLINE_CURVE_WITH_KNOTS ( 'NONE', 3,
 ( #98035, #24187, #57032, #89947, #81829, #7954, #73754, #106650, #34808, #32802 ),
 .UNSPECIFIED., .F., .F.,
 ( 4, 2, 2, 2, 4 ),
 ( -1.267662083617060480E-05, 0.001114285917661883346, 0.002241248456159937019, 0.003368210994657990908, 0.004495173533156045231 ),
 .UNSPECIFIED. ) ;
#51662=VERTEX_POINT ( 'NONE', #92874 ) ;
#51679=ADVANCED_FACE ( 'NONE', ( #93425 ), #75056, .F. ) ;
#51692=FACE_OUTER_BOUND ( 'NONE', #74581, .T. ) ;
#51695=CARTESIAN_POINT ( 'NONE',  ( 4.073826509763722292, -48.95212347009485399, 104.5376934966453746 ) ) ;
#51707=ORIENTED_EDGE ( 'NONE', *, *, #36708, .F. ) ;
#51740=( NAMED_UNIT ( * ) PLANE_ANGLE_UNIT ( ) SI_UNIT ( $, .RADIAN. ) );
#51776=DIRECTION ( 'NONE',  ( -1.000000000000000000, -0.000000000000000000, -0.000000000000000000 ) ) ;
#51804=CARTESIAN_POINT ( 'NONE',  ( -13.60728112438141402, -51.55816952290514621, 30.29609480636782592 ) ) ;
#51805=CARTESIAN_POINT ( 'NONE',  ( -5.000000000000000000, -14.73409751812503110, 12.39902340069096098 ) ) ;
#51856=CARTESIAN_POINT ( 'NONE',  ( 1.468822083365114439, -49.97157980006149103, 101.6459669435612625 ) ) ;
#51878=CARTESIAN_POINT ( 'NONE',  ( 8.593983530299054152, -1.221393525206185826, 15.49134170070576211 ) ) ;
#51897=CARTESIAN_POINT ( 'NONE',  ( 14.91858118607497374, 2.271260765197548532E-16, 15.00000000000000000 ) ) ;
#51916=ORIENTED_EDGE ( 'NONE', *, *, #21221, .T. ) ;
#51919=CARTESIAN_POINT ( 'NONE',  ( 3.769311339735795574, -1.074854658864329959, 104.1674216685381396 ) ) ;
#51954=EDGE_CURVE ( 'NONE', #92559, #96331, #67627, .T. ) ;
#51957=CARTESIAN_POINT ( 'NONE',  ( 4.211261491277978664, -1.586805402942760068, 103.7733746176805880 ) ) ;
#51968=( NAMED_UNIT ( * ) PLANE_ANGLE_UNIT ( ) SI_UNIT ( $, .RADIAN. ) );
#51990=AXIS2_PLACEMENT_3D ( 'NONE', #99429, #66018, #74628 ) ;
#52004=CARTESIAN_POINT ( 'NONE',  ( 5.446579913478287516, -51.29466139981784778, 39.89783452207186087 ) ) ;
#52017=COLOUR_RGB ( '', 0.09019608, 0.27058824, 0.51372549) ;
#52084=CARTESIAN_POINT ( 'NONE',  ( 2.680426334985284598, -7.322430019223747699, -13.10127437669147099 ) ) ;
#52085=EDGE_CURVE ( 'NONE', #25416, #96331, #2567, .T. ) ;
#52087=ORIENTED_EDGE ( 'NONE', *, *, #103113, .T. ) ;
#52096=UNCERTAINTY_MEASURE_WITH_UNIT (LENGTH_MEASURE( 1.000000000000000082E-05 ), #79866, 'distance_accuracy_value', 'NONE');
#52100=CARTESIAN_POINT ( 'NONE',  ( -13.97203307284001994, -57.87174520061537208, 26.07838388608699631 ) ) ;
#52105=( LENGTH_UNIT ( ) NAMED_UNIT ( * ) SI_UNIT ( .MILLI., .METRE. ) );
#52142=FILL_AREA_STYLE_COLOUR ( '', #764 ) ;
#52145=EDGE_CURVE ( 'NONE', #71499, #88866, #19257, .T. ) ;
#52160=( GEOMETRIC_REPRESENTATION_CONTEXT ( 3 ) GLOBAL_UNCERTAINTY_ASSIGNED_CONTEXT ( ( #76141 ) ) GLOBAL_UNIT_ASSIGNED_CONTEXT ( ( #23130, #78667, #39307 ) ) REPRESENTATION_CONTEXT ( 'NONE', 'WORKASPACE' ) );
#52162=STYLED_ITEM ( 'NONE', ( #79323 ), #94732 ) ;
#52193=CARTESIAN_POINT ( 'NONE',  ( -3.352941176470600304, -1.200583151104954283, 104.5794940929807524 ) ) ;
#52226=CARTESIAN_POINT ( 'NONE',  ( 3.564365538398770017, -48.86493411501010087, 104.5953911288812463 ) ) ;
#52235=COLOUR_RGB ( '', 0.72549020, 0.75294118, 0.79215686) ;
#52251=CARTESIAN_POINT ( 'NONE',  ( 5.136066607408869444, -12.96798121126263936, -7.569033233149855100 ) ) ;
#52275=DIRECTION ( 'NONE',  ( -3.552713678800500535E-15, 0.000000000000000000, 1.000000000000000000 ) ) ;
#52300=SURFACE_SIDE_STYLE ('',( #44227 ) ) ;
#52309=CIRCLE ( 'NONE', #74705, 15.00000000000000000 ) ;
#52315=SURFACE_SIDE_STYLE ('',( #68526 ) ) ;
#52336=CARTESIAN_POINT ( 'NONE',  ( -13.64654340589911818, -51.35783868776468353, 30.13167154758286159 ) ) ;
#52352=CARTESIAN_POINT ( 'NONE',  ( -3.355892750373842048, -0.9951980364987413896, 104.3125661743353589 ) ) ;
#52377=DIRECTION ( 'NONE',  ( 0.000000000000000000, 0.000000000000000000, 1.000000000000000000 ) ) ;
#52391=CARTESIAN_POINT ( 'NONE',  ( -9.113097280746998763, -53.73699350858575485, 31.11721482942554928 ) ) ;
#52399=CARTESIAN_POINT ( 'NONE',  ( -4.334722950434925615, -1.119290245239405790, 104.3859289939576627 ) ) ;
#52407=PRESENTATION_STYLE_ASSIGNMENT (( #36289 ) ) ;
#52409=ORIENTED_EDGE ( 'NONE', *, *, #24278, .F. ) ;
#52421=COLOUR_RGB ( '', 0.40784314, 0.44705882, 0.49803922) ;
#52441=FILL_AREA_STYLE ('',( #50839 ) ) ;
#52447=EDGE_LOOP ( 'NONE', ( #15177, #71909, #51115, #75058 ) ) ;
#52451=CARTESIAN_POINT ( 'NONE',  ( 4.073826509764633563, -1.047876529905043874, 104.5376934966472220 ) ) ;
#52456=SURFACE_STYLE_FILL_AREA ( #78329 ) ;
#52458=CARTESIAN_POINT ( 'NONE',  ( -6.063014363552454711, -12.44085613821211389, 12.46297707981385727 ) ) ;
#52469=CARTESIAN_POINT ( 'NONE',  ( 8.471708131381630480, -12.16652409483400810, 8.774944570614499284 ) ) ;
#52489=CARTESIAN_POINT ( 'NONE',  ( 4.999999999999993783, -4.000000000000003553, 102.2532056551910387 ) ) ;
#52501=AXIS2_PLACEMENT_3D ( 'NONE', #7339, #81221, #50451 ) ;
#52515=ORIENTED_EDGE ( 'NONE', *, *, #74940, .F. ) ;
#52524=DIRECTION ( 'NONE',  ( -0.7142857142857168551, 0.6998542122237625396, 0.000000000000000000 ) ) ;
#52534=CARTESIAN_POINT ( 'NONE',  ( 3.333770628267000546, -49.25119931019934683, 44.08595898032793059 ) ) ;
#52556=CARTESIAN_POINT ( 'NONE',  ( -2.049017173238487644, -49.86226168011652504, 44.73325810198269181 ) ) ;
#52570=CIRCLE ( 'NONE', #62917, 4.000000000000003553 ) ;
#52584=ORIENTED_EDGE ( 'NONE', *, *, #11537, .T. ) ;
#52632=ORIENTED_EDGE ( 'NONE', *, *, #4582, .T. ) ;
#52640=VERTEX_POINT ( 'NONE', #17326 ) ;
#52673=SURFACE_SIDE_STYLE ('',( #29515 ) ) ;
#52686=CARTESIAN_POINT ( 'NONE',  ( 13.42019126081076941, -52.95647893691098318, 30.98765330636284077 ) ) ;
#52687=DIRECTION ( 'NONE',  ( 0.000000000000000000, 0.000000000000000000, 1.000000000000000000 ) ) ;
#52700=SURFACE_STYLE_USAGE ( .BOTH. , #93711 ) ;
#52767=( NAMED_UNIT ( * ) SI_UNIT ( $, .STERADIAN. ) SOLID_ANGLE_UNIT ( ) );
#52788=CARTESIAN_POINT ( 'NONE',  ( 5.446322446741273637, -11.07408952718074602, -10.13262891269592458 ) ) ;
#52820=STYLED_ITEM ( 'NONE', ( #72479 ), #15259 ) ;
#52824=CARTESIAN_POINT ( 'NONE',  ( 3.471301144393694749, -0.8437115307660071339, 103.7432070447316050 ) ) ;
#52839=CARTESIAN_POINT ( 'NONE',  ( -12.32676478774256523, -2.923359614653776362, 20.67314872818923988 ) ) ;
#52867=CARTESIAN_POINT ( 'NONE',  ( -1.139671569113011707, -70.62079937436291743, 13.04394488173644540 ) ) ;
#52877=CARTESIAN_POINT ( 'NONE',  ( -13.98725534264629466, -50.02704942377346953, 27.65002740835610240 ) ) ;
#52896=CARTESIAN_POINT ( 'NONE',  ( -2.100699074824130985, -0.1482055178558705777, 102.1543794502939022 ) ) ;
#52937=COLOUR_RGB ( '', 0.40784314, 0.44705882, 0.49803922) ;
#52947=DIRECTION ( 'NONE',  ( 0.000000000000000000, 1.000000000000000000, 0.000000000000000000 ) ) ;
#52956=MECHANICAL_DESIGN_GEOMETRIC_PRESENTATION_REPRESENTATION('',(#46042),#58108);
#52958=CARTESIAN_POINT ( 'NONE',  ( -1.000000000000000000, -4.607398061199006634, -14.28094137034753608 ) ) ;
#52959=CARTESIAN_POINT ( 'NONE',  ( 0.000000000000000000, -80.00000000000000000, 39.00000000000000000 ) ) ;
#52980=AXIS2_PLACEMENT_3D ( 'NONE', #45427, #29273, #54532 ) ;
#52995=( GEOMETRIC_REPRESENTATION_CONTEXT ( 3 ) GLOBAL_UNCERTAINTY_ASSIGNED_CONTEXT ( ( #45097 ) ) GLOBAL_UNIT_ASSIGNED_CONTEXT ( ( #23073, #51434, #49295 ) ) REPRESENTATION_CONTEXT ( 'NONE', 'WORKASPACE' ) );
#53003=CARTESIAN_POINT ( 'NONE',  ( -1.688865360058640741, -5.975540627551688466, -13.79722992719856123 ) ) ;
#53037=B_SPLINE_CURVE_WITH_KNOTS ( 'NONE', 3,
 ( #44303, #77198, #3310, #77739, #3849, #66993, #83681, #26046, #9787, #12446, #22171, #45374 ),
 .UNSPECIFIED., .F., .F.,
 ( 4, 2, 2, 2, 2, 4 ),
 ( 0.008226835460202822081, 0.01428459443934570333, 0.02034235341848858458, 0.03245787137677434708, 0.04457338933506011652, 0.05668890729334587902 ),
 .UNSPECIFIED. ) ;
#53039=CARTESIAN_POINT ( 'NONE',  ( 5.238409285680427629, -1.996984918271484277, 104.1169421774613681 ) ) ;
#53040=MECHANICAL_DESIGN_GEOMETRIC_PRESENTATION_REPRESENTATION('',(#82362),#42717);
#53053=COLOUR_RGB ( '', 0.66274510, 0.83137255, 0.94901961) ;
#53056=SURFACE_SIDE_STYLE ('',( #45509 ) ) ;
#53085=CARTESIAN_POINT ( 'NONE',  ( 2.992324825358647189, -53.48068721642265899, 40.67781845958850084 ) ) ;
#53104=CARTESIAN_POINT ( 'NONE',  ( -5.459621313820996136, -51.29419033140447226, 39.89514185836628712 ) ) ;
#53137=MECHANICAL_DESIGN_GEOMETRIC_PRESENTATION_REPRESENTATION('',(#1447),#11844);
#53147=( GEOMETRIC_REPRESENTATION_CONTEXT ( 3 ) GLOBAL_UNCERTAINTY_ASSIGNED_CONTEXT ( ( #99086 ) ) GLOBAL_UNIT_ASSIGNED_CONTEXT ( ( #9638, #46158, #13762 ) ) REPRESENTATION_CONTEXT ( 'NONE', 'WORKASPACE' ) );
#53167=CARTESIAN_POINT ( 'NONE',  ( 2.349637580323456376, -6.873737774778126308, -13.34209367997882900 ) ) ;
#53180=DIRECTION ( 'NONE',  ( 0.000000000000000000, 1.000000000000000000, 0.000000000000000000 ) ) ;
#53181=CARTESIAN_POINT ( 'NONE',  ( -13.60715398569422874, -56.44111117512002096, 30.29660545413128503 ) ) ;
#53182=VECTOR ( 'NONE', #40805, 1000.000000000000000 ) ;
#53185=CARTESIAN_POINT ( 'NONE',  ( 12.15800707188965113, -2.467988851150757057, 20.68556527105151943 ) ) ;
#53224=FILL_AREA_STYLE ('',( #61329 ) ) ;
#53237=CARTESIAN_POINT ( 'NONE',  ( 13.45079846400083312, -54.00000000000000711, 23.11721482942554928 ) ) ;
#53244=STYLED_ITEM ( 'NONE', ( #70779 ), #185 ) ;
#53270=SURFACE_STYLE_FILL_AREA ( #4720 ) ;
#53299=CARTESIAN_POINT ( 'NONE',  ( 4.424150818701950705, -68.80753671330023735, 13.71457674299446694 ) ) ;
#53306=CARTESIAN_POINT ( 'NONE',  ( -8.237488943525885787, -5.130131229380902269, 14.25442149443525786 ) ) ;
#53307=ORIENTED_EDGE ( 'NONE', *, *, #48632, .F. ) ;
#53309=FILL_AREA_STYLE_COLOUR ( '', #35377 ) ;
#53310=CARTESIAN_POINT ( 'NONE',  ( -2.103213117735936333, -7.611216007246521364, -13.05636887007053026 ) ) ;
#53338=CARTESIAN_POINT ( 'NONE',  ( 0.9999999999999956701, 0.000000000000000000, 42.58845726811989607 ) ) ;
#53364=( NAMED_UNIT ( * ) SI_UNIT ( $, .STERADIAN. ) SOLID_ANGLE_UNIT ( ) );
#53374=CARTESIAN_POINT ( 'NONE',  ( 3.454253436624921569, -49.15858197120396511, 103.7259032015043090 ) ) ;
#53380=CARTESIAN_POINT ( 'NONE',  ( -14.45621599724610462, 0.5024826578611153449, 14.99287714740787081 ) ) ;
#53387=B_SPLINE_CURVE_WITH_KNOTS ( 'NONE', 3,
 ( #21745, #29314, #95089, #37935, #80459, #6041, #22801, #62714 ),
 .UNSPECIFIED., .F., .F.,
 ( 4, 2, 2, 4 ),
 ( 0.000000000000000000, 0.0002399497798984991234, 0.0004798995597969982468, 0.0009597991195940054924 ),
 .UNSPECIFIED. ) ;
#53410=CARTESIAN_POINT ( 'NONE',  ( -6.691148393532302840, -12.00380193953480124, 9.409600457876113211 ) ) ;
#53414=CARTESIAN_POINT ( 'NONE',  ( 3.433099864421321978, -0.8249814671519515308, 103.8029710478607939 ) ) ;
#53419=CARTESIAN_POINT ( 'NONE',  ( -13.45079846400083490, -53.73428511282628506, 23.11721482942555284 ) ) ;
#53428=VERTEX_POINT ( 'NONE', #38324 ) ;
#53469=AXIS2_PLACEMENT_3D ( 'NONE', #55460, #47381, #54390 ) ;
#53493=CARTESIAN_POINT ( 'NONE',  ( -5.000000000000000888, -32.16754151681192297, -4.059900122541123757 ) ) ;
#53513=ORIENTED_EDGE ( 'NONE', *, *, #22767, .T. ) ;
#53516=CARTESIAN_POINT ( 'NONE',  ( -1.992238869817333669, -0.1163433470869644354, 102.1880563748278519 ) ) ;
#53521=SURFACE_STYLE_USAGE ( .BOTH. , #104180 ) ;
#53532=CARTESIAN_POINT ( 'NONE',  ( -1.574031687317222650, -6.039084736198661041, -13.77476369210226537 ) ) ;
#53560=CARTESIAN_POINT ( 'NONE',  ( 5.000000000003806733, -51.23885339962929208, 3.814018968197090853 ) ) ;
#53606=CARTESIAN_POINT ( 'NONE',  ( 1.266928293263013039, -50.00000000000000000, 44.94249618006135449 ) ) ;
#53638=CARTESIAN_POINT ( 'NONE',  ( 0.000000000000000000, -46.00000000000000000, 119.0000000000000142 ) ) ;
#53700=CARTESIAN_POINT ( 'NONE',  ( -13.99726531479253566, -57.99988801012565887, 27.38140257663831889 ) ) ;
#53711=DIRECTION ( 'NONE',  ( -0.8257009859295904031, 0.000000000000000000, 0.5641080409238132809 ) ) ;
#53714=ORIENTED_EDGE ( 'NONE', *, *, #54688, .F. ) ;
#53721=CARTESIAN_POINT ( 'NONE',  ( -1.729270706310499062, -69.60346723319459272, 12.84471657573915593 ) ) ;
#53757=SURFACE_STYLE_FILL_AREA ( #78036 ) ;
#53758=CARTESIAN_POINT ( 'NONE',  ( 5.000000000000000000, -13.79684580664352112, 10.70524563074489954 ) ) ;
#53769=( LENGTH_UNIT ( ) NAMED_UNIT ( * ) SI_UNIT ( .MILLI., .METRE. ) );
#53789=CARTESIAN_POINT ( 'NONE',  ( 0.000000000000000000, -46.00000000000000000, 112.0000000000000000 ) ) ;
#53819=CARTESIAN_POINT ( 'NONE',  ( -8.643860566174014437, -4.452774918521638980, 14.41948991096433907 ) ) ;
#53822=CARTESIAN_POINT ( 'NONE',  ( 4.245164436741635683, -48.92819220080328080, 104.4592797835102687 ) ) ;
#53823=AXIS2_PLACEMENT_3D ( 'NONE', #70729, #3344, #93951 ) ;
#53827=AXIS2_PLACEMENT_3D ( 'NONE', #18247, #90515, #32305 ) ;
#53872=FILL_AREA_STYLE_COLOUR ( '', #95582 ) ;
#53892=CARTESIAN_POINT ( 'NONE',  ( -9.397382606151760243, -3.219694582843974473, 14.78427261612472599 ) ) ;
#53909=CARTESIAN_POINT ( 'NONE',  ( -4.335182740494876619, -48.88046597750100375, 104.3855524028883792 ) ) ;
#53918=CARTESIAN_POINT ( 'NONE',  ( -5.000000000000000000, -12.42851940633630825, 8.537252933895542739 ) ) ;
#53927=CARTESIAN_POINT ( 'NONE',  ( -13.77155591953703961, -50.98632431394131714, 24.47427385584959225 ) ) ;
#53940=CARTESIAN_POINT ( 'NONE',  ( -1.901054659336256725, -69.56322987786279555, 12.86594763132180397 ) ) ;
#54031=EDGE_LOOP ( 'NONE', ( #13017, #65589, #6191, #43922, #88258, #68246 ) ) ;
#54034=CARTESIAN_POINT ( 'NONE',  ( -1.000000000000000000, -5.000000000000015099, -14.14213562373094923 ) ) ;
#54062=CARTESIAN_POINT ( 'NONE',  ( 1.000000000000000000, -56.64186896442130603, 6.232146447172338455 ) ) ;
#54087=CARTESIAN_POINT ( 'NONE',  ( -4.562211633346542783, -47.83778420154242639, 43.06387934016247243 ) ) ;
#54089=EDGE_CURVE ( 'NONE', #2153, #19188, #59165, .T. ) ;
#54127=CARTESIAN_POINT ( 'NONE',  ( -1.000000000000000000, -64.45248229066025658, 10.00070197187164389 ) ) ;
#54136=CARTESIAN_POINT ( 'NONE',  ( -4.415716460554405032, -52.49535300446108721, 40.28654576308774438 ) ) ;
#54188=FILL_AREA_STYLE_COLOUR ( '', #73731 ) ;
#54208=CARTESIAN_POINT ( 'NONE',  ( -5.683639242321874008, -47.06573826195067056, 103.9372442403038121 ) ) ;
#54230=ORIENTED_EDGE ( 'NONE', *, *, #94181, .F. ) ;
#54327=CARTESIAN_POINT ( 'NONE',  ( -5.719235665873437569, -7.817867488105560092, 13.77080619359168878 ) ) ;
#54356=CARTESIAN_POINT ( 'NONE',  ( 3.105144143682717406, -0.5701562126480363979, 103.2828762868857098 ) ) ;
#54379=DIRECTION ( 'NONE',  ( 0.4999999999999993339, 0.000000000000000000, 0.8660254037844390407 ) ) ;
#54388=SURFACE_STYLE_USAGE ( .BOTH. , #95411 ) ;
#54390=DIRECTION ( 'NONE',  ( 0.000000000000000000, 0.000000000000000000, -1.000000000000000000 ) ) ;
#54401=CARTESIAN_POINT ( 'NONE',  ( -9.784430647098096401, -3.383477514783840956, 15.02353616751815402 ) ) ;
#54430=CARTESIAN_POINT ( 'NONE',  ( -6.060168961275133270, -62.82544565322023544, 14.37957135237512674 ) ) ;
#54432=( LENGTH_UNIT ( ) NAMED_UNIT ( * ) SI_UNIT ( .MILLI., .METRE. ) );
#54436=CARTESIAN_POINT ( 'NONE',  ( 0.000000000000000000, -48.44948974278317877, 120.5000000000000000 ) ) ;
#54438=CARTESIAN_POINT ( 'NONE',  ( -13.45079846400083312, -54.00000000000000711, 23.11721482942554928 ) ) ;
#54454=( NAMED_UNIT ( * ) SI_UNIT ( $, .STERADIAN. ) SOLID_ANGLE_UNIT ( ) );
#54532=DIRECTION ( 'NONE',  ( 0.1091179629861610406, 0.9940288075069810825, 0.000000000000000000 ) ) ;
#54544=CARTESIAN_POINT ( 'NONE',  ( -3.473068986403389236, -0.8450860966016455755, 103.7454523020564920 ) ) ;
#54560=AXIS2_PLACEMENT_3D ( 'NONE', #85358, #59500, #92373 ) ;
#54607=( NAMED_UNIT ( * ) SI_UNIT ( $, .STERADIAN. ) SOLID_ANGLE_UNIT ( ) );
#54639=ORIENTED_EDGE ( 'NONE', *, *, #26635, .F. ) ;
#54665=CARTESIAN_POINT ( 'NONE',  ( -9.624613452210644127, -12.93026283660781317, 16.83029889311164240 ) ) ;
#54667=CARTESIAN_POINT ( 'NONE',  ( -2.996823056566161547, -53.47853005769305668, 40.67684663563603209 ) ) ;
#54680=( GEOMETRIC_REPRESENTATION_CONTEXT ( 3 ) GLOBAL_UNCERTAINTY_ASSIGNED_CONTEXT ( ( #5989 ) ) GLOBAL_UNIT_ASSIGNED_CONTEXT ( ( #90708, #50745, #58329 ) ) REPRESENTATION_CONTEXT ( 'NONE', 'WORKASPACE' ) );
#54686=FILL_AREA_STYLE_COLOUR ( '', #52017 ) ;
#54688=EDGE_CURVE ( 'NONE', #56644, #25211, #28233, .T. ) ;
#54701=AXIS2_PLACEMENT_3D ( 'NONE', #90550, #10156, #50596 ) ;
#54746=( LENGTH_UNIT ( ) NAMED_UNIT ( * ) SI_UNIT ( .MILLI., .METRE. ) );
#54748=COLOUR_RGB ( '', 0.40784314, 0.44705882, 0.49803922) ;
#54755=DIRECTION ( 'NONE',  ( -0.5166563581656308246, 0.4014477553983988312, -0.7562446080816809246 ) ) ;
#54802=CARTESIAN_POINT ( 'NONE',  ( 13.66195738444678831, -51.55796608476862986, 23.93843443166228724 ) ) ;
#54813=CIRCLE ( 'NONE', #47954, 2.000000000000000000 ) ;
#54818=FILL_AREA_STYLE_COLOUR ( '', #64732 ) ;
#54824=CARTESIAN_POINT ( 'NONE',  ( -1.896692290086544386, -49.86802981722174621, 102.2313487884823076 ) ) ;
#54843=CARTESIAN_POINT ( 'NONE',  ( -3.857142857142854986, -1.200583151104943846, 103.1763305333244176 ) ) ;
#54863=EDGE_CURVE ( 'NONE', #34686, #87879, #38601, .T. ) ;
#54872=CARTESIAN_POINT ( 'NONE',  ( -10.66614630375940109, -11.24660294604464461, 17.92171734272679018 ) ) ;
#54881=ORIENTED_EDGE ( 'NONE', *, *, #36673, .T. ) ;
#54882=TOROIDAL_SURFACE ( 'NONE', #106545, 11.00000000000000533, 4.000000000000000000 ) ;
#54914=CARTESIAN_POINT ( 'NONE',  ( -3.352941176470589646, -48.79941684889505638, 104.5794940929807524 ) ) ;
#54925=PRESENTATION_STYLE_ASSIGNMENT (( #22613 ) ) ;
#54944=CARTESIAN_POINT ( 'NONE',  ( -9.474490489458172959, -1.979363373267127857, 15.47598927252669654 ) ) ;
#54962=CARTESIAN_POINT ( 'NONE',  ( -4.284822031654945462, -48.90716638558773610, 104.4267991316944943 ) ) ;
#55030=CARTESIAN_POINT ( 'NONE',  ( 3.498313567329702778, -49.14282678961173900, 104.2430177423136826 ) ) ;
#55035=CARTESIAN_POINT ( 'NONE',  ( -9.901632022247257581, -50.20920921090512934, 28.42038564161779135 ) ) ;
#55053=FACE_OUTER_BOUND ( 'NONE', #72983, .T. ) ;
#55054=SURFACE_SIDE_STYLE ('',( #49083 ) ) ;
#55061=CARTESIAN_POINT ( 'NONE',  ( -5.000000000000000000, -25.25113514762997013, -2.443230580349978531 ) ) ;
#55075=EDGE_CURVE ( 'NONE', #30348, #39260, #71284, .T. ) ;
#55088=FACE_OUTER_BOUND ( 'NONE', #33844, .T. ) ;
#55111=ORIENTED_EDGE ( 'NONE', *, *, #49160, .T. ) ;
#55115=CARTESIAN_POINT ( 'NONE',  ( 13.45844644947841751, -54.52725136547403650, 23.14343646736056570 ) ) ;
#55131=DIRECTION ( 'NONE',  ( 0.000000000000000000, 0.000000000000000000, -1.000000000000000000 ) ) ;
#55189=FILL_AREA_STYLE_COLOUR ( '', #30327 ) ;
#55266=TOROIDAL_SURFACE ( 'NONE', #29462, 10.00000000000000000, 4.000000000000000000 ) ;
#55277=EDGE_LOOP ( 'NONE', ( #22426, #56607, #8984, #18402 ) ) ;
#55326=UNCERTAINTY_MEASURE_WITH_UNIT (LENGTH_MEASURE( 1.000000000000000082E-05 ), #12742, 'distance_accuracy_value', 'NONE');
#55334=EDGE_CURVE ( 'NONE', #65995, #93762, #31744, .T. ) ;
#55382=PRESENTATION_STYLE_ASSIGNMENT (( #104477 ) ) ;
#55387=FILL_AREA_STYLE ('',( #63516 ) ) ;
#55402=CARTESIAN_POINT ( 'NONE',  ( -11.87184877076866485, -7.546347915368680326, 19.57404110235124151 ) ) ;
#55433=CARTESIAN_POINT ( 'NONE',  ( 1.112351485006119578, -1.486542822431297095E-16, 101.1532825174488579 ) ) ;
#55460=CARTESIAN_POINT ( 'NONE',  ( 5.000000000000000000, 0.000000000000000000, 0.000000000000000000 ) ) ;
#55489=CIRCLE ( 'NONE', #53823, 11.00000000000000000 ) ;
#55493=CARTESIAN_POINT ( 'NONE',  ( -5.000000000000000000, -14.13517361223578916, 11.83579766571232206 ) ) ;
#55496=DIRECTION ( 'NONE',  ( 0.000000000000000000, 0.000000000000000000, 1.000000000000000000 ) ) ;
#55500=CARTESIAN_POINT ( 'NONE',  ( 30.00000000000000000, 1.347111479062088405E-15, 11.00000000000000000 ) ) ;
#55501=CARTESIAN_POINT ( 'NONE',  ( 27.99999999999999645, 0.000000000000000000, -13.00000000000000000 ) ) ;
#55521=( BOUNDED_SURFACE ( )  B_SPLINE_SURFACE ( 3, 2, ( 
 ( #39228, #71559, #54843 ),
 ( #87772, #65073, #48343 ),
 ( #89363, #81238, #97422 ),
 ( #30612, #104466, #79131 ),
 ( #88302, #79662, #14376 ),
 ( #72102, #64038, #24122 ),
 ( #7355, #96916, #105009 ),
 ( #105530, #55885, #88820 ),
 ( #71042, #73140, #47285 ),
 ( #62961, #14915, #40265 ),
 ( #95861, #106043, #80713 ),
 ( #64554, #46766, #6829 ) ),
 .UNSPECIFIED., .F., .F., .F. ) 
 B_SPLINE_SURFACE_WITH_KNOTS ( ( 4, 2, 2, 2, 2, 4 ),
 ( 3, 3 ),
 ( -3.903127820947815962E-18, 0.001187588843296127862, 0.001781383264944193853, 0.002375177686592259627, 0.003562766529888391608, 0.004750355373184523590 ),
 ( 0.000000000000000000, 1.000000000000000000 ),
 .UNSPECIFIED. ) 
 GEOMETRIC_REPRESENTATION_ITEM ( )  RATIONAL_B_SPLINE_SURFACE ( (
 ( 1.000000000000000000, 0.9359444767143314525, 1.000000000000000000),
 ( 1.000000000000000000, 0.9295581727144297535, 1.000000000000000000),
 ( 1.000000000000000000, 0.9234593375675015370, 1.000000000000000000),
 ( 1.000000000000000000, 0.9150808072273350913, 1.000000000000000000),
 ( 1.000000000000000000, 0.9124161408737702095, 1.000000000000000000),
 ( 1.000000000000000000, 0.9074047588826502642, 1.000000000000000000),
 ( 1.000000000000000000, 0.9050663310860240784, 1.000000000000000000),
 ( 1.000000000000000000, 0.8987692007139229666, 1.000000000000000000),
 ( 1.000000000000000000, 0.8954627112850603865, 1.000000000000000000),
 ( 1.000000000000000000, 0.8909338199771259514, 1.000000000000000000),
 ( 1.000000000000000000, 0.8897377579433781714, 1.000000000000000000),
 ( 1.000000000000000000, 0.8897565210026093796, 1.000000000000000000) ) ) 
 REPRESENTATION_ITEM ( '' )  SURFACE ( )  );
#55524=CARTESIAN_POINT ( 'NONE',  ( -3.352941176470582985, -48.79941684889506348, 104.5794940929807382 ) ) ;
#55602=FILL_AREA_STYLE ('',( #21707 ) ) ;
#55615=DIRECTION ( 'NONE',  ( 0.000000000000000000, -0.000000000000000000, 1.000000000000000000 ) ) ;
#55648=CARTESIAN_POINT ( 'NONE',  ( 11.36457253998776551, -9.486455709443886164, 18.81580886345433967 ) ) ;
#55668=CARTESIAN_POINT ( 'NONE',  ( -3.647056030525466674, -49.00888714197444074, 43.86785402897538688 ) ) ;
#55680=CARTESIAN_POINT ( 'NONE',  ( -9.996020202094923590, -57.99966105432783792, 27.38654800878193996 ) ) ;
#55722=CARTESIAN_POINT ( 'NONE',  ( -6.835997281635401102, -47.84397377247658767, 39.21766570620285108 ) ) ;
#55728=ADVANCED_FACE ( 'NONE', ( #40248 ), #56948, .T. ) ;
#55810=CARTESIAN_POINT ( 'NONE',  ( -2.531139591009138989, -70.38595913997060904, 13.22873017836408494 ) ) ;
#55826=STYLED_ITEM ( 'NONE', ( #76022 ), #98511 ) ;
#55842=ORIENTED_EDGE ( 'NONE', *, *, #43040, .F. ) ;
#55860=STYLED_ITEM ( 'NONE', ( #97719 ), #85645 ) ;
#55883=CARTESIAN_POINT ( 'NONE',  ( 4.919733272805031810, -1.562181361514374034, 104.2477112191710802 ) ) ;
#55885=CARTESIAN_POINT ( 'NONE',  ( -4.844458925424343754, -2.858988884355133209, 103.3760426044467380 ) ) ;
#55932=EDGE_CURVE ( 'NONE', #41710, #101089, #57386, .T. ) ;
#55941=CIRCLE ( 'NONE', #21583, 1.999999999999994227 ) ;
#55952=ORIENTED_EDGE ( 'NONE', *, *, #91607, .F. ) ;
#55970=ADVANCED_FACE ( 'NONE', ( #48202 ), #104684, .F. ) ;
#55971=CYLINDRICAL_SURFACE ( 'NONE', #13587, 4.000000000000003553 ) ;
#55972=CARTESIAN_POINT ( 'NONE',  ( 3.964299495115819916, -1.290159053846382520, 103.9028936078240832 ) ) ;
#56017=EDGE_CURVE ( 'NONE', #17242, #10104, #49761, .T. ) ;
#56023=CARTESIAN_POINT ( 'NONE',  ( -5.000000000000000000, -13.99860067247083073, 11.59399192991872596 ) ) ;
#56037=B_SPLINE_CURVE_WITH_KNOTS ( 'NONE', 3,
 ( #80710, #80182, #15451, #106586, #6289, #39226, #88819, #48870 ),
 .UNSPECIFIED., .F., .F.,
 ( 4, 2, 2, 4 ),
 ( 0.000000000000000000, 0.0002494395879357873573, 0.0004988791758715747145, 0.0009977583517431533322 ),
 .UNSPECIFIED. ) ;
#56079=CARTESIAN_POINT ( 'NONE',  ( -9.864453787710772303, -50.40643955470380178, 25.34106120123098549 ) ) ;
#56084=COLOUR_RGB ( '', 0.31764706, 0.68627451, 0.89019608) ;
#56088=CIRCLE ( 'NONE', #69925, 14.00000000000000178 ) ;
#56096=ORIENTED_EDGE ( 'NONE', *, *, #24339, .T. ) ;
#56114=VERTEX_POINT ( 'NONE', #45451 ) ;
#56168=AXIS2_PLACEMENT_3D ( 'NONE', #5000, #28247, #103688 ) ;
#56169=CARTESIAN_POINT ( 'NONE',  ( -4.073826509764605142, -1.047876529904877785, 104.5376934966490268 ) ) ;
#56176=CARTESIAN_POINT ( 'NONE',  ( 15.71253448772373673, -4.310224761972015983, 14.37944430768630255 ) ) ;
#56197=CARTESIAN_POINT ( 'NONE',  ( -4.882603763050360257, -46.97189056336372914, 42.72181775637868384 ) ) ;
#56253=ORIENTED_EDGE ( 'NONE', *, *, #83418, .T. ) ;
#56254=CARTESIAN_POINT ( 'NONE',  ( -4.644779468754994589, -47.71105737603588182, 40.40507978762116892 ) ) ;
#56269=FILL_AREA_STYLE_COLOUR ( '', #83846 ) ;
#56275=( GEOMETRIC_REPRESENTATION_CONTEXT ( 3 ) GLOBAL_UNCERTAINTY_ASSIGNED_CONTEXT ( ( #21873 ) ) GLOBAL_UNIT_ASSIGNED_CONTEXT ( ( #52105, #43497, #77458 ) ) REPRESENTATION_CONTEXT ( 'NONE', 'WORKASPACE' ) );
#56285=CARTESIAN_POINT ( 'NONE',  ( -3.040541989225158837, -0.8315988256275635981, 104.0108293352680988 ) ) ;
#56331=FILL_AREA_STYLE ('',( #45628 ) ) ;
#56349=CARTESIAN_POINT ( 'NONE',  ( -4.744147290358121438, -64.75533526552750629, 13.06247057915002863 ) ) ;
#56371=B_SPLINE_CURVE_WITH_KNOTS ( 'NONE', 3,
 ( #42347, #57993, #34295, #48825, #40751, #82269, #25684, #25134, #67169, #73638, #90913, #8911 ),
 .UNSPECIFIED., .F., .F.,
 ( 4, 2, 2, 2, 2, 4 ),
 ( 0.002780326429443416222, 0.01490779258427995906, 0.02703525873911650362, 0.03916272489395304646, 0.04522645797137132828, 0.05129019104878961011 ),
 .UNSPECIFIED. ) ;
#56441=CARTESIAN_POINT ( 'NONE',  ( 5.000000000000000888, -12.28614229754743903, 10.41767341469848951 ) ) ;
#56454=EDGE_CURVE ( 'NONE', #103713, #85095, #87041, .T. ) ;
#56456=ORIENTED_EDGE ( 'NONE', *, *, #21221, .F. ) ;
#56461=DIRECTION ( 'NONE',  ( 1.000000000000000000, 0.000000000000000000, 0.000000000000000000 ) ) ;
#56475=ADVANCED_FACE ( 'NONE', ( #85797 ), #63449, .F. ) ;
#56491=COLOUR_RGB ( '', 0.31764706, 0.68627451, 0.89019608) ;
#56495=CARTESIAN_POINT ( 'NONE',  ( -5.437321008177769421, -47.65716784822934216, 104.0362115404849845 ) ) ;
#56563=CARTESIAN_POINT ( 'NONE',  ( -5.000000000000000000, -14.90207541443127148, 12.47233211438449629 ) ) ;
#56591=DIRECTION ( 'NONE',  ( 0.000000000000000000, 0.000000000000000000, 1.000000000000000000 ) ) ;
#56602=ORIENTED_EDGE ( 'NONE', *, *, #64455, .F. ) ;
#56607=ORIENTED_EDGE ( 'NONE', *, *, #99623, .T. ) ;
#56618=( NAMED_UNIT ( * ) SI_UNIT ( $, .STERADIAN. ) SOLID_ANGLE_UNIT ( ) );
#56625=CARTESIAN_POINT ( 'NONE',  ( 9.521849859704259345, -51.55475818109406561, 23.94093251888962470 ) ) ;
#56642=CARTESIAN_POINT ( 'NONE',  ( 4.247384345738219658, -12.84326104839635896, -9.569854795092682664 ) ) ;
#56644=VERTEX_POINT ( 'NONE', #25309 ) ;
#56664=CARTESIAN_POINT ( 'NONE',  ( -30.00000000000000000, 0.000000000000000000, 0.000000000000000000 ) ) ;
#56684=CARTESIAN_POINT ( 'NONE',  ( -9.680134077953582050, 2.794975873512704378, 14.73912665704113500 ) ) ;
#56691=VERTEX_POINT ( 'NONE', #21467 ) ;
#56708=CARTESIAN_POINT ( 'NONE',  ( 13.56235479181388115, -55.77948487150412404, 23.52533112101723844 ) ) ;
#56718=CARTESIAN_POINT ( 'NONE',  ( 9.934548988108780065, -57.86759105402752823, 28.17116772486389564 ) ) ;
#56729=CARTESIAN_POINT ( 'NONE',  ( -1.545654944153988408, -49.97154544717239588, 101.5781950003720482 ) ) ;
#56753=CARTESIAN_POINT ( 'NONE',  ( -9.933368185767806224, -57.79351752493647609, 25.82212275612567964 ) ) ;
#56773=EDGE_CURVE ( 'NONE', #52640, #5765, #56088, .T. ) ;
#56819=B_SPLINE_CURVE_WITH_KNOTS ( 'NONE', 3,
 ( #20867, #68301, #3022, #35972, #3566, #93101, #101720, #35429, #36503, #102790, #11633, #44565, #44019, #101195, #52100, #94718, #27354, #53700, #61275, #86632, #60232, #100650, #85010, #51568, #76368, #11094, #53181, #86098, #69369, #68843, #60754, #12696, #12169, #102251 ),
 .UNSPECIFIED., .F., .F.,
 ( 4, 2, 2, 2, 2, 2, 2, 2, 2, 2, 2, 2, 2, 2, 2, 2, 4 ),
 ( 0.000000000000000000, 0.0007857361314144349846, 0.001571472262828869969, 0.002357208394243305062, 0.003142944525657739938, 0.003928680657072174814, 0.004714416788486610124, 0.005500152919901044567, 0.006285889051315479877, 0.007071625182729915186, 0.007857361314144349629, 0.008643097445558784939, 0.009428833576973220248, 0.01021456970838765556, 0.01100030583980208913, 0.01178604197121652444, 0.01257177810263095975 ),
 .UNSPECIFIED. ) ;
#56823=MECHANICAL_DESIGN_GEOMETRIC_PRESENTATION_REPRESENTATION('',(#93032),#98182);
#56863=DIRECTION ( 'NONE',  ( 0.000000000000000000, 1.000000000000000000, 0.000000000000000000 ) ) ;
#56885=CARTESIAN_POINT ( 'NONE',  ( -3.693992608460733074, -68.08033126016331948, 13.10824594383253050 ) ) ;
#56912=DIRECTION ( 'NONE',  ( 1.096832036894112098E-16, -0.000000000000000000, 1.000000000000000000 ) ) ;
#56931=UNCERTAINTY_MEASURE_WITH_UNIT (LENGTH_MEASURE( 1.000000000000000082E-05 ), #49252, 'distance_accuracy_value', 'NONE');
#56939=CARTESIAN_POINT ( 'NONE',  ( 8.091997990208083635, -14.49474307880116086, 15.56218444166430892 ) ) ;
#56943=CARTESIAN_POINT ( 'NONE',  ( 4.999999999999524825, -61.74609737454713354, 12.75775085714972690 ) ) ;
#56948=PLANE ( 'NONE',  #52501 ) ;
#56966=UNCERTAINTY_MEASURE_WITH_UNIT (LENGTH_MEASURE( 1.000000000000000082E-05 ), #69042, 'distance_accuracy_value', 'NONE');
#57010=ORIENTED_EDGE ( 'NONE', *, *, #49451, .T. ) ;
#57018=ORIENTED_EDGE ( 'NONE', *, *, #37366, .T. ) ;
#57026=CARTESIAN_POINT ( 'NONE',  ( -4.902312018371808300, -46.91782384206801737, 103.3400275729950550 ) ) ;
#57032=CARTESIAN_POINT ( 'NONE',  ( 1.461497756933666903, -49.97255764215042717, 101.6363431123547798 ) ) ;
#57033=DIRECTION ( 'NONE',  ( 0.000000000000000000, 0.000000000000000000, 1.000000000000000000 ) ) ;
#57067=( LENGTH_UNIT ( ) NAMED_UNIT ( * ) SI_UNIT ( .MILLI., .METRE. ) );
#57070=CARTESIAN_POINT ( 'NONE',  ( -6.419907845689960091, -0.01065582494818990457, 18.86296154573671657 ) ) ;
#57097=CARTESIAN_POINT ( 'NONE',  ( -6.249254171365509869, -12.00724809824330386, 11.39149369527972766 ) ) ;
#57123=ADVANCED_FACE ( 'NONE', ( #44949 ), #23518, .F. ) ;
#57149=CARTESIAN_POINT ( 'NONE',  ( 2.727075792294463508, -69.18208090123930276, 12.97754602523916212 ) ) ;
#57183=CARTESIAN_POINT ( 'NONE',  ( -4.571008445750556426, -47.80671748343184646, 102.5889671997070991 ) ) ;
#57188=CARTESIAN_POINT ( 'NONE',  ( 4.392764327028893412, -1.139124805377877303, 104.3925874334283037 ) ) ;
#57193=STYLED_ITEM ( 'NONE', ( #52407 ), #51679 ) ;
#57200=STYLED_ITEM ( 'NONE', ( #85975 ), #20774 ) ;
#57210=CARTESIAN_POINT ( 'NONE',  ( -8.833736740224848560, 2.942687158940284764, 14.70881556658443756 ) ) ;
#57220=( GEOMETRIC_REPRESENTATION_CONTEXT ( 3 ) GLOBAL_UNCERTAINTY_ASSIGNED_CONTEXT ( ( #75515 ) ) GLOBAL_UNIT_ASSIGNED_CONTEXT ( ( #72696, #6898, #99084 ) ) REPRESENTATION_CONTEXT ( 'NONE', 'WORKASPACE' ) );
#57222=EDGE_CURVE ( 'NONE', #57919, #97345, #53387, .T. ) ;
#57238=VERTEX_POINT ( 'NONE', #13068 ) ;
#57244=CARTESIAN_POINT ( 'NONE',  ( 9.771873710511815858, -57.46329652640150698, 29.13520411490522122 ) ) ;
#57250=CARTESIAN_POINT ( 'NONE',  ( 1.000000000000000000, -4.607437535715904531, -14.28092741399824384 ) ) ;
#57252=CARTESIAN_POINT ( 'NONE',  ( 13.71723496859481983, -8.874210861067291845, 12.10439619743532624 ) ) ;
#57274=CARTESIAN_POINT ( 'NONE',  ( -1.955013656259688704, -53.86110022085453863, 40.86468968543578484 ) ) ;
#57281=CARTESIAN_POINT ( 'NONE',  ( -9.981919929974880645, -57.97247446290226947, 27.65434374221348435 ) ) ;
#57293=CARTESIAN_POINT ( 'NONE',  ( 4.999999999999996447, -3.723962137281043638, 102.2532056551910529 ) ) ;
#57339=CYLINDRICAL_SURFACE ( 'NONE', #18431, 4.000000000000000000 ) ;
#57349=FILL_AREA_STYLE_COLOUR ( '', #81731 ) ;
#57368=DIRECTION ( 'NONE',  ( 0.000000000000000000, 1.000000000000000000, 0.000000000000000000 ) ) ;
#57386=B_SPLINE_CURVE_WITH_KNOTS ( 'NONE', 3,
 ( #65991, #24512, #73534, #91348, #64934, #83233, #33122, #81616, #15314, #25579 ),
 .UNSPECIFIED., .F., .F.,
 ( 4, 2, 2, 2, 4 ),
 ( 1.748223473168675632E-18, 0.0008022363492415249221, 0.001604472698483048109, 0.002406709047724571188, 0.003208945396966094484 ),
 .UNSPECIFIED. ) ;
#57395=FILL_AREA_STYLE_COLOUR ( '', #10736 ) ;
#57407=ORIENTED_EDGE ( 'NONE', *, *, #72017, .T. ) ;
#57420=CARTESIAN_POINT ( 'NONE',  ( 9.215420734788356327, -54.00000000000000000, 23.11721482942554928 ) ) ;
#57429=FILL_AREA_STYLE_COLOUR ( '', #15379 ) ;
#57468=ORIENTED_EDGE ( 'NONE', *, *, #94659, .T. ) ;
#57474=CARTESIAN_POINT ( 'NONE',  ( 4.962386525749626465, -62.75672373854419561, 12.88232180906529223 ) ) ;
#57480=CARTESIAN_POINT ( 'NONE',  ( 4.861072549008417454, -47.07915654916947545, 102.3606070684416807 ) ) ;
#57481=EDGE_CURVE ( 'NONE', #97430, #5281, #102706, .T. ) ;
#57505=CARTESIAN_POINT ( 'NONE',  ( 5.000000000000000000, -13.83542193917754126, 11.07282995724436780 ) ) ;
#57525=CARTESIAN_POINT ( 'NONE',  ( 4.869065774733604357, -47.04879514974216903, 102.3543991519893979 ) ) ;
#57568=FACE_OUTER_BOUND ( 'NONE', #89711, .T. ) ;
#57581=CARTESIAN_POINT ( 'NONE',  ( 3.668277386370350612, -48.89637005407674053, 104.6014336420241051 ) ) ;
#57607=EDGE_LOOP ( 'NONE', ( #21998, #42987, #79402, #4942 ) ) ;
#57615=VERTEX_POINT ( 'NONE', #40357 ) ;
#57619=CARTESIAN_POINT ( 'NONE',  ( -6.282481257750798243, -11.96849729169379906, 11.22390784433505218 ) ) ;
#57635=B_SPLINE_CURVE_WITH_KNOTS ( 'NONE', 3,
 ( #12087, #35888, #28867, #27804 ),
 .UNSPECIFIED., .F., .F.,
 ( 4, 4 ),
 ( 0.0008765341530664233537, 0.001750917060903518828 ),
 .UNSPECIFIED. ) ;
#57643=CARTESIAN_POINT ( 'NONE',  ( 14.83341732121158074, 0.1101086422626733341, 15.00090745772169498 ) ) ;
#57673=CARTESIAN_POINT ( 'NONE',  ( 3.073649067497001841, -68.88943550113336300, 13.02707457859375495 ) ) ;
#57689=DIRECTION ( 'NONE',  ( 0.000000000000000000, 0.8363101477004194484, -0.5482566341170006519 ) ) ;
#57694=CARTESIAN_POINT ( 'NONE',  ( 4.948897892503503648, -15.25620861757297853, -6.941426030570269745 ) ) ;
#57769=SURFACE_STYLE_USAGE ( .BOTH. , #16261 ) ;
#57776=SURFACE_SIDE_STYLE ('',( #89639 ) ) ;
#57789=CARTESIAN_POINT ( 'NONE',  ( -0.9999999999999941158, -50.00000000000000000, 101.0455488498966758 ) ) ;
#57810=CARTESIAN_POINT ( 'NONE',  ( -1.017643907183658269, -54.00000000000000711, 40.96503185701687499 ) ) ;
#57867=DIRECTION ( 'NONE',  ( 0.000000000000000000, 1.000000000000000000, -1.224646799147353207E-16 ) ) ;
#57875=SURFACE_SIDE_STYLE ('',( #65458 ) ) ;
#57886=CARTESIAN_POINT ( 'NONE',  ( -5.446322446741861611, -11.07408952718066075, -10.13262891269602228 ) ) ;
#57919=VERTEX_POINT ( 'NONE', #53374 ) ;
#57938=CARTESIAN_POINT ( 'NONE',  ( -15.91602873225749981, -2.171392360670797217, 14.84268258422452291 ) ) ;
#57944=ORIENTED_EDGE ( 'NONE', *, *, #1204, .T. ) ;
#57951=CARTESIAN_POINT ( 'NONE',  ( -5.876235947983078134, -64.54950742897155180, 14.29271017806149047 ) ) ;
#57993=CARTESIAN_POINT ( 'NONE',  ( -5.000000000000000000, -19.72303380912273951, -4.527417031999413588 ) ) ;
#58005=CIRCLE ( 'NONE', #33959, 9.999999999999994671 ) ;
#58009=CARTESIAN_POINT ( 'NONE',  ( 7.157676179766298219, -15.10646866768545138, 14.96459782267552718 ) ) ;
#58012=CARTESIAN_POINT ( 'NONE',  ( 4.691239167085950790, -66.59475614380380648, 13.79106926437629355 ) ) ;
#58030=AXIS2_PLACEMENT_3D ( 'NONE', #8521, #41424, #81863 ) ;
#58033=ADVANCED_FACE ( 'NONE', ( #40362 ), #48965, .F. ) ;
#58044=ORIENTED_EDGE ( 'NONE', *, *, #92025, .T. ) ;
#58046=CARTESIAN_POINT ( 'NONE',  ( 5.000000000000000000, -13.99860067247109896, 11.59399192991907057 ) ) ;
#58061=( LENGTH_UNIT ( ) NAMED_UNIT ( * ) SI_UNIT ( .MILLI., .METRE. ) );
#58066=CARTESIAN_POINT ( 'NONE',  ( 4.188755055078837941, -48.42812442300451892, 102.8981131900555113 ) ) ;
#58084=AXIS2_PLACEMENT_3D ( 'NONE', #75026, #26021, #91771 ) ;
#58098=CARTESIAN_POINT ( 'NONE',  ( -4.999999999999993783, -45.99999999999999289, 103.2791840072761858 ) ) ;
#58108=( GEOMETRIC_REPRESENTATION_CONTEXT ( 3 ) GLOBAL_UNCERTAINTY_ASSIGNED_CONTEXT ( ( #14621 ) ) GLOBAL_UNIT_ASSIGNED_CONTEXT ( ( #9866, #83758, #19084 ) ) REPRESENTATION_CONTEXT ( 'NONE', 'WORKASPACE' ) );
#58117=SURFACE_STYLE_USAGE ( .BOTH. , #72706 ) ;
#58151=( GEOMETRIC_REPRESENTATION_CONTEXT ( 3 ) GLOBAL_UNCERTAINTY_ASSIGNED_CONTEXT ( ( #23269 ) ) GLOBAL_UNIT_ASSIGNED_CONTEXT ( ( #62595, #79290, #54454 ) ) REPRESENTATION_CONTEXT ( 'NONE', 'WORKASPACE' ) );
#58165=ORIENTED_EDGE ( 'NONE', *, *, #80520, .F. ) ;
#58192=CARTESIAN_POINT ( 'NONE',  ( 9.518831299010095393, -3.343618015359576479, 14.84779095168542185 ) ) ;
#58205=CIRCLE ( 'NONE', #52980, 1.999999999999995781 ) ;
#58228=CARTESIAN_POINT ( 'NONE',  ( 9.215420734788352775, -53.73264731217665968, 23.11721482942554928 ) ) ;
#58242=CARTESIAN_POINT ( 'NONE',  ( 4.744389013293887736, -48.62707453416835790, 104.3204960233004357 ) ) ;
#58248=SURFACE_STYLE_FILL_AREA ( #59328 ) ;
#58253=CARTESIAN_POINT ( 'NONE',  ( -12.41646176392127465, -3.622442468400648430, 20.56049830252581856 ) ) ;
#58257=AXIS2_PLACEMENT_3D ( 'NONE', #47941, #63639, #55496 ) ;
#58289=( NAMED_UNIT ( * ) SI_UNIT ( $, .STERADIAN. ) SOLID_ANGLE_UNIT ( ) );
#58321=PRESENTATION_STYLE_ASSIGNMENT (( #57769 ) ) ;
#58322=EDGE_CURVE ( 'NONE', #90150, #27782, #98264, .T. ) ;
#58329=( NAMED_UNIT ( * ) SI_UNIT ( $, .STERADIAN. ) SOLID_ANGLE_UNIT ( ) );
#58334=CARTESIAN_POINT ( 'NONE',  ( 8.456527595092419247, -14.17828489812255555, 15.83957000666675441 ) ) ;
#58338=CARTESIAN_POINT ( 'NONE',  ( -2.679344702993184058, -49.64160073592847056, 103.0669469697010783 ) ) ;
#58359=CARTESIAN_POINT ( 'NONE',  ( -2.625313013168337761, -53.64477807593443259, 40.75338374577381728 ) ) ;
#58386=PRESENTATION_STYLE_ASSIGNMENT (( #67555 ) ) ;
#58398=FILL_AREA_STYLE ('',( #25539 ) ) ;
#58421=ADVANCED_FACE ( 'NONE', ( #102323 ), #18417, .T. ) ;
#58422=CARTESIAN_POINT ( 'NONE',  ( -27.99999999999999645, 1.592040838891559095E-15, 13.00000000000000000 ) ) ;
#58437=SURFACE_STYLE_USAGE ( .BOTH. , #49261 ) ;
#58440=CARTESIAN_POINT ( 'NONE',  ( -4.999999999999999112, -14.05766640829038572, -5.232782735144287933 ) ) ;
#58443=CARTESIAN_POINT ( 'NONE',  ( -14.85442893618376203, -6.964787325848677213, 13.28843411678688824 ) ) ;
#58474=( NAMED_UNIT ( * ) SI_UNIT ( $, .STERADIAN. ) SOLID_ANGLE_UNIT ( ) );
#58487=PLANE ( 'NONE',  #79040 ) ;
#58494=SURFACE_STYLE_USAGE ( .BOTH. , #25632 ) ;
#58523=FILL_AREA_STYLE_COLOUR ( '', #53053 ) ;
#58564=CIRCLE ( 'NONE', #77508, 8.142857142857131691 ) ;
#58569=CARTESIAN_POINT ( 'NONE',  ( 9.632588565166363637, -12.91979337038410236, 16.83785788650996906 ) ) ;
#58574=CARTESIAN_POINT ( 'NONE',  ( 4.818407882770804562, -68.11195407130082913, 13.85475016061880815 ) ) ;
#58620=SURFACE_STYLE_USAGE ( .BOTH. , #1950 ) ;
#58627=EDGE_CURVE ( 'NONE', #50280, #85444, #70213, .T. ) ;
#58630=AXIS2_PLACEMENT_3D ( 'NONE', #28279, #11504, #84885 ) ;
#58662=VECTOR ( 'NONE', #67440, 1000.000000000000000 ) ;
#58677=( GEOMETRIC_REPRESENTATION_CONTEXT ( 3 ) GLOBAL_UNCERTAINTY_ASSIGNED_CONTEXT ( ( #38341 ) ) GLOBAL_UNIT_ASSIGNED_CONTEXT ( ( #10449, #51968, #34772 ) ) REPRESENTATION_CONTEXT ( 'NONE', 'WORKASPACE' ) );
#58744=CARTESIAN_POINT ( 'NONE',  ( 11.08738460869479425, -1.234896052969738811, 20.41726963649704985 ) ) ;
#58756=CIRCLE ( 'NONE', #62157, 9.000000000000000000 ) ;
#58772=SURFACE_STYLE_FILL_AREA ( #99747 ) ;
#58780=FILL_AREA_STYLE_COLOUR ( '', #63479 ) ;
#58802=DIRECTION ( 'NONE',  ( 1.096832036894112098E-16, 0.000000000000000000, 1.000000000000000000 ) ) ;
#58832=CARTESIAN_POINT ( 'NONE',  ( 27.99999999999999645, 0.000000000000000000, 0.000000000000000000 ) ) ;
#58840=CARTESIAN_POINT ( 'NONE',  ( -4.441657994893222217, -48.84245552582405736, 104.3851447015591418 ) ) ;
#58859=CARTESIAN_POINT ( 'NONE',  ( -13.83893552277105776, -50.53287629637878098, 29.12875707416400317 ) ) ;
#58860=CARTESIAN_POINT ( 'NONE',  ( -5.000000000000000000, -13.90189243245667683, 9.982568754601910399 ) ) ;
#58876=CARTESIAN_POINT ( 'NONE',  ( -3.096827034336463669, -0.5867034388794662991, 103.2812265879066729 ) ) ;
#58885=CARTESIAN_POINT ( 'NONE',  ( 10.09816733998641780, -12.27101698752137260, 17.29391650327562857 ) ) ;
#58889=SURFACE_STYLE_USAGE ( .BOTH. , #41628 ) ;
#58953=ORIENTED_EDGE ( 'NONE', *, *, #42951, .F. ) ;
#58971=ORIENTED_EDGE ( 'NONE', *, *, #14482, .T. ) ;
#58976=CARTESIAN_POINT ( 'NONE',  ( 4.195612334302333046, -1.058759987296113314, 104.4881327927231922 ) ) ;
#58978=CARTESIAN_POINT ( 'NONE',  ( -3.717184411740621197, -9.782292260249612070, -11.42823731287377242 ) ) ;
#58980=DIRECTION ( 'NONE',  ( 0.000000000000000000, 1.000000000000000000, 0.000000000000000000 ) ) ;
#58982=CARTESIAN_POINT ( 'NONE',  ( 3.415272474501187094, -0.8295767683060059072, 103.8818886975935385 ) ) ;
#59009=CARTESIAN_POINT ( 'NONE',  ( -3.626288723284335713, -48.95575889185635532, 104.3502830461760453 ) ) ;
#59043=CARTESIAN_POINT ( 'NONE',  ( -5.285714285714286476, 0.1991252733425830368, 103.1763305333244318 ) ) ;
#59050=( NAMED_UNIT ( * ) PLANE_ANGLE_UNIT ( ) SI_UNIT ( $, .RADIAN. ) );
#59105=CARTESIAN_POINT ( 'NONE',  ( 5.125760364506777300, -62.79129649437295058, 13.92958920382542232 ) ) ;
#59125=UNCERTAINTY_MEASURE_WITH_UNIT (LENGTH_MEASURE( 1.000000000000000082E-05 ), #25521, 'distance_accuracy_value', 'NONE');
#59131=ADVANCED_FACE ( 'NONE', ( #38933 ), #96103, .F. ) ;
#59133=CARTESIAN_POINT ( 'NONE',  ( 5.977446511978467214, -14.23238268869237544, 14.05797248975824409 ) ) ;
#59165=B_SPLINE_CURVE_WITH_KNOTS ( 'NONE', 3,
 ( #38204, #79683, #61942, #93756, #37143, #61401, #5794, #38715, #94293, #20458, #53299, #102909, #62456, #94835, #63523, #14397, #49431, #31176, #80204, #64578 ),
 .UNSPECIFIED., .F., .F.,
 ( 4, 2, 2, 2, 2, 2, 2, 2, 2, 4 ),
 ( 0.000000000000000000, 0.0008044152215796346881, 0.001608830443159269376, 0.002413245664738903739, 0.003217660886318538752, 0.004826491329477807478, 0.006435321772637075770, 0.008044152215796343194, 0.009652982658955611486, 0.01287064354527419144 ),
 .UNSPECIFIED. ) ;
#59174=FACE_OUTER_BOUND ( 'NONE', #32535, .T. ) ;
#59196=( NAMED_UNIT ( * ) PLANE_ANGLE_UNIT ( ) SI_UNIT ( $, .RADIAN. ) );
#59198=AXIS2_PLACEMENT_3D ( 'NONE', #34544, #83060, #1036 ) ;
#59207=DIRECTION ( 'NONE',  ( 0.000000000000000000, 0.000000000000000000, 1.000000000000000000 ) ) ;
#59247=CARTESIAN_POINT ( 'NONE',  ( -4.147911490760923137, -1.050630162886936780, 104.5115833471886191 ) ) ;
#59260=CIRCLE ( 'NONE', #45493, 2.000000000000000000 ) ;
#59275=CARTESIAN_POINT ( 'NONE',  ( 11.22451676794676168, -1.339060030482434271, 20.46088173027341028 ) ) ;
#59304=CARTESIAN_POINT ( 'NONE',  ( 5.000000000000000888, -14.05766640829038394, -5.232782735144291486 ) ) ;
#59328=FILL_AREA_STYLE ('',( #1589 ) ) ;
#59334=EDGE_CURVE ( 'NONE', #65995, #51662, #22516, .T. ) ;
#59349=CARTESIAN_POINT ( 'NONE',  ( -1.000000000000002442, 0.000000000000000000, 27.00000000000000000 ) ) ;
#59357=CARTESIAN_POINT ( 'NONE',  ( -12.37144696128342147, -4.000000000000002665, 20.44658103856077602 ) ) ;
#59364=CARTESIAN_POINT ( 'NONE',  ( 0.000000000000000000, -1.200583151104947843, 120.8571428571428612 ) ) ;
#59383=VECTOR ( 'NONE', #83830, 1000.000000000000000 ) ;
#59393=CARTESIAN_POINT ( 'NONE',  ( -13.42014116845449934, -52.95667802455457718, 30.98782490008220236 ) ) ;
#59394=CARTESIAN_POINT ( 'NONE',  ( -4.999999999999999112, -15.43654613828065969, 12.61250543006183378 ) ) ;
#59417=PRESENTATION_STYLE_ASSIGNMENT (( #3291 ) ) ;
#59444=CARTESIAN_POINT ( 'NONE',  ( 3.301573598373775287, -49.28812056075076953, 103.9445864789744149 ) ) ;
#59470=DIRECTION ( 'NONE',  ( 1.000000000000000000, 0.000000000000000000, 0.000000000000000000 ) ) ;
#59477=DIRECTION ( 'NONE',  ( 0.000000000000000000, 1.000000000000000000, 0.000000000000000000 ) ) ;
#59500=DIRECTION ( 'NONE',  ( 0.000000000000000000, 1.000000000000000000, 0.000000000000000000 ) ) ;
#59507=CARTESIAN_POINT ( 'NONE',  ( 3.369683342533197123, -0.9132179776671599525, 104.1613013819149245 ) ) ;
#59512=CARTESIAN_POINT ( 'NONE',  ( -9.858452382526078139, -11.68277816304066796, 9.415667523937807815 ) ) ;
#59513=CARTESIAN_POINT ( 'NONE',  ( -6.224163897435901482, -12.02839407259639870, 11.51386142893533560 ) ) ;
#59529=CARTESIAN_POINT ( 'NONE',  ( 14.73587750591858736, -7.217011146677200450, 13.15299077803314809 ) ) ;
#59546=UNCERTAINTY_MEASURE_WITH_UNIT (LENGTH_MEASURE( 1.000000000000000082E-05 ), #77584, 'distance_accuracy_value', 'NONE');
#59548=CARTESIAN_POINT ( 'NONE',  ( 4.642888266381937967, -2.342832151813803332, 102.5319024079573751 ) ) ;
#59567=AXIS2_PLACEMENT_3D ( 'NONE', #21050, #11831, #60424 ) ;
#59589=EDGE_CURVE ( 'NONE', #10296, #101939, #13717, .T. ) ;
#59591=CARTESIAN_POINT ( 'NONE',  ( 4.571169277359397043, -52.34660364318141035, 40.23372900632212890 ) ) ;
#59647=ADVANCED_FACE ( 'NONE', ( #45585 ), #5117, .T. ) ;
#59666=CARTESIAN_POINT ( 'NONE',  ( 5.000000000000000000, -14.13517361223990498, 11.83579766570910508 ) ) ;
#59687=CARTESIAN_POINT ( 'NONE',  ( 5.385673916453011856, 0.000000000000000000, 18.57417562100670949 ) ) ;
#59688=ORIENTED_EDGE ( 'NONE', *, *, #56017, .F. ) ;
#59694=MECHANICAL_DESIGN_GEOMETRIC_PRESENTATION_REPRESENTATION('',(#52820),#37382);
#59765=MECHANICAL_DESIGN_GEOMETRIC_PRESENTATION_REPRESENTATION('',(#78749),#21907);
#59779=DIRECTION ( 'NONE',  ( 1.000000000000000000, 0.000000000000000000, 0.000000000000000000 ) ) ;
#59809=CARTESIAN_POINT ( 'NONE',  ( 9.918658701378005205, -2.743202263443990763, 15.35583465422220861 ) ) ;
#59815=FILL_AREA_STYLE ('',( #53309 ) ) ;
#59826=CIRCLE ( 'NONE', #30574, 3.999999999999999112 ) ;
#59831=ADVANCED_FACE ( 'NONE', ( #34191 ), #41984, .F. ) ;
#59837=AXIS2_PLACEMENT_3D ( 'NONE', #13518, #14574, #5961 ) ;
#59858=CYLINDRICAL_SURFACE ( 'NONE', #48981, 9.999999999999998224 ) ;
#59870=DIRECTION ( 'NONE',  ( 0.000000000000000000, 1.000000000000000000, 0.000000000000000000 ) ) ;
#59889=ORIENTED_EDGE ( 'NONE', *, *, #105393, .T. ) ;
#59903=ORIENTED_EDGE ( 'NONE', *, *, #82380, .F. ) ;
#59910=FILL_AREA_STYLE_COLOUR ( '', #25687 ) ;
#59920=B_SPLINE_CURVE_WITH_KNOTS ( 'NONE', 3,
 ( #86555, #12613, #4544, #54127, #87070, #105363, #6119, #48695, #88645, #47109, #22880, #16342, #72455, #32021, #31503, #14737 ),
 .UNSPECIFIED., .F., .F.,
 ( 4, 2, 2, 2, 2, 2, 2, 4 ),
 ( 0.0004635561819301090036, 0.004837973112655610287, 0.009212390043381110324, 0.01796122390483211387, 0.02671005776628311568, 0.03545889162773411402, 0.05295655935063611763, 0.07045422707353812819 ),
 .UNSPECIFIED. ) ;
#59946=DIRECTION ( 'NONE',  ( 1.000000000000000000, 0.000000000000000000, 0.000000000000000000 ) ) ;
#59952=CARTESIAN_POINT ( 'NONE',  ( -4.003587701499479401, -1.050376533302832094, 104.5574048719304443 ) ) ;
#59959=CARTESIAN_POINT ( 'NONE',  ( 10.05948821411846872, -11.59943296283969971, 9.519649634508279945 ) ) ;
#59989=CARTESIAN_POINT ( 'NONE',  ( 0.9999999999999940048, -50.00000000000000000, 101.0455488498966758 ) ) ;
#59994=CYLINDRICAL_SURFACE ( 'NONE', #49403, 9.999999999999994671 ) ;
#60049=FACE_OUTER_BOUND ( 'NONE', #18571, .T. ) ;
#60074=CARTESIAN_POINT ( 'NONE',  ( 15.90614609307868399, -3.157894736842107530, 14.66382285868950675 ) ) ;
#60078=DIRECTION ( 'NONE',  ( 1.000000000000000000, 0.000000000000000000, 0.000000000000000000 ) ) ;
#60093=CARTESIAN_POINT ( 'NONE',  ( 4.902312018372324331, -3.082176157930677451, 103.3400275729950835 ) ) ;
#60095=CARTESIAN_POINT ( 'NONE',  ( -3.685905252139206834, -48.95891067205180747, 104.2837900504744368 ) ) ;
#60142=CARTESIAN_POINT ( 'NONE',  ( 3.116130668582941965, -49.50076467470627506, 40.80225857358325925 ) ) ;
#60187=CARTESIAN_POINT ( 'NONE',  ( -1.450084842030770593, -49.97618070428583081, 101.4852282631765661 ) ) ;
#60232=CARTESIAN_POINT ( 'NONE',  ( -13.93078765908243710, -57.79386853345808106, 28.41172023899451560 ) ) ;
#60285=CIRCLE ( 'NONE', #86073, 13.00000000000000000 ) ;
#60298=CARTESIAN_POINT ( 'NONE',  ( 6.474469369223094795, -49.25375315074590787, 39.41384094684381267 ) ) ;
#60306=CARTESIAN_POINT ( 'NONE',  ( -4.999999999999993783, -4.000000000000003553, 102.2532056551910387 ) ) ;
#60322=( NAMED_UNIT ( * ) PLANE_ANGLE_UNIT ( ) SI_UNIT ( $, .RADIAN. ) );
#60354=CARTESIAN_POINT ( 'NONE',  ( -6.903421418544427368, -12.56552240113756014, 8.191925706847577260 ) ) ;
#60379=CARTESIAN_POINT ( 'NONE',  ( 1.000000000000000000, -5.000000000000018652, -14.14213562373094568 ) ) ;
#60407=DIRECTION ( 'NONE',  ( 0.000000000000000000, 1.000000000000000000, 0.000000000000000000 ) ) ;
#60424=DIRECTION ( 'NONE',  ( 0.000000000000000000, 0.000000000000000000, -1.000000000000000000 ) ) ;
#60434=ADVANCED_FACE ( 'NONE', ( #29183 ), #47855, .T. ) ;
#60441=CIRCLE ( 'NONE', #63826, 14.00000000000000178 ) ;
#60459=CARTESIAN_POINT ( 'NONE',  ( -4.391938347788321373, -1.138802597855428589, 104.3926446507461065 ) ) ;
#60464=( LENGTH_UNIT ( ) NAMED_UNIT ( * ) SI_UNIT ( .MILLI., .METRE. ) );
#60470=CARTESIAN_POINT ( 'NONE',  ( -13.44292909870241459, -52.70664433108516533, 30.91132584605806244 ) ) ;
#60485=CARTESIAN_POINT ( 'NONE',  ( -3.883877898720556665, -1.065320993063029631, 104.5781496044265424 ) ) ;
#60489=CYLINDRICAL_SURFACE ( 'NONE', #42605, 2.000000000000000000 ) ;
#60500=CARTESIAN_POINT ( 'NONE',  ( -5.000000000000000000, -15.62228920881133298, 12.61250543006184088 ) ) ;
#60515=CARTESIAN_POINT ( 'NONE',  ( 2.893255198029168973, -49.53525371043113523, 103.3592142771324518 ) ) ;
#60527=SURFACE_STYLE_FILL_AREA ( #42186 ) ;
#60539=CARTESIAN_POINT ( 'NONE',  ( 8.644795791334905388, -0.2475540741395084177, 19.58096426192390638 ) ) ;
#60543=SURFACE_STYLE_FILL_AREA ( #58398 ) ;
#60580=CARTESIAN_POINT ( 'NONE',  ( 3.352941176471716744, -1.200583151107622815, 104.5794940929782797 ) ) ;
#60603=( NAMED_UNIT ( * ) SI_UNIT ( $, .STERADIAN. ) SOLID_ANGLE_UNIT ( ) );
#60611=( BOUNDED_SURFACE ( )  B_SPLINE_SURFACE ( 3, 2, ( 
 ( #30907, #22811, #105292 ),
 ( #45487, #38978, #14663 ),
 ( #4478, #88058, #80469 ),
 ( #63788, #70280, #103700 ),
 ( #95612, #5013, #71851 ),
 ( #6580, #104757, #13610 ),
 ( #54062, #39513, #72387 ),
 ( #97189, #53560, #46524 ),
 ( #103179, #87007, #13078 ),
 ( #46007, #37947, #70806 ),
 ( #5533, #38459, #104219 ),
 ( #54, #24928, #64835 ),
 ( #82610, #31953, #17364 ),
 ( #98258, #73972, #23333 ),
 ( #1125, #89115, #34099 ),
 ( #57250, #99303, #50237 ) ),
 .UNSPECIFIED., .F., .F., .T. ) 
 B_SPLINE_SURFACE_WITH_KNOTS ( ( 4, 2, 2, 2, 2, 2, 2, 4 ),
 ( 3, 3 ),
 ( -2.388584351323025812E-05, 0.004361143453687739771, 0.008746172750888710559, 0.01751623134529065040, 0.02628628993969259198, 0.03505634853409453355, 0.05259646572289841671, 0.07013658291170229986 ),
 ( 0.000000000000000000, 1.000000000000000000 ),
 .UNSPECIFIED. ) 
 GEOMETRIC_REPRESENTATION_ITEM ( )  RATIONAL_B_SPLINE_SURFACE ( (
 ( 1.000000000000000000, 0.7071067811865475727, 1.000000000000000000),
 ( 1.000000000000000000, 0.7071067811865475727, 1.000000000000000000),
 ( 1.000000000000000000, 0.7071067811865475727, 1.000000000000000000),
 ( 1.000000000000000000, 0.7071067811865475727, 1.000000000000000000),
 ( 1.000000000000000000, 0.7071067811865475727, 1.000000000000000000),
 ( 1.000000000000000000, 0.7071067811865475727, 1.000000000000000000),
 ( 1.000000000000000000, 0.7071067811865473507, 1.000000000000000000),
 ( 1.000000000000000000, 0.7071067811865473507, 1.000000000000000000),
 ( 1.000000000000000000, 0.7071067811865475727, 1.000000000000000000),
 ( 1.000000000000000000, 0.7071067811865475727, 1.000000000000000000),
 ( 1.000000000000000000, 0.7071067811865475727, 1.000000000000000000),
 ( 1.000000000000000000, 0.7071067811865475727, 1.000000000000000000),
 ( 1.000000000000000000, 0.7071067811865475727, 1.000000000000000000),
 ( 1.000000000000000000, 0.7071067811865475727, 1.000000000000000000),
 ( 1.000000000000000000, 0.7071067811865475727, 1.000000000000000000),
 ( 1.000000000000000000, 0.7071067811865475727, 1.000000000000000000) ) ) 
 REPRESENTATION_ITEM ( '' )  SURFACE ( )  );
#60612=CARTESIAN_POINT ( 'NONE',  ( 3.202572202863678275, -1.001691937163285528, 104.2977074219132447 ) ) ;
#60620=CARTESIAN_POINT ( 'NONE',  ( 4.999999999999993783, -3.737948356800089300, 102.2532056550983128 ) ) ;
#60621=CARTESIAN_POINT ( 'NONE',  ( -3.558939058151462831, -48.93902971889401954, 104.4181685828932871 ) ) ;
#60665=CARTESIAN_POINT ( 'NONE',  ( 4.972909066023143865, -46.53482677768356979, 42.62007988880538534 ) ) ;
#60684=CARTESIAN_POINT ( 'NONE',  ( -5.036565248985447774, -51.83812713192594401, 40.06353886212085769 ) ) ;
#60709=CARTESIAN_POINT ( 'NONE',  ( -2.100696513098593066, -49.85179523580853100, 102.1543767095519968 ) ) ;
#60754=CARTESIAN_POINT ( 'NONE',  ( -13.42019126081076941, -55.04352106308903103, 30.98765330636284077 ) ) ;
#60785=ADVANCED_FACE ( 'NONE', ( #98626 ), #84053, .F. ) ;
#60796=( LENGTH_UNIT ( ) NAMED_UNIT ( * ) SI_UNIT ( .MILLI., .METRE. ) );
#60813=MECHANICAL_DESIGN_GEOMETRIC_PRESENTATION_REPRESENTATION('',(#52162),#83112);
#60875=ORIENTED_EDGE ( 'NONE', *, *, #50931, .F. ) ;
#60878=CARTESIAN_POINT ( 'NONE',  ( 3.604576940038719979, -48.95215848635503164, 104.3731177596920503 ) ) ;
#60879=CARTESIAN_POINT ( 'NONE',  ( -4.669235002214947805, -14.10229584173631601, -8.329632653661956709 ) ) ;
#60900=CARTESIAN_POINT ( 'NONE',  ( 4.337283319710566687, -10.96666117361874093, -10.25672613774106345 ) ) ;
#60907=ORIENTED_EDGE ( 'NONE', *, *, #10578, .T. ) ;
#60911=CARTESIAN_POINT ( 'NONE',  ( 0.000000000000000000, -50.00000000000000000, 45.00000000000000000 ) ) ;
#60936=CARTESIAN_POINT ( 'NONE',  ( 1.993516955649224487, -0.1166279987392843664, 102.1895970170251644 ) ) ;
#60948=CARTESIAN_POINT ( 'NONE',  ( -11.48322309281289044, -1.563619715725306891, 20.53900286216184057 ) ) ;
#60953=ADVANCED_FACE ( 'NONE', ( #18830 ), #94476, .F. ) ;
#61034=COLOUR_RGB ( '', 0.09019608, 0.27058824, 0.51372549) ;
#61038=CARTESIAN_POINT ( 'NONE',  ( 1.545731922506614175, -49.97157980004173083, 101.5782547351728624 ) ) ;
#61061=CARTESIAN_POINT ( 'NONE',  ( 5.385673916453010968, -2.602085213965210642E-15, 15.34388420865771607 ) ) ;
#61066=CARTESIAN_POINT ( 'NONE',  ( -5.000000000000000000, -30.71019771943890575, -0.3346393655629185671 ) ) ;
#61101=CARTESIAN_POINT ( 'NONE',  ( 1.000000000000000000, -15.98920185053503928, -10.19345919381780519 ) ) ;
#61102=MECHANICAL_DESIGN_GEOMETRIC_PRESENTATION_REPRESENTATION('',(#21319),#91883);
#61137=CARTESIAN_POINT ( 'NONE',  ( 4.464768147782852026, -1.996984918325857006, 102.6740199126133888 ) ) ;
#61144=CARTESIAN_POINT ( 'NONE',  ( 27.99999999999999645, 0.000000000000000000, 15.00000000000000000 ) ) ;
#61146=DIRECTION ( 'NONE',  ( 1.000000000000000000, 0.000000000000000000, 0.000000000000000000 ) ) ;
#61184=CARTESIAN_POINT ( 'NONE',  ( 5.701904463861252381, -50.89740538927692626, 39.78701112839326015 ) ) ;
#61186=AXIS2_PLACEMENT_3D ( 'NONE', #65556, #66082, #54379 ) ;
#61204=CARTESIAN_POINT ( 'NONE',  ( -4.173972032418419076, -48.44822883994723384, 43.43505066642690338 ) ) ;
#61222=STYLED_ITEM ( 'NONE', ( #96900 ), #35149 ) ;
#61226=ORIENTED_EDGE ( 'NONE', *, *, #5398, .F. ) ;
#61275=CARTESIAN_POINT ( 'NONE',  ( -13.98736753405778543, -57.97328548197708642, 27.64795516495958339 ) ) ;
#61277=FACE_OUTER_BOUND ( 'NONE', #84240, .T. ) ;
#61286=CARTESIAN_POINT ( 'NONE',  ( -4.681380154937277993, -50.73787295680603648, 103.7259032015044795 ) ) ;
#61298=DIRECTION ( 'NONE',  ( 8.673617379884035472E-16, 1.000000000000000000, -4.449471833015289037E-16 ) ) ;
#61323=CARTESIAN_POINT ( 'NONE',  ( 3.454253436624935336, -0.8414180287960453253, 103.7259032015043232 ) ) ;
#61329=FILL_AREA_STYLE_COLOUR ( '', #104166 ) ;
#61339=CARTESIAN_POINT ( 'NONE',  ( 4.999999999999995559, -4.000000000000000000, 42.58845726811989607 ) ) ;
#61374=COLOUR_RGB ( '', 0.09019608, 0.27058824, 0.51372549) ;
#61400=ORIENTED_EDGE ( 'NONE', *, *, #87955, .T. ) ;
#61401=CARTESIAN_POINT ( 'NONE',  ( 2.679328824289926914, -70.32470627744208969, 13.25646130353394803 ) ) ;
#61413=CARTESIAN_POINT ( 'NONE',  ( 3.626288723285761240, -48.95575889185589347, 104.3502830461769406 ) ) ;
#61435=CARTESIAN_POINT ( 'NONE',  ( 5.939725004867027813, -11.78992312938688336, -9.289959103331071333 ) ) ;
#61468=LINE ( 'NONE', #377, #81693 ) ;
#61488=CARTESIAN_POINT ( 'NONE',  ( -11.81863854137958647, -1.931387118382052570, 20.62778170009254808 ) ) ;
#61517=PRESENTATION_STYLE_ASSIGNMENT (( #13983 ) ) ;
#61539=CIRCLE ( 'NONE', #83910, 3.999999999999999112 ) ;
#61576=CARTESIAN_POINT ( 'NONE',  ( 3.677584134044423969, -48.98458100588077713, 104.5297932675492376 ) ) ;
#61602=CARTESIAN_POINT ( 'NONE',  ( 8.928123070943627226, -1.462223317312293158, 15.49551036417120109 ) ) ;
#61608=CARTESIAN_POINT ( 'NONE',  ( -5.000000000000000000, -49.64217499592842131, 7.481703942370503846 ) ) ;
#61631=ORIENTED_EDGE ( 'NONE', *, *, #91727, .T. ) ;
#61633=CARTESIAN_POINT ( 'NONE',  ( -0.9999999999999943379, -1.409462824231155764E-15, 101.0455488498966758 ) ) ;
#61638=( LENGTH_UNIT ( ) NAMED_UNIT ( * ) SI_UNIT ( .MILLI., .METRE. ) );
#61642=MECHANICAL_DESIGN_GEOMETRIC_PRESENTATION_REPRESENTATION('',(#92636),#52995);
#61643=EDGE_CURVE ( 'NONE', #41445, #40039, #97137, .T. ) ;
#61696=AXIS2_PLACEMENT_3D ( 'NONE', #98604, #16635, #39468 ) ;
#61706=CARTESIAN_POINT ( 'NONE',  ( 5.000000000000000000, -63.32102160712415895, 12.61250543006184088 ) ) ;
#61727=FILL_AREA_STYLE_COLOUR ( '', #47692 ) ;
#61731=CARTESIAN_POINT ( 'NONE',  ( 1.529791816479536326, -49.97354766897922218, 44.88943603909616087 ) ) ;
#61739=CARTESIAN_POINT ( 'NONE',  ( 0.000000000000000000, -78.00000000000000000, 41.00000000000000000 ) ) ;
#61742=CARTESIAN_POINT ( 'NONE',  ( 0.000000000000000000, -78.00000000000000000, 27.00000000000000000 ) ) ;
#61750=CARTESIAN_POINT ( 'NONE',  ( -4.332563242637840872, -48.31029031541129370, 40.50631733802364209 ) ) ;
#61797=APPLICATION_CONTEXT ( 'automotive_design' ) ;
#61812=( GEOMETRIC_REPRESENTATION_CONTEXT ( 3 ) GLOBAL_UNCERTAINTY_ASSIGNED_CONTEXT ( ( #9477 ) ) GLOBAL_UNIT_ASSIGNED_CONTEXT ( ( #50185, #73381, #1617 ) ) REPRESENTATION_CONTEXT ( 'NONE', 'WORKASPACE' ) );
#61823=CARTESIAN_POINT ( 'NONE',  ( 6.677362058809300116, -11.98847278904868396, 9.465251842568012108 ) ) ;
#61840=DIRECTION ( 'NONE',  ( 1.096832036894112098E-16, -0.000000000000000000, 1.000000000000000000 ) ) ;
#61845=ORIENTED_EDGE ( 'NONE', *, *, #36312, .F. ) ;
#61866=CARTESIAN_POINT ( 'NONE',  ( 0.9999999999999961142, -4.000000000000000000, 27.00000000000000000 ) ) ;
#61916=PRESENTATION_STYLE_ASSIGNMENT (( #102345 ) ) ;
#61942=CARTESIAN_POINT ( 'NONE',  ( 1.408267258621023643, -70.62266515023254954, 13.06855514134478469 ) ) ;
#61948=CARTESIAN_POINT ( 'NONE',  ( -5.330204762053584844, -8.150230459544712147, 13.71357708370459072 ) ) ;
#61951=CARTESIAN_POINT ( 'NONE',  ( 4.284822031654949015, -48.90716638558772900, 104.4267991316944943 ) ) ;
#61981=CARTESIAN_POINT ( 'NONE',  ( 3.454253436624935336, -0.8414180287960453253, 103.7259032015043232 ) ) ;
#62009=CARTESIAN_POINT ( 'NONE',  ( 2.678351059745755602, -0.3580534592355345547, 103.0656783881315306 ) ) ;
#62023=CARTESIAN_POINT ( 'NONE',  ( -11.60195201528633291, -1.681760983426669576, 20.57261808643857037 ) ) ;
#62039=DIRECTION ( 'NONE',  ( -0.000000000000000000, -1.000000000000000000, -0.000000000000000000 ) ) ;
#62058=CARTESIAN_POINT ( 'NONE',  ( -4.999999999999922728, -12.25926108426836514, 9.485372419963017165 ) ) ;
#62068=CIRCLE ( 'NONE', #15526, 9.999999999999994671 ) ;
#62081=CARTESIAN_POINT ( 'NONE',  ( -3.631499270081283814, -68.18321798808027268, 13.10122733214759982 ) ) ;
#62082=DIRECTION ( 'NONE',  ( 0.000000000000000000, 0.000000000000000000, 1.000000000000000000 ) ) ;
#62151=ORIENTED_EDGE ( 'NONE', *, *, #26086, .T. ) ;
#62157=AXIS2_PLACEMENT_3D ( 'NONE', #14415, #46806, #38216 ) ;
#62167=UNCERTAINTY_MEASURE_WITH_UNIT (LENGTH_MEASURE( 1.000000000000000082E-05 ), #43860, 'distance_accuracy_value', 'NONE');
#62179=PLANE ( 'NONE',  #69926 ) ;
#62181=CARTESIAN_POINT ( 'NONE',  ( 1.000000000000000000, -69.59657292934913642, 12.76848391599222765 ) ) ;
#62185=( NAMED_UNIT ( * ) PLANE_ANGLE_UNIT ( ) SI_UNIT ( $, .RADIAN. ) );
#62207=CARTESIAN_POINT ( 'NONE',  ( 4.999999999999995559, -4.000000000000003553, 40.07669683062201926 ) ) ;
#62214=SURFACE_SIDE_STYLE ('',( #22281 ) ) ;
#62219=ORIENTED_EDGE ( 'NONE', *, *, #92025, .F. ) ;
#62233=DIRECTION ( 'NONE',  ( 1.000000000000000000, 0.000000000000000000, 0.000000000000000000 ) ) ;
#62236=FILL_AREA_STYLE ('',( #101061 ) ) ;
#62278=ORIENTED_EDGE ( 'NONE', *, *, #15787, .F. ) ;
#62330=CARTESIAN_POINT ( 'NONE',  ( 1.337681583493947279, -5.478209635665768573, -13.97306298562694060 ) ) ;
#62341=UNCERTAINTY_MEASURE_WITH_UNIT (LENGTH_MEASURE( 1.000000000000000082E-05 ), #97403, 'distance_accuracy_value', 'NONE');
#62347=CARTESIAN_POINT ( 'NONE',  ( 13.28402714419663155, 1.403786919265707089, 14.93563726026576788 ) ) ;
#62368=DIRECTION ( 'NONE',  ( -1.000000000000000000, 8.673617379884035472E-16, 0.000000000000000000 ) ) ;
#62398=CARTESIAN_POINT ( 'NONE',  ( 13.59360248487383771, -51.99192117344531994, 23.64795065864135637 ) ) ;
#62412=SURFACE_SIDE_STYLE ('',( #62940 ) ) ;
#62423=MECHANICAL_DESIGN_GEOMETRIC_PRESENTATION_REPRESENTATION('',(#2104),#57220);
#62427=AXIS2_PLACEMENT_3D ( 'NONE', #33114, #82696, #65979 ) ;
#62456=CARTESIAN_POINT ( 'NONE',  ( 5.146599240078983506, -67.41437153544924854, 13.97902347505284837 ) ) ;
#62463=CARTESIAN_POINT ( 'NONE',  ( -5.846241857870205116, -7.705620505147201094, 13.78798924724435615 ) ) ;
#62468=CARTESIAN_POINT ( 'NONE',  ( -3.158708192431145090, -10.09041393549569499, -11.69019864734867831 ) ) ;
#62537=CARTESIAN_POINT ( 'NONE',  ( -9.803567740517793894, -0.5665513748614124934, 19.98103188536380870 ) ) ;
#62566=( LENGTH_UNIT ( ) NAMED_UNIT ( * ) SI_UNIT ( .MILLI., .METRE. ) );
#62570=SURFACE_SIDE_STYLE ('',( #47420 ) ) ;
#62571=DIRECTION ( 'NONE',  ( 0.000000000000000000, 1.000000000000000000, 0.000000000000000000 ) ) ;
#62595=( LENGTH_UNIT ( ) NAMED_UNIT ( * ) SI_UNIT ( .MILLI., .METRE. ) );
#62599=CARTESIAN_POINT ( 'NONE',  ( 4.391938347788338248, -48.86119740214457607, 104.3926446507460923 ) ) ;
#62631=CARTESIAN_POINT ( 'NONE',  ( 1.469576158976823947E-15, -78.00000000000000000, 15.00000000000000000 ) ) ;
#62643=B_SPLINE_CURVE_WITH_KNOTS ( 'NONE', 3,
 ( #30670, #87827, #91982, #60187, #67719, #76322, #60709, #41835, #43446, #93591, #2435, #83889 ),
 .UNSPECIFIED., .F., .F.,
 ( 4, 2, 2, 2, 2, 4 ),
 ( -4.799938976750792050E-05, 0.0004199937929076860850, 0.0008879869755828801109, 0.001823973340933268163, 0.002759959706283656323, 0.003695946071634044483 ),
 .UNSPECIFIED. ) ;
#62662=CARTESIAN_POINT ( 'NONE',  ( -1.000000000000000000, -56.64697988393488259, 6.234486214427730211 ) ) ;
#62663=DIRECTION ( 'NONE',  ( 0.4999999999999996669, 0.000000000000000000, -0.8660254037844390407 ) ) ;
#62680=CARTESIAN_POINT ( 'NONE',  ( -3.303250429860502102, -0.7130296830186633184, 103.9470740044716024 ) ) ;
#62702=EDGE_CURVE ( 'NONE', #89611, #42044, #68256, .T. ) ;
#62709=CARTESIAN_POINT ( 'NONE',  ( 13.38090213880806800, -54.26185238422452528, 31.11721482942555994 ) ) ;
#62714=CARTESIAN_POINT ( 'NONE',  ( 3.352941176470589646, -48.79941684889505638, 104.5794940929807524 ) ) ;
#62726=CYLINDRICAL_SURFACE ( 'NONE', #79985, 4.000000000000000000 ) ;
#62742=( NAMED_UNIT ( * ) PLANE_ANGLE_UNIT ( ) SI_UNIT ( $, .RADIAN. ) );
#62745=CARTESIAN_POINT ( 'NONE',  ( -4.969492168108461172, -46.56556601679959329, 42.62409117991908403 ) ) ;
#62771=DIRECTION ( 'NONE',  ( 0.000000000000000000, 0.000000000000000000, 1.000000000000000000 ) ) ;
#62787=CARTESIAN_POINT ( 'NONE',  ( 8.999999999999996447, -4.000000000000003553, 42.58845726811989607 ) ) ;
#62794=CARTESIAN_POINT ( 'NONE',  ( -9.788305016933179559, -12.70835420169926167, 16.98816223485645693 ) ) ;
#62796=CARTESIAN_POINT ( 'NONE',  ( -1.607819346471298427, -53.94600928665112605, 40.91329866885064348 ) ) ;
#62798=( BOUNDED_SURFACE ( )  B_SPLINE_SURFACE ( 3, 2, ( 
 ( #84800, #68636, #1735 ),
 ( #67029, #27671, #51354 ),
 ( #83196, #9293, #50293 ),
 ( #2261, #17950, #10362 ),
 ( #1182, #50812, #43276 ),
 ( #34690, #83716, #9825 ),
 ( #76161, #63185, #62662 ),
 ( #61608, #96079, #14069 ),
 ( #4407, #29261, #46463 ),
 ( #79350, #45935, #22210 ),
 ( #78289, #5470, #13544 ),
 ( #61066, #53493, #4947 ),
 ( #55061, #30296, #38393 ),
 ( #104152, #46978, #87991 ),
 ( #70735, #79876, #78815 ),
 ( #87465, #102577, #52958 ) ),
 .UNSPECIFIED., .F., .F., .F. ) 
 B_SPLINE_SURFACE_WITH_KNOTS ( ( 4, 2, 2, 2, 2, 2, 2, 4 ),
 ( 3, 3 ),
 ( -3.089907223421224040E-05, 0.004354571166036939195, 0.008740041404308090955, 0.01751098188085039448, 0.02628192235739269800, 0.03505286283393500152, 0.05259474378701960162, 0.07013662474010420866 ),
 ( 0.000000000000000000, 1.000000000000000000 ),
 .UNSPECIFIED. ) 
 GEOMETRIC_REPRESENTATION_ITEM ( )  RATIONAL_B_SPLINE_SURFACE ( (
 ( 1.000000000000000000, 0.7071067811865475727, 1.000000000000000000),
 ( 1.000000000000000000, 0.7071067811865475727, 1.000000000000000000),
 ( 1.000000000000000000, 0.7071067811865475727, 1.000000000000000000),
 ( 1.000000000000000000, 0.7071067811865475727, 1.000000000000000000),
 ( 1.000000000000000000, 0.7071067811865479058, 1.000000000000000000),
 ( 1.000000000000000000, 0.7071067811865479058, 1.000000000000000000),
 ( 1.000000000000000000, 0.7071067811865475727, 1.000000000000000000),
 ( 1.000000000000000000, 0.7071067811865475727, 1.000000000000000000),
 ( 1.000000000000000000, 0.7071067811865475727, 1.000000000000000000),
 ( 1.000000000000000000, 0.7071067811865475727, 1.000000000000000000),
 ( 1.000000000000000000, 0.7071067811865475727, 1.000000000000000000),
 ( 1.000000000000000000, 0.7071067811865475727, 1.000000000000000000),
 ( 1.000000000000000000, 0.7071067811865475727, 1.000000000000000000),
 ( 1.000000000000000000, 0.7071067811865475727, 1.000000000000000000),
 ( 1.000000000000000000, 0.7071067811865475727, 1.000000000000000000),
 ( 1.000000000000000000, 0.7071067811865475727, 1.000000000000000000) ) ) 
 REPRESENTATION_ITEM ( '' )  SURFACE ( )  );
#62818=VERTEX_POINT ( 'NONE', #89141 ) ;
#62837=ORIENTED_EDGE ( 'NONE', *, *, #41694, .T. ) ;
#62841=CIRCLE ( 'NONE', #18035, 3.999999999999989786 ) ;
#62842=MECHANICAL_DESIGN_GEOMETRIC_PRESENTATION_REPRESENTATION('',(#31811),#7680);
#62851=FILL_AREA_STYLE ('',( #54188 ) ) ;
#62856=CIRCLE ( 'NONE', #24982, 2.000000000000000000 ) ;
#62892=CARTESIAN_POINT ( 'NONE',  ( -0.9330442100817423201, -70.05675763226157926, 13.03100537459360986 ) ) ;
#62916=CARTESIAN_POINT ( 'NONE',  ( 30.00000000000000000, 0.000000000000000000, -11.00000000000000000 ) ) ;
#62917=AXIS2_PLACEMENT_3D ( 'NONE', #70641, #103535, #103016 ) ;
#62940=SURFACE_STYLE_FILL_AREA ( #13830 ) ;
#62943=CARTESIAN_POINT ( 'NONE',  ( -1.232335077818826452, -49.99311995005906084, 101.3399051430503164 ) ) ;
#62947=FACE_OUTER_BOUND ( 'NONE', #32801, .T. ) ;
#62952=DIRECTION ( 'NONE',  ( 0.000000000000000000, -0.3488521823429531765, 0.9371777605526920851 ) ) ;
#62961=CARTESIAN_POINT ( 'NONE',  ( -5.803898591548312780, -3.468598768277427524, 103.8893302396401879 ) ) ;
#62994=CARTESIAN_POINT ( 'NONE',  ( -8.016921032071788744, -5.439319868627221943, 14.17797645233462056 ) ) ;
#63032=CARTESIAN_POINT ( 'NONE',  ( -3.510275272315380057, -48.85091879836223683, 104.5952116206504456 ) ) ;
#63066=CARTESIAN_POINT ( 'NONE',  ( -9.057198557144582551, -0.3318150627287249632, 19.72202478657212765 ) ) ;
#63093=CARTESIAN_POINT ( 'NONE',  ( 6.125000000000000000, -60.71953810597977252, 14.41094225130411033 ) ) ;
#63098=CARTESIAN_POINT ( 'NONE',  ( 1.112434445721927290, -50.00000000000002132, 101.1533620683574952 ) ) ;
#63100=CARTESIAN_POINT ( 'NONE',  ( -13.50929957260945535, -52.70262457293414826, 23.32445699588452470 ) ) ;
#63101=DIRECTION ( 'NONE',  ( 0.000000000000000000, 1.224646799147353454E-16, 1.000000000000000000 ) ) ;
#63106=VERTEX_POINT ( 'NONE', #84235 ) ;
#63126=UNCERTAINTY_MEASURE_WITH_UNIT (LENGTH_MEASURE( 1.000000000000000082E-05 ), #1729, 'distance_accuracy_value', 'NONE');
#63158=ORIENTED_EDGE ( 'NONE', *, *, #37057, .T. ) ;
#63185=CARTESIAN_POINT ( 'NONE',  ( -5.000000000000000888, -56.64697988390040706, 6.234486214504725510 ) ) ;
#63209=CARTESIAN_POINT ( 'NONE',  ( -3.870939636683478291, -1.214734195355908319, 104.2727580839184895 ) ) ;
#63210=SURFACE_STYLE_USAGE ( .BOTH. , #6008 ) ;
#63215=MECHANICAL_DESIGN_GEOMETRIC_PRESENTATION_REPRESENTATION('',(#66668),#75277);
#63241=CARTESIAN_POINT ( 'NONE',  ( 13.95403936970824965, -57.86992245155132508, 28.16216733762122004 ) ) ;
#63303=CARTESIAN_POINT ( 'NONE',  ( 0.000000000000000000, -46.00000000000000000, 112.0000000000000000 ) ) ;
#63323=CIRCLE ( 'NONE', #8553, 4.000000000000003553 ) ;
#63334=CARTESIAN_POINT ( 'NONE',  ( -11.96225037626273036, -7.080565903723901933, 19.72249172895450542 ) ) ;
#63335=ORIENTED_EDGE ( 'NONE', *, *, #16592, .T. ) ;
#63353=CARTESIAN_POINT ( 'NONE',  ( 0.000000000000000000, 0.000000000000000000, 18.57417562100670949 ) ) ;
#63359=ORIENTED_EDGE ( 'NONE', *, *, #47375, .T. ) ;
#63365=SURFACE_STYLE_USAGE ( .BOTH. , #12654 ) ;
#63390=SURFACE_STYLE_FILL_AREA ( #62851 ) ;
#63415=CARTESIAN_POINT ( 'NONE',  ( 6.251124561268293967, 3.157894736842103534, 14.66382285868950675 ) ) ;
#63449=( BOUNDED_SURFACE ( )  B_SPLINE_SURFACE ( 3, 2, ( 
 ( #94409, #102492, #71688 ),
 ( #28635, #53918, #104063 ),
 ( #30206, #20572, #4856 ),
 ( #53410, #62058, #12394 ),
 ( #86849, #80308, #65740 ),
 ( #98621, #24770, #64679 ),
 ( #31279, #80847, #16654 ),
 ( #57619, #105655, #88431 ),
 ( #57097, #15585, #90545 ),
 ( #32864, #49544, #82449 ),
 ( #6420, #41455, #8554 ),
 ( #74346, #73820, #106714 ),
 ( #423, #65202, #56023 ),
 ( #15049, #73276, #33391 ),
 ( #66263, #22657, #55493 ),
 ( #23175, #24248, #14505 ),
 ( #47417, #39359, #72236 ),
 ( #88954, #105139, #47938 ),
 ( #72749, #64165, #6959 ),
 ( #16115, #7477, #32334 ),
 ( #97037, #106172, #40393 ),
 ( #39876, #31793, #56563 ),
 ( #97552, #8018, #23711 ),
 ( #89490, #48475, #81368 ),
 ( #98097, #90011, #81901 ),
 ( #48999, #40927, #85112 ) ),
 .UNSPECIFIED., .F., .F., .F. ) 
 B_SPLINE_SURFACE_WITH_KNOTS ( ( 4, 2, 2, 2, 2, 2, 2, 2, 2, 2, 2, 2, 4 ),
 ( 3, 3 ),
 ( -8.736501105888194729E-16, 0.0005478302971548104335, 0.001095660594310494517, 0.001643490891466178492, 0.001917406040044020588, 0.002191321188621862467, 0.002465236337199704347, 0.002739151485777546226, 0.003013066634355388539, 0.003286981782933230418, 0.003560896931511072297, 0.003834812080088914610, 0.004382642377244598368 ),
 ( 0.000000000000000000, 1.000000000000000000 ),
 .UNSPECIFIED. ) 
 GEOMETRIC_REPRESENTATION_ITEM ( )  RATIONAL_B_SPLINE_SURFACE ( (
 ( 1.000000000000000000, 0.7071067811865463515, 1.000000000000000000),
 ( 1.000000000000000000, 0.7205633224822174387, 1.000000000000000000),
 ( 1.000000000000000000, 0.7338046748641441352, 1.000000000000000000),
 ( 1.000000000000000000, 0.7598569482828753108, 1.000000000000000000),
 ( 1.000000000000000000, 0.7728059803407538730, 1.000000000000000000),
 ( 1.000000000000000000, 0.7970392697931634185, 1.000000000000000000),
 ( 1.000000000000000000, 0.8084357292879817969, 1.000000000000000000),
 ( 1.000000000000000000, 0.8242617997985818290, 1.000000000000000000),
 ( 1.000000000000000000, 0.8292815833619189281, 1.000000000000000000),
 ( 1.000000000000000000, 0.8385524799095220860, 1.000000000000000000),
 ( 1.000000000000000000, 0.8428399694390146246, 1.000000000000000000),
 ( 1.000000000000000000, 0.8506757475323690754, 1.000000000000000000),
 ( 1.000000000000000000, 0.8542245152660158380, 1.000000000000000000),
 ( 1.000000000000000000, 0.8604965487139214497, 1.000000000000000000),
 ( 1.000000000000000000, 0.8631692933856984773, 1.000000000000000000),
 ( 1.000000000000000000, 0.8674535388008016712, 1.000000000000000000),
 ( 1.000000000000000000, 0.8690878299427780007, 1.000000000000000000),
 ( 1.000000000000000000, 0.8713061800473431706, 1.000000000000000000),
 ( 1.000000000000000000, 0.8718871419634710573, 1.000000000000000000),
 ( 1.000000000000000000, 0.8719209662387543691, 1.000000000000000000),
 ( 1.000000000000000000, 0.8713887681177838740, 1.000000000000000000),
 ( 1.000000000000000000, 0.8692752663532812285, 1.000000000000000000),
 ( 1.000000000000000000, 0.8676790533738677480, 1.000000000000000000),
 ( 1.000000000000000000, 0.8614089247988945264, 1.000000000000000000),
 ( 1.000000000000000000, 0.8553884691243534011, 1.000000000000000000),
 ( 1.000000000000000000, 0.8477912478906586280, 1.000000000000000000) ) ) 
 REPRESENTATION_ITEM ( '' )  SURFACE ( )  );
#63460=EDGE_CURVE ( 'NONE', #90150, #91492, #64737, .T. ) ;
#63479=COLOUR_RGB ( '', 0.72549020, 0.75294118, 0.79215686) ;
#63496=CARTESIAN_POINT ( 'NONE',  ( -7.000000000000001776, -80.00000000000000000, 39.12435565298213902 ) ) ;
#63516=FILL_AREA_STYLE_COLOUR ( '', #3833 ) ;
#63523=CARTESIAN_POINT ( 'NONE',  ( 5.615011524526196673, -65.90784209089324008, 14.17484251393565309 ) ) ;
#63531=CARTESIAN_POINT ( 'NONE',  ( -12.97770155848252926, -9.693230400136535252, 11.45906137556292670 ) ) ;
#63532=B_SPLINE_CURVE_WITH_KNOTS ( 'NONE', 3,
 ( #92213, #32959, #73909, #57188, #43157, #50679, #1056, #34031 ),
 .UNSPECIFIED., .F., .F.,
 ( 4, 2, 2, 4 ),
 ( 1.852685484479510593E-18, 0.0001460451837441709491, 0.0002190677756162548516, 0.0002920903674883387540 ),
 .UNSPECIFIED. ) ;
#63535=CARTESIAN_POINT ( 'NONE',  ( 8.572527594031477134E-16, -50.00000000000000000, 105.0000000000000000 ) ) ;
#63552=CIRCLE ( 'NONE', #29163, 13.00000000000000000 ) ;
#63587=VERTEX_POINT ( 'NONE', #25799 ) ;
#63610=FILL_AREA_STYLE_COLOUR ( '', #87560 ) ;
#63636=( LENGTH_UNIT ( ) NAMED_UNIT ( * ) SI_UNIT ( .MILLI., .METRE. ) );
#63639=DIRECTION ( 'NONE',  ( 0.000000000000000000, 1.000000000000000000, 0.000000000000000000 ) ) ;
#63652=ORIENTED_EDGE ( 'NONE', *, *, #81486, .T. ) ;
#63700=CARTESIAN_POINT ( 'NONE',  ( -9.521335790331885818, -51.55696187956029064, 23.93938989165062026 ) ) ;
#63719=AXIS2_PLACEMENT_3D ( 'NONE', #92033, #18167, #1947 ) ;
#63744=FACE_OUTER_BOUND ( 'NONE', #104172, .T. ) ;
#63747=CARTESIAN_POINT ( 'NONE',  ( 0.000000000000000000, -54.00000000000000711, 27.00000000000000000 ) ) ;
#63783=CARTESIAN_POINT ( 'NONE',  ( 9.113097280746996987, -54.00000000000000711, 31.11721482942554928 ) ) ;
#63788=CARTESIAN_POINT ( 'NONE',  ( 1.000000000000000000, -64.69017754617701144, 10.12118620307032302 ) ) ;
#63820=CARTESIAN_POINT ( 'NONE',  ( -9.995225837605406838, -57.97473475263401355, 26.59626811386029743 ) ) ;
#63826=AXIS2_PLACEMENT_3D ( 'NONE', #10245, #51219, #42080 ) ;
#63843=VERTEX_POINT ( 'NONE', #11669 ) ;
#63863=CARTESIAN_POINT ( 'NONE',  ( -5.000000000000003553, -45.99999999999999289, 40.27905619136138426 ) ) ;
#63886=ORIENTED_EDGE ( 'NONE', *, *, #92997, .T. ) ;
#63954=( NAMED_UNIT ( * ) PLANE_ANGLE_UNIT ( ) SI_UNIT ( $, .RADIAN. ) );
#63971=B_SPLINE_CURVE_WITH_KNOTS ( 'NONE', 3,
 ( #90749, #97758, #6633, #14713, #23925, #47087, #106376, #65409, #24457, #80514, #57293, #82105 ),
 .UNSPECIFIED., .F., .F.,
 ( 4, 2, 2, 2, 2, 4 ),
 ( 0.000000000000000000, 0.0008138854558913180548, 0.001220828183836985756, 0.001627770911782653457, 0.002441656367673991027, 0.003255541823565328598 ),
 .UNSPECIFIED. ) ;
#63993=UNCERTAINTY_MEASURE_WITH_UNIT (LENGTH_MEASURE( 1.000000000000000082E-05 ), #22994, 'distance_accuracy_value', 'NONE');
#64007=CARTESIAN_POINT ( 'NONE',  ( 15.90614609307868399, -3.157894736842107530, 14.66382285868950675 ) ) ;
#64038=CARTESIAN_POINT ( 'NONE',  ( -4.680975426248723537, -2.415770170678390727, 103.4780497728483226 ) ) ;
#64039=ORIENTED_EDGE ( 'NONE', *, *, #81987, .F. ) ;
#64069=CARTESIAN_POINT ( 'NONE',  ( -14.03901844863619530, -8.437680008516872832, 12.41437985069090466 ) ) ;
#64119=FACE_OUTER_BOUND ( 'NONE', #2581, .T. ) ;
#64139=DIRECTION ( 'NONE',  ( -0.000000000000000000, -1.000000000000000000, -0.000000000000000000 ) ) ;
#64140=( NAMED_UNIT ( * ) PLANE_ANGLE_UNIT ( ) SI_UNIT ( $, .RADIAN. ) );
#64141=STYLED_ITEM ( 'NONE', ( #31592 ), #10316 ) ;
#64144=SURFACE_SIDE_STYLE ('',( #80283 ) ) ;
#64161=VERTEX_POINT ( 'NONE', #92087 ) ;
#64165=CARTESIAN_POINT ( 'NONE',  ( -4.999999999999999112, -13.81090860391436514, 13.12305563960475752 ) ) ;
#64168=FACE_OUTER_BOUND ( 'NONE', #9382, .T. ) ;
#64189=CARTESIAN_POINT ( 'NONE',  ( -9.113097280746996987, -54.00000000000000711, 31.11721482942554928 ) ) ;
#64224=CARTESIAN_POINT ( 'NONE',  ( 9.442395496852061143, -51.55837707188687347, 30.29618450995123169 ) ) ;
#64228=CARTESIAN_POINT ( 'NONE',  ( -9.821751540093583088, -50.53182543592436815, 25.10730599066359758 ) ) ;
#64251=EDGE_CURVE ( 'NONE', #63843, #40108, #73297, .T. ) ;
#64252=EDGE_CURVE ( 'NONE', #41862, #5701, #49314, .T. ) ;
#64274=( NAMED_UNIT ( * ) SI_UNIT ( $, .STERADIAN. ) SOLID_ANGLE_UNIT ( ) );
#64300=CARTESIAN_POINT ( 'NONE',  ( 13.59366797464709720, -56.00856538105860949, 23.64820470065338753 ) ) ;
#64312=CARTESIAN_POINT ( 'NONE',  ( -3.769311339736956867, -1.074854658864006440, 104.1674216685381822 ) ) ;
#64316=( LENGTH_UNIT ( ) NAMED_UNIT ( * ) SI_UNIT ( .MILLI., .METRE. ) );
#64329=ORIENTED_EDGE ( 'NONE', *, *, #82380, .T. ) ;
#64350=AXIS2_PLACEMENT_3D ( 'NONE', #81589, #72978, #30982 ) ;
#64390=CARTESIAN_POINT ( 'NONE',  ( -6.663161659568015871, -48.60989497021113692, 39.31288131909047223 ) ) ;
#64425=CARTESIAN_POINT ( 'NONE',  ( -2.504960188439524060, -0.4123968666590282495, 103.1314300587539776 ) ) ;
#64450=CARTESIAN_POINT ( 'NONE',  ( -27.99999999999999645, 1.102182119232617714E-15, -9.000000000000000000 ) ) ;
#64455=EDGE_CURVE ( 'NONE', #50280, #3333, #25264, .T. ) ;
#64477=( NAMED_UNIT ( * ) SI_UNIT ( $, .STERADIAN. ) SOLID_ANGLE_UNIT ( ) );
#64482=CARTESIAN_POINT ( 'NONE',  ( -2.551467019400163405, -69.79337258748924455, 13.23174192411898353 ) ) ;
#64524=COLOUR_RGB ( '', 0.09019608, 0.27058824, 0.51372549) ;
#64534=CARTESIAN_POINT ( 'NONE',  ( -2.504928271494545555, -49.58762337132401399, 103.1313799838700191 ) ) ;
#64554=CARTESIAN_POINT ( 'NONE',  ( -5.833333333333327708, -4.000000000000004441, 103.8776713793258608 ) ) ;
#64578=CARTESIAN_POINT ( 'NONE',  ( 6.125000000000000000, -60.71953810597977252, 14.41094225130411033 ) ) ;
#64586=PRESENTATION_STYLE_ASSIGNMENT (( #49441 ) ) ;
#64624=CARTESIAN_POINT ( 'NONE',  ( -4.147930821993661255, -48.94936713426047703, 104.5115743862824331 ) ) ;
#64659=SURFACE_STYLE_FILL_AREA ( #16102 ) ;
#64679=CARTESIAN_POINT ( 'NONE',  ( -5.000000000000000000, -13.80294717177778274, 10.52286356751779550 ) ) ;
#64689=DIRECTION ( 'NONE',  ( 0.000000000000000000, 0.000000000000000000, -1.000000000000000000 ) ) ;
#64730=( NAMED_UNIT ( * ) PLANE_ANGLE_UNIT ( ) SI_UNIT ( $, .RADIAN. ) );
#64732=COLOUR_RGB ( '', 0.72549020, 0.75294118, 0.79215686) ;
#64736=CARTESIAN_POINT ( 'NONE',  ( 9.728434877168217199, -50.82153073783059227, 24.67462639010848946 ) ) ;
#64737=CIRCLE ( 'NONE', #81874, 2.000000000000003553 ) ;
#64767=CARTESIAN_POINT ( 'NONE',  ( -3.857142857142847880, -48.79941684889506348, 103.1763305333244318 ) ) ;
#64797=ORIENTED_EDGE ( 'NONE', *, *, #13287, .F. ) ;
#64824=ORIENTED_EDGE ( 'NONE', *, *, #99623, .F. ) ;
#64830=CARTESIAN_POINT ( 'NONE',  ( 9.960739174314243272, -57.87150899010582350, 26.07695415532590033 ) ) ;
#64835=CARTESIAN_POINT ( 'NONE',  ( 5.000000000000000000, -30.70749484266840312, -0.3356907877405980178 ) ) ;
#64837=CARTESIAN_POINT ( 'NONE',  ( 15.82312105870659025, -3.732472542269488880, 14.54008594198294801 ) ) ;
#64908=CARTESIAN_POINT ( 'NONE',  ( -7.000000000000000888, -46.00000000000000711, 39.12435565298213902 ) ) ;
#64913=CARTESIAN_POINT ( 'NONE',  ( -3.704240196697770049, -48.94878093480736680, 103.3230214382350596 ) ) ;
#64934=CARTESIAN_POINT ( 'NONE',  ( -5.371950044183565254, -2.205168805904307305, 104.0625755208173473 ) ) ;
#64983=CARTESIAN_POINT ( 'NONE',  ( -15.26755105656414990, -0.4567640699404665883, 14.99506816343297011 ) ) ;
#64991=SURFACE_STYLE_FILL_AREA ( #39146 ) ;
#65002=ORIENTED_EDGE ( 'NONE', *, *, #4373, .T. ) ;
#65005=DIRECTION ( 'NONE',  ( -1.000000000000000000, 0.000000000000000000, 0.000000000000000000 ) ) ;
#65006=SURFACE_SIDE_STYLE ('',( #42853 ) ) ;
#65018=MECHANICAL_DESIGN_GEOMETRIC_PRESENTATION_REPRESENTATION('',(#1230),#58151);
#65027=( NAMED_UNIT ( * ) PLANE_ANGLE_UNIT ( ) SI_UNIT ( $, .RADIAN. ) );
#65028=DIRECTION ( 'NONE',  ( 0.000000000000000000, 0.000000000000000000, 1.000000000000000000 ) ) ;
#65034=MECHANICAL_DESIGN_GEOMETRIC_PRESENTATION_REPRESENTATION('',(#46115),#11678);
#65073=CARTESIAN_POINT ( 'NONE',  ( -4.211261491276407476, -1.586805402943917587, 103.7733746176806875 ) ) ;
#65099=CARTESIAN_POINT ( 'NONE',  ( 5.973896061805174185, -13.10340519129061043, 13.28276905619554427 ) ) ;
#65135=CARTESIAN_POINT ( 'NONE',  ( -5.603804764708762320, -47.29776092513153429, 103.9691152301449790 ) ) ;
#65140=CARTESIAN_POINT ( 'NONE',  ( 7.000000000000000000, -80.00000000000000000, 12.61250543006184088 ) ) ;
#65177=ORIENTED_EDGE ( 'NONE', *, *, #105637, .T. ) ;
#65198=ORIENTED_EDGE ( 'NONE', *, *, #69675, .T. ) ;
#65202=CARTESIAN_POINT ( 'NONE',  ( -5.000000000000039968, -12.89614509140995224, 12.11365041472577886 ) ) ;
#65265=CARTESIAN_POINT ( 'NONE',  ( 9.901690565149895207, -50.20903247757873089, 28.42036373910763558 ) ) ;
#65269=CARTESIAN_POINT ( 'NONE',  ( -9.934548988108780065, -50.13240894597250019, 28.17116772486389564 ) ) ;
#65280=CARTESIAN_POINT ( 'NONE',  ( 5.802268690544500451, -46.54360925828362383, 103.8899761878886494 ) ) ;
#65311=( BOUNDED_SURFACE ( )  B_SPLINE_SURFACE ( 3, 2, ( 
 ( #91941, #49342, #83845 ),
 ( #42860, #89824, #98433 ),
 ( #15928, #16453, #60665 ),
 ( #68755, #12600, #27255 ),
 ( #18614, #12077, #45007 ),
 ( #85454, #101099, #67675 ),
 ( #4003, #2390, #69283 ),
 ( #36413, #11539, #93552 ),
 ( #61184, #51476, #84391 ),
 ( #52004, #1850, #76282 ),
 ( #10480, #86540, #27793 ),
 ( #20238, #60142, #93006 ),
 ( #43400, #35337, #19701 ),
 ( #59591, #102695, #19170 ),
 ( #102158, #86007, #52534 ),
 ( #100558, #28308, #44464 ),
 ( #35876, #68199, #77359 ),
 ( #53085, #77892, #94626 ),
 ( #69798, #84921, #94071 ),
 ( #34807, #3470, #36933 ),
 ( #76812, #11006, #28857 ),
 ( #43923, #2922, #61731 ),
 ( #101636, #20771, #53606 ),
 ( #75753, #26719, #92463 ) ),
 .UNSPECIFIED., .F., .F., .T. ) 
 B_SPLINE_SURFACE_WITH_KNOTS ( ( 4, 2, 2, 2, 2, 2, 2, 2, 2, 2, 2, 4 ),
 ( 3, 3 ),
 ( 0.004964016820073290440, 0.006562036933636941453, 0.008160057047200592467, 0.009758077160764244348, 0.01055708721754607116, 0.01135609727432789623, 0.01215510733110972130, 0.01295411738789154811, 0.01455213750145519999, 0.01535114755823702680, 0.01615015761501885361, 0.01774817772858250375 ),
 ( 0.000000000000000000, 1.000000000000000000 ),
 .UNSPECIFIED. ) 
 GEOMETRIC_REPRESENTATION_ITEM ( )  RATIONAL_B_SPLINE_SURFACE ( (
 ( 1.000000000000000000, 0.8660254037844384856, 1.000000000000000000),
 ( 1.000000000000000000, 0.8660222092865146326, 1.000000000000000000),
 ( 1.000000000000000000, 0.8641678725695443042, 1.000000000000000000),
 ( 1.000000000000000000, 0.8570944999502960737, 1.000000000000000000),
 ( 1.000000000000000000, 0.8517853798393946185, 1.000000000000000000),
 ( 1.000000000000000000, 0.8386467772024601697, 1.000000000000000000),
 ( 1.000000000000000000, 0.8308203150020515571, 1.000000000000000000),
 ( 1.000000000000000000, 0.8176719580059066406, 1.000000000000000000),
 ( 1.000000000000000000, 0.8130708599674437709, 1.000000000000000000),
 ( 1.000000000000000000, 0.8036702313420579502, 1.000000000000000000),
 ( 1.000000000000000000, 0.7988516037130688474, 1.000000000000000000),
 ( 1.000000000000000000, 0.7890840531758207543, 1.000000000000000000),
 ( 1.000000000000000000, 0.7841348415510249747, 1.000000000000000000),
 ( 1.000000000000000000, 0.7742194781316240615, 1.000000000000000000),
 ( 1.000000000000000000, 0.7692300867738712800, 1.000000000000000000),
 ( 1.000000000000000000, 0.7547027778490736916, 1.000000000000000000),
 ( 1.000000000000000000, 0.7455429868461489473, 1.000000000000000000),
 ( 1.000000000000000000, 0.7333839939153369292, 1.000000000000000000),
 ( 1.000000000000000000, 0.7295956578554230187, 1.000000000000000000),
 ( 1.000000000000000000, 0.7227015210647820265, 1.000000000000000000),
 ( 1.000000000000000000, 0.7196248032678934647, 1.000000000000000000),
 ( 1.000000000000000000, 0.7118099142936535895, 1.000000000000000000),
 ( 1.000000000000000000, 0.7084153614166502910, 1.000000000000000000),
 ( 1.000000000000000000, 0.7071067811865475727, 1.000000000000000000) ) ) 
 REPRESENTATION_ITEM ( '' )  SURFACE ( )  );
#65341=MECHANICAL_DESIGN_GEOMETRIC_PRESENTATION_REPRESENTATION('',(#24045),#18890);
#65356=DIRECTION ( 'NONE',  ( 0.000000000000000000, 0.000000000000000000, 1.000000000000000000 ) ) ;
#65361=CARTESIAN_POINT ( 'NONE',  ( -3.787335548950263142, -1.092153040502706896, 104.1352136098626318 ) ) ;
#65373=SURFACE_STYLE_FILL_AREA ( #66977 ) ;
#65409=CARTESIAN_POINT ( 'NONE',  ( 4.781335833249819700, -2.669875467129551705, 102.4226025779373401 ) ) ;
#65440=ADVANCED_FACE ( 'NONE', ( #43160, #18923 ), #19993, .T. ) ;
#65458=SURFACE_STYLE_FILL_AREA ( #32048 ) ;
#65492=DIRECTION ( 'NONE',  ( 0.000000000000000000, 1.000000000000000000, 0.000000000000000000 ) ) ;
#65540=CARTESIAN_POINT ( 'NONE',  ( 4.440267933154150803, -48.84299975118083381, 104.3849335852974605 ) ) ;
#65546=( LENGTH_UNIT ( ) NAMED_UNIT ( * ) SI_UNIT ( .MILLI., .METRE. ) );
#65556=CARTESIAN_POINT ( 'NONE',  ( 4.999999999999997335, -4.000000000000003553, 35.66025403784438197 ) ) ;
#65587=CARTESIAN_POINT ( 'NONE',  ( 1.769226153621908271, -70.08155570559151215, 13.10633261097420643 ) ) ;
#65589=ORIENTED_EDGE ( 'NONE', *, *, #23623, .T. ) ;
#65640=ORIENTED_EDGE ( 'NONE', *, *, #13081, .T. ) ;
#65641=( NAMED_UNIT ( * ) SI_UNIT ( $, .STERADIAN. ) SOLID_ANGLE_UNIT ( ) );
#65645=UNCERTAINTY_MEASURE_WITH_UNIT (LENGTH_MEASURE( 1.000000000000000082E-05 ), #94094, 'distance_accuracy_value', 'NONE');
#65677=UNCERTAINTY_MEASURE_WITH_UNIT (LENGTH_MEASURE( 1.000000000000000082E-05 ), #83082, 'distance_accuracy_value', 'NONE');
#65686=CARTESIAN_POINT ( 'NONE',  ( -4.681380154937285987, 0.7378729568060279354, 103.7259032015045079 ) ) ;
#65714=CARTESIAN_POINT ( 'NONE',  ( -6.009389902277268547, 3.157894738987889305, 14.66382285822740883 ) ) ;
#65733=CARTESIAN_POINT ( 'NONE',  ( -3.375199152497164068, -0.8899603717835512517, 104.1123137168933965 ) ) ;
#65738=ORIENTED_EDGE ( 'NONE', *, *, #95507, .T. ) ;
#65740=CARTESIAN_POINT ( 'NONE',  ( -5.000000000000000000, -13.85537367033497169, 10.16084852766932300 ) ) ;
#65759=CARTESIAN_POINT ( 'NONE',  ( 9.720957446278301717, -3.400539410478017555, 14.97579417183843020 ) ) ;
#65760=ORIENTED_EDGE ( 'NONE', *, *, #81985, .T. ) ;
#65791=FILL_AREA_STYLE_COLOUR ( '', #4031 ) ;
#65798=CARTESIAN_POINT ( 'NONE',  ( 9.498520115305538525, -51.35937410768142541, 30.13282173121349317 ) ) ;
#65822=CARTESIAN_POINT ( 'NONE',  ( -4.999999999999993783, -46.27603786271895814, 102.2532056551910387 ) ) ;
#65823=ADVANCED_FACE ( 'NONE', ( #49939, #7171 ), #22343, .T. ) ;
#65839=ORIENTED_EDGE ( 'NONE', *, *, #56454, .F. ) ;
#65875=ORIENTED_EDGE ( 'NONE', *, *, #76707, .F. ) ;
#65893=CARTESIAN_POINT ( 'NONE',  ( 15.43204163116762118, -5.423745131301086708, 13.99747994630663861 ) ) ;
#65899=CARTESIAN_POINT ( 'NONE',  ( -3.473068986402788383, -49.15491390339877142, 103.7454523020563499 ) ) ;
#65942=PRESENTATION_STYLE_ASSIGNMENT (( #97764 ) ) ;
#65973=DIRECTION ( 'NONE',  ( 0.000000000000000000, 1.224646799147352468E-16, 1.000000000000000000 ) ) ;
#65979=DIRECTION ( 'NONE',  ( 0.000000000000000000, 0.000000000000000000, 1.000000000000000000 ) ) ;
#65980=( LENGTH_UNIT ( ) NAMED_UNIT ( * ) SI_UNIT ( .MILLI., .METRE. ) );
#65991=CARTESIAN_POINT ( 'NONE',  ( -4.551587301587304957, -1.200583151104947843, 104.4018401814738155 ) ) ;
#65995=VERTEX_POINT ( 'NONE', #14973 ) ;
#66018=DIRECTION ( 'NONE',  ( 0.000000000000000000, -1.000000000000000000, -0.000000000000000000 ) ) ;
#66030=FACE_OUTER_BOUND ( 'NONE', #21868, .T. ) ;
#66057=CARTESIAN_POINT ( 'NONE',  ( -6.112161658498984629, -61.81941831950287281, 14.40466291265888188 ) ) ;
#66064=CARTESIAN_POINT ( 'NONE',  ( 3.713158817313909843, -48.94636994418067388, 103.2987150069879903 ) ) ;
#66082=DIRECTION ( 'NONE',  ( -0.8660254037844389297, -3.039937634619675546E-16, 0.4999999999999995004 ) ) ;
#66111=CARTESIAN_POINT ( 'NONE',  ( 6.125000000000095923, -15.62228920881129390, 14.41094225130415651 ) ) ;
#66115=CARTESIAN_POINT ( 'NONE',  ( 4.291829500544997344, -67.75856037000218635, 13.66196629111150607 ) ) ;
#66118=SURFACE_STYLE_USAGE ( .BOTH. , #16504 ) ;
#66143=CARTESIAN_POINT ( 'NONE',  ( 6.105464488512484245, -12.30761336975154308, 12.19688296867937538 ) ) ;
#66158=FILL_AREA_STYLE_COLOUR ( '', #56084 ) ;
#66162=CARTESIAN_POINT ( 'NONE',  ( 4.792515968931522430, -47.29776092521730391, 102.4138677444059766 ) ) ;
#66207=MECHANICAL_DESIGN_GEOMETRIC_PRESENTATION_REPRESENTATION('',(#48943),#33497);
#66244=AXIS2_PLACEMENT_3D ( 'NONE', #37733, #28566, #3738 ) ;
#66263=CARTESIAN_POINT ( 'NONE',  ( -6.019773438520521047, -12.68390881199314890, 12.80591459028008749 ) ) ;
#66297=FILL_AREA_STYLE_COLOUR ( '', #70325 ) ;
#66318=STYLED_ITEM ( 'NONE', ( #10746 ), #98816 ) ;
#66342=CARTESIAN_POINT ( 'NONE',  ( -9.000000000000001776, -4.000000000000003553, 42.58845726811989607 ) ) ;
#66354=CARTESIAN_POINT ( 'NONE',  ( 1.000000000000000000, -69.59657292934913642, 12.76848391599222765 ) ) ;
#66368=SURFACE_STYLE_USAGE ( .BOTH. , #18380 ) ;
#66408=( NAMED_UNIT ( * ) SI_UNIT ( $, .STERADIAN. ) SOLID_ANGLE_UNIT ( ) );
#66414=( NAMED_UNIT ( * ) SI_UNIT ( $, .STERADIAN. ) SOLID_ANGLE_UNIT ( ) );
#66426=CARTESIAN_POINT ( 'NONE',  ( -2.228836330358908047, -49.81523274736686346, 102.4817230975880449 ) ) ;
#66464=DIRECTION ( 'NONE',  ( 0.000000000000000000, 0.000000000000000000, 1.000000000000000000 ) ) ;
#66467=SURFACE_STYLE_FILL_AREA ( #49750 ) ;
#66526=CARTESIAN_POINT ( 'NONE',  ( -4.698242434196084893, -14.20142765657231543, -8.220922734484002348 ) ) ;
#66549=CARTESIAN_POINT ( 'NONE',  ( 3.352941176470599860, -1.200583151104954061, 104.5794940929807524 ) ) ;
#66555=VERTEX_POINT ( 'NONE', #27787 ) ;
#66568=FACE_BOUND ( 'NONE', #90531, .T. ) ;
#66575=FILL_AREA_STYLE ('',( #74650 ) ) ;
#66595=ORIENTED_EDGE ( 'NONE', *, *, #71867, .T. ) ;
#66622=ORIENTED_EDGE ( 'NONE', *, *, #30299, .T. ) ;
#66628=EDGE_CURVE ( 'NONE', #6033, #76952, #58005, .T. ) ;
#66649=ADVANCED_FACE ( 'NONE', ( #37463 ), #104522, .T. ) ;
#66653=CARTESIAN_POINT ( 'NONE',  ( 5.053417956347306728, -64.34077225747144269, 13.91206720744365910 ) ) ;
#66668=STYLED_ITEM ( 'NONE', ( #6391 ), #58033 ) ;
#66673=EDGE_LOOP ( 'NONE', ( #47211, #30011, #9977, #96666 ) ) ;
#66684=CARTESIAN_POINT ( 'NONE',  ( 5.000000000000040856, -12.61682532716497640, 11.58371340991119958 ) ) ;
#66709=UNCERTAINTY_MEASURE_WITH_UNIT (LENGTH_MEASURE( 1.000000000000000082E-05 ), #67286, 'distance_accuracy_value', 'NONE');
#66756=DIRECTION ( 'NONE',  ( 0.5166563581656273829, 0.4014477553983911151, 0.7562446080816871419 ) ) ;
#66801=ORIENTED_EDGE ( 'NONE', *, *, #18259, .F. ) ;
#66815=COLOUR_RGB ( '', 0.09019608, 0.27058824, 0.51372549) ;
#66838=PRESENTATION_STYLE_ASSIGNMENT (( #33966 ) ) ;
#66863=ORIENTED_EDGE ( 'NONE', *, *, #93290, .T. ) ;
#66868=DIRECTION ( 'NONE',  ( 1.000000000000000000, 0.000000000000000000, 0.000000000000000000 ) ) ;
#66887=EDGE_CURVE ( 'NONE', #27782, #21120, #63971, .T. ) ;
#66890=CARTESIAN_POINT ( 'NONE',  ( -6.148597574911479846, -3.030260368802259463E-15, 18.77664127325637011 ) ) ;
#66894=STYLED_ITEM ( 'NONE', ( #88179 ), #60953 ) ;
#66936=FACE_OUTER_BOUND ( 'NONE', #69755, .T. ) ;
#66946=CARTESIAN_POINT ( 'NONE',  ( -13.38090213880806800, -53.73814761577546051, 31.11721482942555994 ) ) ;
#66959=FILL_AREA_STYLE_COLOUR ( '', #95963 ) ;
#66972=CARTESIAN_POINT ( 'NONE',  ( 7.576662914407418015, -12.42162669466707570, 8.412646887033078613 ) ) ;
#66973=ADVANCED_FACE ( 'NONE', ( #17404 ), #101138, .T. ) ;
#66977=FILL_AREA_STYLE ('',( #26030 ) ) ;
#66993=CARTESIAN_POINT ( 'NONE',  ( 5.000000000000000000, -46.02075056256854424, 5.909823871114814331 ) ) ;
#67000=( GEOMETRIC_REPRESENTATION_CONTEXT ( 3 ) GLOBAL_UNCERTAINTY_ASSIGNED_CONTEXT ( ( #80788 ) ) GLOBAL_UNIT_ASSIGNED_CONTEXT ( ( #50578, #67854, #84581 ) ) REPRESENTATION_CONTEXT ( 'NONE', 'WORKASPACE' ) );
#67019=DIRECTION ( 'NONE',  ( 0.000000000000000000, 1.000000000000000000, 0.000000000000000000 ) ) ;
#67022=DIRECTION ( 'NONE',  ( 0.000000000000000000, 0.000000000000000000, -1.000000000000000000 ) ) ;
#67029=CARTESIAN_POINT ( 'NONE',  ( -5.000000000000000000, -66.75623614760699809, 15.74601422014960583 ) ) ;
#67065=CARTESIAN_POINT ( 'NONE',  ( 0.9999999999999997780, -32.36379547066533036, -3.982563152093286263 ) ) ;
#67068=CARTESIAN_POINT ( 'NONE',  ( -3.783418949173940504, -11.62946060510804180, -10.57964823094830464 ) ) ;
#67091=CARTESIAN_POINT ( 'NONE',  ( 1.570694327390588674, -0.05369876004218275545, 101.7856530012106759 ) ) ;
#67098=CARTESIAN_POINT ( 'NONE',  ( -4.073826509765688719, -48.95212347009508846, 104.5376934966490694 ) ) ;
#67109=DIRECTION ( 'NONE',  ( -0.000000000000000000, -0.000000000000000000, 1.000000000000000000 ) ) ;
#67139=( GEOMETRIC_REPRESENTATION_CONTEXT ( 3 ) GLOBAL_UNCERTAINTY_ASSIGNED_CONTEXT ( ( #83013 ) ) GLOBAL_UNIT_ASSIGNED_CONTEXT ( ( #44311, #68600, #51317 ) ) REPRESENTATION_CONTEXT ( 'NONE', 'WORKASPACE' ) );
#67160=B_SPLINE_CURVE_WITH_KNOTS ( 'NONE', 3,
 ( #49971, #75850, #7914, #82880, #8977, #73710, #34368, #1946, #41880, #65099, #97996, #24149, #847, #16015, #99579, #48895, #40817, #106614, #61823, #26810, #77452, #2481 ),
 .UNSPECIFIED., .F., .F.,
 ( 4, 2, 2, 2, 2, 2, 2, 2, 2, 2, 4 ),
 ( 2.161454313166970184E-17, 0.001055301598474675008, 0.001582952397712002537, 0.002110603196949330067, 0.002638253996186657596, 0.003165904795423985126, 0.004221206393898647991, 0.005276507992373309988, 0.006331809590847972853, 0.007387111189322636585, 0.008442412787797297716 ),
 .UNSPECIFIED. ) ;
#67169=CARTESIAN_POINT ( 'NONE',  ( -4.999999999999999112, -53.41520084899324416, 9.165069380062005777 ) ) ;
#67176=CARTESIAN_POINT ( 'NONE',  ( 1.957257541017970892, -49.88613852985599095, 44.76450653543791702 ) ) ;
#67197=CARTESIAN_POINT ( 'NONE',  ( 5.146676080590609104, -67.38655984587389014, 13.97995438629998155 ) ) ;
#67227=CARTESIAN_POINT ( 'NONE',  ( 5.000000000000000000, -14.43521912202222524, 12.17944458656167583 ) ) ;
#67234=PRODUCT_DEFINITION_CONTEXT ( 'detailed design', #72768, 'design' ) ;
#67261=VERTEX_POINT ( 'NONE', #3074 ) ;
#67286=( LENGTH_UNIT ( ) NAMED_UNIT ( * ) SI_UNIT ( .MILLI., .METRE. ) );
#67306=DIRECTION ( 'NONE',  ( 0.000000000000000000, 1.000000000000000000, 0.000000000000000000 ) ) ;
#67339=CARTESIAN_POINT ( 'NONE',  ( -3.910135399454920169, -1.060349490810097439, 104.5757312272370427 ) ) ;
#67342=VERTEX_POINT ( 'NONE', #62916 ) ;
#67365=CARTESIAN_POINT ( 'NONE',  ( 11.59943540149712504, -1.679055970110489460, 20.57194209593012957 ) ) ;
#67379=ORIENTED_EDGE ( 'NONE', *, *, #49507, .F. ) ;
#67411=DIRECTION ( 'NONE',  ( 0.05555555555555551084, 0.000000000000000000, -0.9984555975339683975 ) ) ;
#67418=( NAMED_UNIT ( * ) SI_UNIT ( $, .STERADIAN. ) SOLID_ANGLE_UNIT ( ) );
#67427=CARTESIAN_POINT ( 'NONE',  ( -8.390648120624151218, -0.1953587718301813270, 19.49430943995808008 ) ) ;
#67440=DIRECTION ( 'NONE',  ( 1.096832036894112098E-16, -0.000000000000000000, 1.000000000000000000 ) ) ;
#67444=CARTESIAN_POINT ( 'NONE',  ( -15.95159607370372967, -2.671900693682740080, 14.76216555840736255 ) ) ;
#67502=CARTESIAN_POINT ( 'NONE',  ( 9.778942110939100374, -12.74542388620636757, 16.96968632615047667 ) ) ;
#67509=CIRCLE ( 'NONE', #41702, 14.00000000000000178 ) ;
#67532=CARTESIAN_POINT ( 'NONE',  ( 1.993516955649288214, -49.88337200126083815, 102.1895970170251644 ) ) ;
#67542=UNCERTAINTY_MEASURE_WITH_UNIT (LENGTH_MEASURE( 1.000000000000000082E-05 ), #6910, 'distance_accuracy_value', 'NONE');
#67555=SURFACE_STYLE_USAGE ( .BOTH. , #10355 ) ;
#67598=CARTESIAN_POINT ( 'NONE',  ( 3.718188220751057926, -1.049015004457080957, 104.2423402216923733 ) ) ;
#67602=CARTESIAN_POINT ( 'NONE',  ( -14.31840793639504383, -7.983782706452587696, 12.70197556375779513 ) ) ;
#67603=CARTESIAN_POINT ( 'NONE',  ( -6.125000000000002665, -15.62228920881133654, 14.41094225130411211 ) ) ;
#67627=CIRCLE ( 'NONE', #53827, 11.00000000000001066 ) ;
#67646=DIRECTION ( 'NONE',  ( 0.000000000000000000, 0.000000000000000000, 1.000000000000000000 ) ) ;
#67675=CARTESIAN_POINT ( 'NONE',  ( 4.585277158900029626, -47.79285414227015139, 43.04040780539905597 ) ) ;
#67719=CARTESIAN_POINT ( 'NONE',  ( -1.560773912800800467, -49.96204304796045648, 101.5963399667048748 ) ) ;
#67721=CARTESIAN_POINT ( 'NONE',  ( 2.538204850144155866, -70.38324806241240594, 13.23000886114773422 ) ) ;
#67768=ORIENTED_EDGE ( 'NONE', *, *, #49451, .F. ) ;
#67777=EDGE_LOOP ( 'NONE', ( #29114, #12921, #54881, #97893, #4618, #105591 ) ) ;
#67787=ORIENTED_EDGE ( 'NONE', *, *, #37366, .F. ) ;
#67808=CARTESIAN_POINT ( 'NONE',  ( -4.999999999999993783, -4.000000000000003553, 102.2532056551910387 ) ) ;
#67822=CARTESIAN_POINT ( 'NONE',  ( 4.999999999999993783, -46.00000000000000000, 102.2532056551910387 ) ) ;
#67844=ADVANCED_FACE ( 'NONE', ( #35210 ), #62798, .T. ) ;
#67854=( NAMED_UNIT ( * ) PLANE_ANGLE_UNIT ( ) SI_UNIT ( $, .RADIAN. ) );
#67884=CARTESIAN_POINT ( 'NONE',  ( 9.877159628591359208, -2.620207910158452336, 15.38486787623552665 ) ) ;
#67914=CARTESIAN_POINT ( 'NONE',  ( 1.000000000000000000, -5.000000000000016875, -14.14213562373094746 ) ) ;
#67984=( LENGTH_UNIT ( ) NAMED_UNIT ( * ) SI_UNIT ( .MILLI., .METRE. ) );
#68008=ORIENTED_EDGE ( 'NONE', *, *, #103113, .F. ) ;
#68015=CARTESIAN_POINT ( 'NONE',  ( -3.365451957726517840, -0.9314134953371686620, 104.1992105446095422 ) ) ;
#68019=( GEOMETRIC_REPRESENTATION_CONTEXT ( 3 ) GLOBAL_UNCERTAINTY_ASSIGNED_CONTEXT ( ( #18990 ) ) GLOBAL_UNIT_ASSIGNED_CONTEXT ( ( #69023, #33743, #49353 ) ) REPRESENTATION_CONTEXT ( 'NONE', 'WORKASPACE' ) );
#68022=CARTESIAN_POINT ( 'NONE',  ( 7.372535033043513764, -14.99112640172484490, 15.08559782546382166 ) ) ;
#68046=CARTESIAN_POINT ( 'NONE',  ( 0.9999999999999940048, -50.00000000000000000, 101.0455488498966758 ) ) ;
#68052=DIRECTION ( 'NONE',  ( 0.000000000000000000, 1.000000000000000000, 0.000000000000000000 ) ) ;
#68057=B_SPLINE_CURVE_WITH_KNOTS ( 'NONE', 3,
 ( #103312, #21357, #103828, #101709, #77438, #102774, #45087, #77966, #29458, #19255, #93084, #52084, #53167, #84997, #62330, #4081 ),
 .UNSPECIFIED., .F., .F.,
 ( 4, 2, 2, 2, 2, 2, 2, 4 ),
 ( 0.000000000000000000, 0.001828028632607115985, 0.003656057265214231970, 0.005484085897821349039, 0.007312114530428463939, 0.01096817179564269808, 0.01279620042824981992, 0.01462422906085693829 ),
 .UNSPECIFIED. ) ;
#68065=ADVANCED_FACE ( 'NONE', ( #508 ), #33475, .F. ) ;
#68066=CARTESIAN_POINT ( 'NONE',  ( -3.866514940531297295, -1.181881931264997077, 103.9726926151897715 ) ) ;
#68074=MECHANICAL_DESIGN_GEOMETRIC_PRESENTATION_REPRESENTATION('',(#83602),#28535);
#68077=CARTESIAN_POINT ( 'NONE',  ( 5.385673916453011856, -2.602085213965210642E-15, 18.57417562100670949 ) ) ;
#68078=ORIENTED_EDGE ( 'NONE', *, *, #77516, .F. ) ;
#68081=( NAMED_UNIT ( * ) SI_UNIT ( $, .STERADIAN. ) SOLID_ANGLE_UNIT ( ) );
#68114=CARTESIAN_POINT ( 'NONE',  ( -5.000000000000000000, -15.63336956925501653, -6.409577599286857996 ) ) ;
#68120=CARTESIAN_POINT ( 'NONE',  ( -12.31099551388335556, -10.27527576804327936, 10.93729666877207585 ) ) ;
#68121=CARTESIAN_POINT ( 'NONE',  ( -5.973896061805169744, -13.10340519129065839, 13.28276905619559400 ) ) ;
#68122=CARTESIAN_POINT ( 'NONE',  ( 3.348006310196415480, -1.091696481258594975, 104.4601921234425390 ) ) ;
#68149=CARTESIAN_POINT ( 'NONE',  ( 1.057603710517943441, -3.557244269805818156E-15, 101.1178170116175181 ) ) ;
#68153=UNCERTAINTY_MEASURE_WITH_UNIT (LENGTH_MEASURE( 1.000000000000000082E-05 ), #106514, 'distance_accuracy_value', 'NONE');
#68155=FILL_AREA_STYLE_COLOUR ( '', #7600 ) ;
#68166=SURFACE_SIDE_STYLE ('',( #42286 ) ) ;
#68199=CARTESIAN_POINT ( 'NONE',  ( 2.041386142727035224, -49.95395470777400249, 40.93797071785119357 ) ) ;
#68207=AXIS2_PLACEMENT_3D ( 'NONE', #23609, #56461, #89392 ) ;
#68246=ORIENTED_EDGE ( 'NONE', *, *, #32033, .T. ) ;
#68256=B_SPLINE_CURVE_WITH_KNOTS ( 'NONE', 3,
 ( #89410, #17116, #73185, #16033, #7934, #98539, #74265, #14960, #340, #73730, #49992, #16572, #106091, #33308, #41375, #40313 ),
 .UNSPECIFIED., .F., .F.,
 ( 4, 2, 2, 2, 2, 2, 2, 4 ),
 ( -2.482109357202701380E-05, 0.001810221378381205153, 0.003645263850334437561, 0.007315348794240897172, 0.009150391266194126544, 0.01098543373814735505, 0.01282047621010058355, 0.01465551868205381206 ),
 .UNSPECIFIED. ) ;
#68261=ADVANCED_FACE ( 'NONE', ( #85197 ), #13938, .T. ) ;
#68284=CARTESIAN_POINT ( 'NONE',  ( 4.999999999999960032, -13.06782935463053796, 12.36551185560477784 ) ) ;
#68286=ORIENTED_EDGE ( 'NONE', *, *, #83882, .F. ) ;
#68301=CARTESIAN_POINT ( 'NONE',  ( -13.45079846400082957, -54.26579227026637398, 23.11721482942554573 ) ) ;
#68306=CARTESIAN_POINT ( 'NONE',  ( 30.00000000000000000, 0.000000000000000000, 0.000000000000000000 ) ) ;
#68335=ORIENTED_EDGE ( 'NONE', *, *, #98698, .F. ) ;
#68340=DIRECTION ( 'NONE',  ( -1.000000000000000000, 0.000000000000000000, 0.000000000000000000 ) ) ;
#68368=STYLED_ITEM ( 'NONE', ( #45059 ), #59647 ) ;
#68435=CARTESIAN_POINT ( 'NONE',  ( 3.769311339736628241, -48.92514534113568914, 104.1674216685381396 ) ) ;
#68454=AXIS2_PLACEMENT_3D ( 'NONE', #2427, #101133, #27293 ) ;
#68481=SURFACE_STYLE_USAGE ( .BOTH. , #77627 ) ;
#68482=( GEOMETRIC_REPRESENTATION_CONTEXT ( 3 ) GLOBAL_UNCERTAINTY_ASSIGNED_CONTEXT ( ( #75304 ) ) GLOBAL_UNIT_ASSIGNED_CONTEXT ( ( #42, #8171, #66408 ) ) REPRESENTATION_CONTEXT ( 'NONE', 'WORKASPACE' ) );
#68515=CARTESIAN_POINT ( 'NONE',  ( -1.000000000001115108, -52.55160771104127093, 2.953793101315682623 ) ) ;
#68525=STYLED_ITEM ( 'NONE', ( #30865 ), #59131 ) ;
#68526=SURFACE_STYLE_FILL_AREA ( #2158 ) ;
#68541=EDGE_LOOP ( 'NONE', ( #65640, #70988, #21053, #66801 ) ) ;
#68550=CARTESIAN_POINT ( 'NONE',  ( -5.000000000000000000, -14.29967096554028849, 12.05652987285084343 ) ) ;
#68567=CARTESIAN_POINT ( 'NONE',  ( -3.753470829068492165, -1.089309597783810757, 104.5911851069063374 ) ) ;
#68583=DIRECTION ( 'NONE',  ( 0.000000000000000000, 1.000000000000000000, 0.000000000000000000 ) ) ;
#68600=( NAMED_UNIT ( * ) PLANE_ANGLE_UNIT ( ) SI_UNIT ( $, .RADIAN. ) );
#68608=AXIS2_PLACEMENT_3D ( 'NONE', #21878, #100754, #84594 ) ;
#68616=EDGE_CURVE ( 'NONE', #82136, #214, #41079, .T. ) ;
#68632=CARTESIAN_POINT ( 'NONE',  ( 9.241465400471236435, -0.3878019662490226893, 19.78591767756827124 ) ) ;
#68636=CARTESIAN_POINT ( 'NONE',  ( -5.000000000000000888, -70.02685735654881682, 13.01550610203317682 ) ) ;
#68651=AXIS2_PLACEMENT_3D ( 'NONE', #42090, #74449, #17842 ) ;
#68655=STYLED_ITEM ( 'NONE', ( #91398 ), #2790 ) ;
#68670=CARTESIAN_POINT ( 'NONE',  ( 1.000000000000000222, -5.000000000000000000, -14.14213562373095101 ) ) ;
#68674=CARTESIAN_POINT ( 'NONE',  ( -15.69541548456635915, -4.397703964512687413, 14.35461870892897629 ) ) ;
#68682=ORIENTED_EDGE ( 'NONE', *, *, #10578, .F. ) ;
#68689=CARTESIAN_POINT ( 'NONE',  ( 14.46849319673338918, -7.726810110884599681, 12.86012526411075463 ) ) ;
#68703=CARTESIAN_POINT ( 'NONE',  ( 3.454253436624921569, -49.15858197120396511, 103.7259032015043090 ) ) ;
#68708=CARTESIAN_POINT ( 'NONE',  ( 0.000000000000000000, -48.79941684889506348, 120.8571428571428612 ) ) ;
#68733=CIRCLE ( 'NONE', #32553, 2.000000000000001776 ) ;
#68747=( NAMED_UNIT ( * ) SI_UNIT ( $, .STERADIAN. ) SOLID_ANGLE_UNIT ( ) );
#68748=MECHANICAL_DESIGN_GEOMETRIC_PRESENTATION_REPRESENTATION('',(#94619),#80793);
#68755=CARTESIAN_POINT ( 'NONE',  ( 6.794369677605540225, -48.10722477442604372, 39.24113341299863578 ) ) ;
#68776=CARTESIAN_POINT ( 'NONE',  ( -3.443402964575895009, -49.16961384600919871, 44.01147765779307264 ) ) ;
#68843=CARTESIAN_POINT ( 'NONE',  ( -13.44288011066907096, -55.29289060621445628, 30.91149535780206747 ) ) ;
#68847=CARTESIAN_POINT ( 'NONE',  ( 12.23997345424373506, -2.653384265557077626, 20.68770798023725987 ) ) ;
#68860=ORIENTED_EDGE ( 'NONE', *, *, #103803, .T. ) ;
#68905=CARTESIAN_POINT ( 'NONE',  ( 5.000000000000000000, -13.82968113844978220, 11.07308787588975285 ) ) ;
#68912=CARTESIAN_POINT ( 'NONE',  ( 6.966966640339024686, -46.95039021837323645, 39.14360059807137304 ) ) ;
#68931=LINE ( 'NONE', #14364, #92974 ) ;
#68939=B_SPLINE_CURVE_WITH_KNOTS ( 'NONE', 3,
 ( #73137, #41854, #98489, #82313, #88818, #14913, #40792, #55883, #49943, #81236 ),
 .UNSPECIFIED., .F., .F.,
 ( 4, 2, 2, 2, 4 ),
 ( 0.000000000000000000, 0.0008124082233778996513, 0.001624816446755799303, 0.002437224670133698954, 0.003249632893511598605 ),
 .UNSPECIFIED. ) ;
#68941=ORIENTED_EDGE ( 'NONE', *, *, #1640, .F. ) ;
#68948=CARTESIAN_POINT ( 'NONE',  ( 0.000000000000000000, -54.00000000000000711, 27.00000000000000000 ) ) ;
#68970=SURFACE_STYLE_FILL_AREA ( #3156 ) ;
#68996=CARTESIAN_POINT ( 'NONE',  ( 6.934100574218750701, -13.60622170955989141, -6.341742298311421777 ) ) ;
#69023=( LENGTH_UNIT ( ) NAMED_UNIT ( * ) SI_UNIT ( .MILLI., .METRE. ) );
#69042=( LENGTH_UNIT ( ) NAMED_UNIT ( * ) SI_UNIT ( .MILLI., .METRE. ) );
#69052=ORIENTED_EDGE ( 'NONE', *, *, #15917, .T. ) ;
#69064=CARTESIAN_POINT ( 'NONE',  ( 15.90614609307868399, -3.157894736842107530, 14.66382285868950675 ) ) ;
#69080=CARTESIAN_POINT ( 'NONE',  ( -13.38886880393120116, -53.47610516573492845, 31.09159242423791270 ) ) ;
#69096=CARTESIAN_POINT ( 'NONE',  ( -3.534854069000198162, -1.070477528868992723, 104.4405781011824956 ) ) ;
#69113=CARTESIAN_POINT ( 'NONE',  ( -6.999999999999993783, -4.000000000000003553, 102.2532056551910387 ) ) ;
#69157=CARTESIAN_POINT ( 'NONE',  ( 7.477168027001042994, -0.5783290275783404821, 15.45228033502481146 ) ) ;
#69192=SURFACE_STYLE_FILL_AREA ( #52441 ) ;
#69205=CARTESIAN_POINT ( 'NONE',  ( -6.022743854525172580, -12.63762613047084571, 12.76172509297431468 ) ) ;
#69219=CARTESIAN_POINT ( 'NONE',  ( 13.95281146043403098, -57.79492310796621979, 25.82616780902253950 ) ) ;
#69237=EDGE_LOOP ( 'NONE', ( #3674, #78122, #89596, #103081, #16479 ) ) ;
#69251=ORIENTED_EDGE ( 'NONE', *, *, #42893, .F. ) ;
#69283=CARTESIAN_POINT ( 'NONE',  ( 4.461741436590552112, -48.02090051515271796, 43.16544567096210017 ) ) ;
#69286=B_SPLINE_CURVE_WITH_KNOTS ( 'NONE', 3,
 ( #33250, #41844, #98481, #57480, #24109, #33784, #89873, #90406, #15980, #48333, #99000, #7873 ),
 .UNSPECIFIED., .F., .F.,
 ( 4, 2, 2, 2, 2, 4 ),
 ( 0.000000000000000000, 0.0008247946606697752940, 0.001649589321339550588, 0.002061986651674447071, 0.002474383982009343771, 0.003299178642679118957 ),
 .UNSPECIFIED. ) ;
#69287=ORIENTED_EDGE ( 'NONE', *, *, #89266, .T. ) ;
#69304=CARTESIAN_POINT ( 'NONE',  ( -3.913636579744179667, -52.92916190526523934, 40.44644374621901051 ) ) ;
#69320=AXIS2_PLACEMENT_3D ( 'NONE', #20522, #77094, #3214 ) ;
#69360=DIRECTION ( 'NONE',  ( 0.000000000000000000, 0.000000000000000000, -1.000000000000000000 ) ) ;
#69369=CARTESIAN_POINT ( 'NONE',  ( -13.49952125780149714, -55.77501631020759021, 30.71129996282902397 ) ) ;
#69417=DIRECTION ( 'NONE',  ( -1.000000000000000000, 0.000000000000000000, 0.000000000000000000 ) ) ;
#69495=CARTESIAN_POINT ( 'NONE',  ( 3.355892750373768774, -49.00480196350148532, 104.3125661743350179 ) ) ;
#69519=CARTESIAN_POINT ( 'NONE',  ( 5.000000000000000000, -15.93202192939576989, -5.930487099830195952 ) ) ;
#69543=ORIENTED_EDGE ( 'NONE', *, *, #16832, .T. ) ;
#69554=CARTESIAN_POINT ( 'NONE',  ( 3.052800042147856718, -0.8437115306431165473, 104.0321489743691927 ) ) ;
#69560=EDGE_CURVE ( 'NONE', #170, #38295, #60285, .T. ) ;
#69569=CARTESIAN_POINT ( 'NONE',  ( -15.88481125434442909, -1.943298766509323316, 14.87559245782164119 ) ) ;
#69572=( GEOMETRIC_REPRESENTATION_CONTEXT ( 3 ) GLOBAL_UNCERTAINTY_ASSIGNED_CONTEXT ( ( #84747 ) ) GLOBAL_UNIT_ASSIGNED_CONTEXT ( ( #70043, #45770, #4784 ) ) REPRESENTATION_CONTEXT ( 'NONE', 'WORKASPACE' ) );
#69578=CARTESIAN_POINT ( 'NONE',  ( -1.000000000001115108, -5.000000000000000000, -14.14213562373095101 ) ) ;
#69589=CARTESIAN_POINT ( 'NONE',  ( -3.714954396655790969, -48.94453733868888889, 103.2971887958219952 ) ) ;
#69603=CARTESIAN_POINT ( 'NONE',  ( 4.999999999999995559, 0.000000000000000000, 42.58845726811989607 ) ) ;
#69625=CARTESIAN_POINT ( 'NONE',  ( -1.000000000000000000, -69.59657292933731298, 12.76848391598547394 ) ) ;
#69631=EDGE_CURVE ( 'NONE', #63106, #14235, #68931, .T. ) ;
#69666=CARTESIAN_POINT ( 'NONE',  ( -27.99999999999999645, 0.000000000000000000, 9.000000000000000000 ) ) ;
#69671=DIRECTION ( 'NONE',  ( 1.224646799147352468E-16, 0.000000000000000000, -1.000000000000000000 ) ) ;
#69674=CARTESIAN_POINT ( 'NONE',  ( 9.699093171307941574, 2.767019883226315091, 14.74275178253622265 ) ) ;
#69675=EDGE_CURVE ( 'NONE', #88866, #34973, #41232, .T. ) ;
#69685=B_SPLINE_CURVE_WITH_KNOTS ( 'NONE', 3,
 ( #19554, #52391, #11389, #106237, #14047, #105718, #47479, #16180, #39940, #23241, #14573, #79851, #7543, #55035, #65269, #90073, #89021, #39420, #48004, #30814, #104662, #56079, #64228, #97617, #5446, #6489, #63700, #87967, #40459, #46951, #98159, #81429, #80377, #72295 ),
 .UNSPECIFIED., .F., .F.,
 ( 4, 2, 2, 2, 2, 2, 2, 2, 2, 2, 2, 2, 2, 2, 2, 2, 4 ),
 ( 0.01263964810480761557, 0.01342907106096845327, 0.01421849401712929097, 0.01500791697329012866, 0.01579733992945096810, 0.01658676288561180406, 0.01737618584177264350, 0.01816560879793347946, 0.01895503175409431890, 0.01974445471025515486, 0.02053387766641599430, 0.02132330062257683373, 0.02211272357873766969, 0.02290214653489850566, 0.02369156949105934509, 0.02448099244722018453, 0.02527041540338102049 ),
 .UNSPECIFIED. ) ;
#69688=DIRECTION ( 'NONE',  ( 0.000000000000000000, 1.000000000000000000, -1.224646799147353207E-16 ) ) ;
#69737=CARTESIAN_POINT ( 'NONE',  ( 5.833333333333329485, -46.00000000000000000, 103.8776713793258608 ) ) ;
#69740=ORIENTED_EDGE ( 'NONE', *, *, #33526, .F. ) ;
#69755=EDGE_LOOP ( 'NONE', ( #65760, #9883, #63359, #93416 ) ) ;
#69756=CARTESIAN_POINT ( 'NONE',  ( 5.164787682159539983, -1.887557197826887689, 104.1470044518085416 ) ) ;
#69764=( NAMED_UNIT ( * ) SI_UNIT ( $, .STERADIAN. ) SOLID_ANGLE_UNIT ( ) );
#69768=AXIS2_PLACEMENT_3D ( 'NONE', #20334, #53180, #15891 ) ;
#69778=STYLED_ITEM ( 'NONE', ( #27931 ), #13402 ) ;
#69784=CARTESIAN_POINT ( 'NONE',  ( -9.677525045153895888, -57.01317935973843731, 24.47381311117452185 ) ) ;
#69798=CARTESIAN_POINT ( 'NONE',  ( 2.800738256643207524, -53.57001856701707965, 40.71845537227009970 ) ) ;
#69802=EDGE_CURVE ( 'NONE', #12254, #42044, #48147, .T. ) ;
#69816=CARTESIAN_POINT ( 'NONE',  ( -12.37144696128342147, -4.000000000000003553, 20.44658103856077602 ) ) ;
#69818=CARTESIAN_POINT ( 'NONE',  ( -5.715067606001751344, -50.89645767963700251, 39.78281718566972103 ) ) ;
#69905=ORIENTED_EDGE ( 'NONE', *, *, #64251, .F. ) ;
#69925=AXIS2_PLACEMENT_3D ( 'NONE', #68948, #36605, #94275 ) ;
#69926=AXIS2_PLACEMENT_3D ( 'NONE', #80439, #4982, #55615 ) ;
#69959=CARTESIAN_POINT ( 'NONE',  ( 4.869591400170317996, -52.05062436006488724, 40.13051080525804792 ) ) ;
#69962=SURFACE_STYLE_USAGE ( .BOTH. , #62412 ) ;
#69981=STYLED_ITEM ( 'NONE', ( #94563 ), #57123 ) ;
#70017=CARTESIAN_POINT ( 'NONE',  ( -12.37144696128342147, -3.999999999999995559, 20.44658103856077602 ) ) ;
#70043=( LENGTH_UNIT ( ) NAMED_UNIT ( * ) SI_UNIT ( .MILLI., .METRE. ) );
#70061=AXIS2_PLACEMENT_3D ( 'NONE', #50855, #92922, #77282 ) ;
#70068=SURFACE_STYLE_FILL_AREA ( #45275 ) ;
#70077=CARTESIAN_POINT ( 'NONE',  ( 2.806188179629237833, -0.4213828545325281616, 102.9366787940491719 ) ) ;
#70089=CARTESIAN_POINT ( 'NONE',  ( -12.03429798983160914, 2.041993617203186506, 14.86077952815172054 ) ) ;
#70118=CARTESIAN_POINT ( 'NONE',  ( -4.107027841300135762, -69.23752800445994637, 13.61032178755603361 ) ) ;
#70119=FACE_OUTER_BOUND ( 'NONE', #81972, .T. ) ;
#70148=COLOUR_RGB ( '', 0.31764706, 0.68627451, 0.89019608) ;
#70200=EDGE_CURVE ( 'NONE', #40622, #11109, #99895, .T. ) ;
#70213=CIRCLE ( 'NONE', #68454, 4.000000000000000000 ) ;
#70224=EDGE_CURVE ( 'NONE', #87124, #80842, #58564, .T. ) ;
#70227=AXIS2_PLACEMENT_3D ( 'NONE', #56664, #74441, #7576 ) ;
#70240=AXIS2_PLACEMENT_3D ( 'NONE', #11497, #19663, #27210 ) ;
#70280=CARTESIAN_POINT ( 'NONE',  ( 5.000000000000000888, -64.69017754626541716, 10.12118620290157978 ) ) ;
#70283=DIRECTION ( 'NONE',  ( 1.000000000000000000, -0.000000000000000000, -0.000000000000000000 ) ) ;
#70288=( NAMED_UNIT ( * ) SI_UNIT ( $, .STERADIAN. ) SOLID_ANGLE_UNIT ( ) );
#70304=( NAMED_UNIT ( * ) SI_UNIT ( $, .STERADIAN. ) SOLID_ANGLE_UNIT ( ) );
#70325=COLOUR_RGB ( '', 0.09019608, 0.27058824, 0.51372549) ;
#70352=CARTESIAN_POINT ( 'NONE',  ( -1.341815878753393809, -50.03007620914304709, 40.96301477866974494 ) ) ;
#70400=UNCERTAINTY_MEASURE_WITH_UNIT (LENGTH_MEASURE( 1.000000000000000082E-05 ), #16557, 'distance_accuracy_value', 'NONE');
#70441=ORIENTED_EDGE ( 'NONE', *, *, #77644, .F. ) ;
#70448=CARTESIAN_POINT ( 'NONE',  ( -1.964652754746246677, -70.01532877525617948, 13.13671012408558347 ) ) ;
#70484=CARTESIAN_POINT ( 'NONE',  ( 13.45844672282477816, -53.47313501769576050, 23.14344092887451154 ) ) ;
#70488=COLOUR_RGB ( '', 0.09019608, 0.27058824, 0.51372549) ;
#70498=CARTESIAN_POINT ( 'NONE',  ( 3.454253436624935336, -0.8414180287960453253, 103.7259032015043232 ) ) ;
#70500=CARTESIAN_POINT ( 'NONE',  ( 0.2878250504871184279, -70.51393066051385006, 12.99060018351242540 ) ) ;
#70553=DIRECTION ( 'NONE',  ( 0.000000000000000000, 0.000000000000000000, 1.000000000000000000 ) ) ;
#70555=CARTESIAN_POINT ( 'NONE',  ( -5.893532595998363099, -15.73385846051533044, 14.28825528099932818 ) ) ;
#70558=PRESENTATION_STYLE_ASSIGNMENT (( #76503 ) ) ;
#70559=CARTESIAN_POINT ( 'NONE',  ( -1.444753424442138723, -6.061373582658561077, -13.74655991887425088 ) ) ;
#70624=CARTESIAN_POINT ( 'NONE',  ( -9.720412966709314873, -3.400720061511772307, 14.97537720455055421 ) ) ;
#70641=CARTESIAN_POINT ( 'NONE',  ( 0.000000000000000000, -4.000000000000003553, 118.0000000000000000 ) ) ;
#70656=CARTESIAN_POINT ( 'NONE',  ( 1.889565883275343694, -49.90613408882943247, 101.9317875358934486 ) ) ;
#70677=FILL_AREA_STYLE_COLOUR ( '', #52937 ) ;
#70688=CIRCLE ( 'NONE', #24205, 18.00000000000000000 ) ;
#70710=CARTESIAN_POINT ( 'NONE',  ( 3.214365674769854575, -48.98477521967217285, 104.3190434908433559 ) ) ;
#70729=CARTESIAN_POINT ( 'NONE',  ( -30.00000000000000000, 0.000000000000000000, 0.000000000000000000 ) ) ;
#70735=CARTESIAN_POINT ( 'NONE',  ( -5.000000000000000000, -8.792118119421601818, -8.558778717960986882 ) ) ;
#70745=ORIENTED_EDGE ( 'NONE', *, *, #27257, .F. ) ;
#70775=CARTESIAN_POINT ( 'NONE',  ( 1.000000000000000000, -64.45248229067139789, 10.00070197187728738 ) ) ;
#70779=PRESENTATION_STYLE_ASSIGNMENT (( #21725 ) ) ;
#70806=CARTESIAN_POINT ( 'NONE',  ( 5.000000000000000000, -41.55966127977662694, 4.049904920148556187 ) ) ;
#70827=( LENGTH_UNIT ( ) NAMED_UNIT ( * ) SI_UNIT ( .MILLI., .METRE. ) );
#70830=CARTESIAN_POINT ( 'NONE',  ( -1.558121094280061403, -49.97010080782105490, 44.88317974245237707 ) ) ;
#70948=CARTESIAN_POINT ( 'NONE',  ( -4.919733272805022928, -48.43781863848563773, 104.2477112191710802 ) ) ;
#70951=CARTESIAN_POINT ( 'NONE',  ( 14.91858118607497374, 2.271260765197548532E-16, 15.00000000000000000 ) ) ;
#70988=ORIENTED_EDGE ( 'NONE', *, *, #2312, .F. ) ;
#70999=SURFACE_SIDE_STYLE ('',( #88317 ) ) ;
#71003=CARTESIAN_POINT ( 'NONE',  ( 5.000000000000000000, -14.43154361897128091, 12.18621392300911133 ) ) ;
#71016=FILL_AREA_STYLE_COLOUR ( '', #87315 ) ;
#71019=EDGE_CURVE ( 'NONE', #86174, #56691, #5140, .T. ) ;
#71042=CARTESIAN_POINT ( 'NONE',  ( -5.688569873206696492, -2.951204850235074062, 103.9352763293502733 ) ) ;
#71044=ORIENTED_EDGE ( 'NONE', *, *, #14502, .T. ) ;
#71071=SURFACE_STYLE_FILL_AREA ( #37691 ) ;
#71130=CARTESIAN_POINT ( 'NONE',  ( 0.9999999999999941158, -1.734723475976807094E-15, 101.0455488498966758 ) ) ;
#71132=DIRECTION ( 'NONE',  ( 0.000000000000000000, 0.000000000000000000, -1.000000000000000000 ) ) ;
#71136=DIRECTION ( 'NONE',  ( -0.000000000000000000, -1.000000000000000000, -0.000000000000000000 ) ) ;
#71144=CARTESIAN_POINT ( 'NONE',  ( -11.22550744430827407, -1.339777127611723628, 20.46120208494560089 ) ) ;
#71170=FILL_AREA_STYLE ('',( #96525 ) ) ;
#71200=CARTESIAN_POINT ( 'NONE',  ( 4.284822031654949015, -48.90716638558772900, 104.4267991316944943 ) ) ;
#71217=CARTESIAN_POINT ( 'NONE',  ( 5.385673916453011856, 3.157894736842104866, 14.66382285868950675 ) ) ;
#71279=CARTESIAN_POINT ( 'NONE',  ( -7.000000000000000000, -15.62228920881133298, 12.61250543006184088 ) ) ;
#71280=SURFACE_STYLE_USAGE ( .BOTH. , #96630 ) ;
#71284=CIRCLE ( 'NONE', #23045, 2.000000000000000000 ) ;
#71285=SURFACE_STYLE_FILL_AREA ( #38422 ) ;
#71294=ORIENTED_EDGE ( 'NONE', *, *, #58322, .F. ) ;
#71311=CARTESIAN_POINT ( 'NONE',  ( 13.49954484221011519, -55.77516891766431684, 30.71121296612578888 ) ) ;
#71326=SURFACE_STYLE_USAGE ( .BOTH. , #62214 ) ;
#71378=FILL_AREA_STYLE ('',( #55189 ) ) ;
#71389=CARTESIAN_POINT ( 'NONE',  ( -8.084562802546505722, -14.50028042835467978, 15.55702922181462000 ) ) ;
#71436=COLOUR_RGB ( '', 0.66274510, 0.83137255, 0.94901961) ;
#71466=CARTESIAN_POINT ( 'NONE',  ( 8.835895239905601883, 2.942464897321981798, 14.70886157470553712 ) ) ;
#71486=PRESENTATION_STYLE_ASSIGNMENT (( #78001 ) ) ;
#71488=LINE ( 'NONE', #106506, #100998 ) ;
#71495=PRESENTATION_STYLE_ASSIGNMENT (( #7286 ) ) ;
#71499=VERTEX_POINT ( 'NONE', #14661 ) ;
#71521=CARTESIAN_POINT ( 'NONE',  ( 13.53382989543471560, -51.99084025137695875, 30.58576288564093915 ) ) ;
#71533=CARTESIAN_POINT ( 'NONE',  ( 3.704240196697786924, -1.051219065192640079, 103.3230214382351022 ) ) ;
#71559=CARTESIAN_POINT ( 'NONE',  ( -4.051286199644067665, -1.398729870307594769, 103.8758286790404810 ) ) ;
#71569=CARTESIAN_POINT ( 'NONE',  ( 5.000000000000000000, -13.79684580107986314, 10.70524563036420673 ) ) ;
#71582=AXIS2_PLACEMENT_3D ( 'NONE', #21247, #61146, #44972 ) ;
#71590=CARTESIAN_POINT ( 'NONE',  ( -11.63039212333523231, -10.74677606290342524, 10.46692874658227979 ) ) ;
#71609=VERTEX_POINT ( 'NONE', #73434 ) ;
#71622=CARTESIAN_POINT ( 'NONE',  ( 1.561520857470387602, -0.03805639397032387072, 101.5970913444665911 ) ) ;
#71662=CARTESIAN_POINT ( 'NONE',  ( -9.885149946167103963, -3.299727015031442168, 15.11772029901440462 ) ) ;
#71671=ORIENTED_EDGE ( 'NONE', *, *, #85921, .F. ) ;
#71684=ORIENTED_EDGE ( 'NONE', *, *, #5716, .F. ) ;
#71688=CARTESIAN_POINT ( 'NONE',  ( -5.000000000000000000, -14.21727251090714361, 9.320362779988990098 ) ) ;
#71707=( GEOMETRIC_REPRESENTATION_CONTEXT ( 3 ) GLOBAL_UNCERTAINTY_ASSIGNED_CONTEXT ( ( #36482 ) ) GLOBAL_UNIT_ASSIGNED_CONTEXT ( ( #97775, #48157, #47100 ) ) REPRESENTATION_CONTEXT ( 'NONE', 'WORKASPACE' ) );
#71721=ORIENTED_EDGE ( 'NONE', *, *, #52085, .T. ) ;
#71728=ORIENTED_EDGE ( 'NONE', *, *, #72017, .F. ) ;
#71738=CIRCLE ( 'NONE', #70061, 4.000000000000000000 ) ;
#71750=DIRECTION ( 'NONE',  ( 0.000000000000000000, 1.000000000000000000, 0.000000000000000000 ) ) ;
#71801=CARTESIAN_POINT ( 'NONE',  ( -1.509171067931242671, -0.02491874495535326833, 101.6143504438094851 ) ) ;
#71814=EDGE_CURVE ( 'NONE', #93762, #43590, #76628, .T. ) ;
#71820=( GEOMETRIC_REPRESENTATION_CONTEXT ( 3 ) GLOBAL_UNCERTAINTY_ASSIGNED_CONTEXT ( ( #80343 ) ) GLOBAL_UNIT_ASSIGNED_CONTEXT ( ( #92908, #84829, #43827 ) ) REPRESENTATION_CONTEXT ( 'NONE', 'WORKASPACE' ) );
#71832=ORIENTED_EDGE ( 'NONE', *, *, #99818, .F. ) ;
#71851=CARTESIAN_POINT ( 'NONE',  ( 5.000000000000000000, -61.56619815149595354, 13.02652999465270511 ) ) ;
#71860=CARTESIAN_POINT ( 'NONE',  ( -5.385673916453011856, 3.157894736842104866, 14.66382285868950675 ) ) ;
#71867=EDGE_CURVE ( 'NONE', #42316, #88009, #105728, .T. ) ;
#71909=ORIENTED_EDGE ( 'NONE', *, *, #7797, .T. ) ;
#71920=PRESENTATION_STYLE_ASSIGNMENT (( #105353 ) ) ;
#71934=CARTESIAN_POINT ( 'NONE',  ( -12.24528424494010714, -5.249243268855193989, 20.21143042290738734 ) ) ;
#71936=CARTESIAN_POINT ( 'NONE',  ( -4.955398898941148822, -46.70857795648188926, 40.29592611768291022 ) ) ;
#71955=EDGE_CURVE ( 'NONE', #71499, #13645, #67160, .T. ) ;
#71994=TOROIDAL_SURFACE ( 'NONE', #25537, 10.00000000000000000, 4.000000000000000000 ) ;
#72004=UNCERTAINTY_MEASURE_WITH_UNIT (LENGTH_MEASURE( 1.000000000000000082E-05 ), #64316, 'distance_accuracy_value', 'NONE');
#72011=CARTESIAN_POINT ( 'NONE',  ( 5.385673916453011856, 3.157894736842104866, 14.66382285868950675 ) ) ;
#72017=EDGE_CURVE ( 'NONE', #56114, #88353, #56819, .T. ) ;
#72076=CARTESIAN_POINT ( 'NONE',  ( 0.8750000000000039968, -70.58759490697437400, 13.02737050516259210 ) ) ;
#72102=CARTESIAN_POINT ( 'NONE',  ( -5.374793246923815992, -2.224716758540647099, 104.0614974883207111 ) ) ;
#72112=CARTESIAN_POINT ( 'NONE',  ( 5.000000000000000000, -13.82147230827996331, 10.98112731479300308 ) ) ;
#72130=PRESENTATION_STYLE_ASSIGNMENT (( #73167 ) ) ;
#72134=CARTESIAN_POINT ( 'NONE',  ( -9.475162301762221517, -11.83642075861501830, 9.220471602222437113 ) ) ;
#72167=FACE_OUTER_BOUND ( 'NONE', #26172, .T. ) ;
#72177=UNCERTAINTY_MEASURE_WITH_UNIT (LENGTH_MEASURE( 1.000000000000000082E-05 ), #23153, 'distance_accuracy_value', 'NONE');
#72205=( NAMED_UNIT ( * ) SI_UNIT ( $, .STERADIAN. ) SOLID_ANGLE_UNIT ( ) );
#72210=ORIENTED_EDGE ( 'NONE', *, *, #88339, .F. ) ;
#72211=SURFACE_STYLE_USAGE ( .BOTH. , #64144 ) ;
#72218=STYLED_ITEM ( 'NONE', ( #9068 ), #45217 ) ;
#72222=( NAMED_UNIT ( * ) SI_UNIT ( $, .STERADIAN. ) SOLID_ANGLE_UNIT ( ) );
#72236=CARTESIAN_POINT ( 'NONE',  ( -5.000000000000000000, -14.30429124282216513, 12.05126107871866026 ) ) ;
#72295=CARTESIAN_POINT ( 'NONE',  ( -9.215420734788356327, -54.00000000000001421, 23.11721482942554928 ) ) ;
#72305=ORIENTED_EDGE ( 'NONE', *, *, #88339, .T. ) ;
#72347=CARTESIAN_POINT ( 'NONE',  ( -2.067305840858484345, -0.1358350450447191882, 102.1177254334556892 ) ) ;
#72352=CARTESIAN_POINT ( 'NONE',  ( -12.53073535838927910, 1.820007232887559612, 14.89064316150549594 ) ) ;
#72387=CARTESIAN_POINT ( 'NONE',  ( 5.000000000000000000, -54.97504912987177050, 9.868491161016267554 ) ) ;
#72437=B_SPLINE_CURVE_WITH_KNOTS ( 'NONE', 3,
 ( #66549, #60612, #75700, #99427, #50881, #85401, #91373, #67091, #83785, #77305, #76229, #25606, #68149, #35276 ),
 .UNSPECIFIED., .F., .F.,
 ( 4, 2, 2, 2, 2, 2, 4 ),
 ( 1.532679976604137452E-17, 0.001109001854540035822, 0.002218003709080056032, 0.003327005563620077759, 0.003881506490890071926, 0.004158756954525069660, 0.004436007418160066960 ),
 .UNSPECIFIED. ) ;
#72448=DIRECTION ( 'NONE',  ( 0.000000000000000000, 0.000000000000000000, 1.000000000000000000 ) ) ;
#72455=CARTESIAN_POINT ( 'NONE',  ( -1.000000000000000000, -26.91905550219100363, -6.087553237119084137 ) ) ;
#72479=PRESENTATION_STYLE_ASSIGNMENT (( #23432 ) ) ;
#72520=B_SPLINE_CURVE_WITH_KNOTS ( 'NONE', 3,
 ( #70951, #96827, #29472, #14820, #6737, #38603, #62347, #79567, #4635, #95239, #22957, #105442, #71466, #104366, #63415, #72011 ),
 .UNSPECIFIED., .F., .F.,
 ( 4, 2, 2, 2, 2, 2, 2, 4 ),
 ( 0.003415289155120490843, 0.004063164684144634359, 0.004711040213168779175, 0.006006791271217062737, 0.007302542329265346299, 0.008598293387313628994, 0.01118979550341019785, 0.01378129761950676671 ),
 .UNSPECIFIED. ) ;
#72523=CARTESIAN_POINT ( 'NONE',  ( -0.5839975711783412793, -70.55108709206167816, 13.00914722619329211 ) ) ;
#72538=AXIS2_PLACEMENT_3D ( 'NONE', #58422, #57867, #65973 ) ;
#72552=CARTESIAN_POINT ( 'NONE',  ( -2.070413606167707421, -70.53207026027745030, 13.15197026184339713 ) ) ;
#72562=SURFACE_SIDE_STYLE ('',( #79595 ) ) ;
#72569=SURFACE_SIDE_STYLE ('',( #6233 ) ) ;
#72571=AXIS2_PLACEMENT_3D ( 'NONE', #687, #8286, #98364 ) ;
#72572=( NAMED_UNIT ( * ) SI_UNIT ( $, .STERADIAN. ) SOLID_ANGLE_UNIT ( ) );
#72638=( NAMED_UNIT ( * ) PLANE_ANGLE_UNIT ( ) SI_UNIT ( $, .RADIAN. ) );
#72656=CARTESIAN_POINT ( 'NONE',  ( -1.000000000001114220, -70.58759490697448769, 11.03128057732874190 ) ) ;
#72657=CARTESIAN_POINT ( 'NONE',  ( -2.529110775640357911, -69.31258397332325671, 12.94914962940092629 ) ) ;
#72696=( LENGTH_UNIT ( ) NAMED_UNIT ( * ) SI_UNIT ( .MILLI., .METRE. ) );
#72702=STYLED_ITEM ( 'NONE', ( #59417 ), #20210 ) ;
#72706=SURFACE_SIDE_STYLE ('',( #17152 ) ) ;
#72723=( GEOMETRIC_REPRESENTATION_CONTEXT ( 3 ) GLOBAL_UNCERTAINTY_ASSIGNED_CONTEXT ( ( #18985 ) ) GLOBAL_UNIT_ASSIGNED_CONTEXT ( ( #16984, #63954, #64477 ) ) REPRESENTATION_CONTEXT ( 'NONE', 'WORKASPACE' ) );
#72726=( NAMED_UNIT ( * ) PLANE_ANGLE_UNIT ( ) SI_UNIT ( $, .RADIAN. ) );
#72749=CARTESIAN_POINT ( 'NONE',  ( -5.959251246171386462, -13.44866041637656728, 13.58291813670143888 ) ) ;
#72768=APPLICATION_CONTEXT ( 'automotive_design' ) ;
#72823=CARTESIAN_POINT ( 'NONE',  ( 1.889203326810533268, -7.108778228558977119, -13.31560817771940108 ) ) ;
#72865=CARTESIAN_POINT ( 'NONE',  ( -10.92479762610444638, 2.452360385479824600, 14.79862712302001881 ) ) ;
#72888=CARTESIAN_POINT ( 'NONE',  ( 13.45079846400083490, -54.26571488717375757, 23.11721482942555284 ) ) ;
#72899=CARTESIAN_POINT ( 'NONE',  ( 9.287587386881233087, -55.78087779922811507, 30.70844757271691350 ) ) ;
#72917=EDGE_LOOP ( 'NONE', ( #63335, #96320, #15384, #12416 ) ) ;
#72922=DIRECTION ( 'NONE',  ( 0.000000000000000000, 1.000000000000000000, 0.000000000000000000 ) ) ;
#72924=CARTESIAN_POINT ( 'NONE',  ( -5.000000000000001776, -46.28716247248784299, 42.58845726811990318 ) ) ;
#72927=CARTESIAN_POINT ( 'NONE',  ( -6.967015948558341165, -46.95078337943017743, 39.14357484227694783 ) ) ;
#72933=STYLED_ITEM ( 'NONE', ( #5085 ), #18881 ) ;
#72974=COLOUR_RGB ( '', 0.08235294, 0.09019608, 0.10196078) ;
#72978=DIRECTION ( 'NONE',  ( -0.000000000000000000, -1.000000000000000000, -0.000000000000000000 ) ) ;
#72981=CARTESIAN_POINT ( 'NONE',  ( -3.778422651548678068, -48.87976032229202872, 103.2432416460067799 ) ) ;
#72983=EDGE_LOOP ( 'NONE', ( #39831, #14648, #83443, #102146 ) ) ;
#73000=FILL_AREA_STYLE ('',( #57349 ) ) ;
#73007=CARTESIAN_POINT ( 'NONE',  ( -1.907451454365918675, -0.1079931744079098421, 102.2322703247678248 ) ) ;
#73021=FACE_OUTER_BOUND ( 'NONE', #84181, .T. ) ;
#73048=COLOUR_RGB ( '', 0.09019608, 0.27058824, 0.51372549) ;
#73057=CARTESIAN_POINT ( 'NONE',  ( -27.99999999999999645, 0.000000000000000000, 0.000000000000000000 ) ) ;
#73062=CARTESIAN_POINT ( 'NONE',  ( -5.789193319501154456, -65.08511655608099034, 14.25240442334545676 ) ) ;
#73081=( NAMED_UNIT ( * ) PLANE_ANGLE_UNIT ( ) SI_UNIT ( $, .RADIAN. ) );
#73108=MECHANICAL_DESIGN_GEOMETRIC_PRESENTATION_REPRESENTATION('',(#12847),#97234);
#73117=CARTESIAN_POINT ( 'NONE',  ( 11.55908542073290945, -8.827506715863462361, 19.09556135803124377 ) ) ;
#73119=MECHANICAL_DESIGN_GEOMETRIC_PRESENTATION_REPRESENTATION('',(#69778),#26693);
#73137=CARTESIAN_POINT ( 'NONE',  ( 5.833333333333329485, -4.000000000000003553, 103.8776713793258608 ) ) ;
#73140=CARTESIAN_POINT ( 'NONE',  ( -4.902312018371978830, -3.082176157930676563, 103.3400275729950835 ) ) ;
#73143=ORIENTED_EDGE ( 'NONE', *, *, #56773, .T. ) ;
#73167=SURFACE_STYLE_USAGE ( .BOTH. , #33287 ) ;
#73179=ORIENTED_EDGE ( 'NONE', *, *, #18259, .T. ) ;
#73185=CARTESIAN_POINT ( 'NONE',  ( -1.678777966127334764, -5.952373502067780819, -13.77784384362900738 ) ) ;
#73209=CARTESIAN_POINT ( 'NONE',  ( -5.000000000093224983, -46.22753318115157128, 103.2791840072271157 ) ) ;
#73220=ORIENTED_EDGE ( 'NONE', *, *, #42893, .T. ) ;
#73276=CARTESIAN_POINT ( 'NONE',  ( -4.999999999999960032, -13.06782935463013473, 12.36551185560430710 ) ) ;
#73297=B_SPLINE_CURVE_WITH_KNOTS ( 'NONE', 3,
 ( #45157, #11155, #3085, #86685, #38147, #36031, #53758, #68905, #95823, #44084, #19852, #101778, #71003, #29527, #27945, #86161, #29017, #37087 ),
 .UNSPECIFIED., .F., .F.,
 ( 4, 2, 2, 2, 2, 2, 2, 2, 4 ),
 ( 8.901954559210201327E-16, 0.0005478302971557816618, 0.001095660594310672977, 0.001643490891465564400, 0.002191321188620456040, 0.002739151485775347464, 0.003286981782930238887, 0.003834812080085130311, 0.004382642377240021300 ),
 .UNSPECIFIED. ) ;
#73326=CARTESIAN_POINT ( 'NONE',  ( 1.000000000000000000, -69.59657292934913642, 12.76848391599222765 ) ) ;
#73337=ORIENTED_EDGE ( 'NONE', *, *, #42951, .T. ) ;
#73342=CARTESIAN_POINT ( 'NONE',  ( -1.000000000000000444, -54.00000000000000711, 44.97220075561143204 ) ) ;
#73358=AXIS2_PLACEMENT_3D ( 'NONE', #81342, #95967, #97014 ) ;
#73381=( NAMED_UNIT ( * ) PLANE_ANGLE_UNIT ( ) SI_UNIT ( $, .RADIAN. ) );
#73423=SURFACE_STYLE_FILL_AREA ( #9225 ) ;
#73432=CARTESIAN_POINT ( 'NONE',  ( -3.438773559902674304, -0.8293899918508151892, 103.7823003339716053 ) ) ;
#73434=CARTESIAN_POINT ( 'NONE',  ( 1.224646799147353454E-15, -4.000000000000003553, 17.00000000000000000 ) ) ;
#73439=CARTESIAN_POINT ( 'NONE',  ( 12.00269904674914656, -6.870077166404533031, 19.79010987306656588 ) ) ;
#73443=CARTESIAN_POINT ( 'NONE',  ( -1.276674890335059320, -50.00000000000000000, 101.3108517956396639 ) ) ;
#73446=ORIENTED_EDGE ( 'NONE', *, *, #104818, .T. ) ;
#73461=CARTESIAN_POINT ( 'NONE',  ( -3.258466594083123002, -53.34205889910419529, 40.61703279866434002 ) ) ;
#73462=( GEOMETRIC_REPRESENTATION_CONTEXT ( 3 ) GLOBAL_UNCERTAINTY_ASSIGNED_CONTEXT ( ( #70400 ) ) GLOBAL_UNIT_ASSIGNED_CONTEXT ( ( #16557, #852, #65641 ) ) REPRESENTATION_CONTEXT ( 'NONE', 'WORKASPACE' ) );
#73468=CARTESIAN_POINT ( 'NONE',  ( -9.960763185286923616, -57.87158879323015270, 26.07764662560745705 ) ) ;
#73473=CARTESIAN_POINT ( 'NONE',  ( -3.454253436624930451, -0.8414180287960395521, 103.7259032015043232 ) ) ;
#73534=CARTESIAN_POINT ( 'NONE',  ( -4.919733272805030921, -1.562181361514374478, 104.2477112191710944 ) ) ;
#73569=CARTESIAN_POINT ( 'NONE',  ( -0.2923334656586880076, -70.53271932724192084, 13.00000000000000000 ) ) ;
#73601=CARTESIAN_POINT ( 'NONE',  ( -4.259638269668483801, -69.00982656590272768, 13.66265674538449204 ) ) ;
#73638=CARTESIAN_POINT ( 'NONE',  ( -5.000000000000000000, -57.08340687971455196, 10.85455823726397284 ) ) ;
#73660=CARTESIAN_POINT ( 'NONE',  ( 11.20469880689023334, -9.947014048322465385, 18.60075416151417471 ) ) ;
#73696=CARTESIAN_POINT ( 'NONE',  ( 5.000000000000160760, -12.34932486159375031, 8.854147762509146702 ) ) ;
#73709=DIRECTION ( 'NONE',  ( 0.9921085174016663899, 0.1089071661330606455, -0.06212824529900790038 ) ) ;
#73710=CARTESIAN_POINT ( 'NONE',  ( 5.964242399901847236, -13.95070288504633638, 13.91433285878922632 ) ) ;
#73716=CARTESIAN_POINT ( 'NONE',  ( 5.833333333391548692, -46.26205164321707741, 103.8776713793676834 ) ) ;
#73728=CIRCLE ( 'NONE', #8282, 0.5000000000000004441 ) ;
#73730=CARTESIAN_POINT ( 'NONE',  ( -5.911961378333534967, -11.74849339892130295, -9.342346711816039928 ) ) ;
#73731=COLOUR_RGB ( '', 0.40784314, 0.44705882, 0.49803922) ;
#73754=CARTESIAN_POINT ( 'NONE',  ( 2.691782409370788276, -49.46317646816598312, 103.4277688390371281 ) ) ;
#73784=FILL_AREA_STYLE ('',( #16085 ) ) ;
#73789=DIRECTION ( 'NONE',  ( 0.000000000000000000, 0.000000000000000000, 1.000000000000000000 ) ) ;
#73820=CARTESIAN_POINT ( 'NONE',  ( -5.000000000000039080, -12.81882114893590341, 11.98449427369159004 ) ) ;
#73842=CARTESIAN_POINT ( 'NONE',  ( 11.47368253460178700, 2.275697256493656617, 14.82749015516199087 ) ) ;
#73872=B_SPLINE_CURVE_WITH_KNOTS ( 'NONE', 3,
 ( #28787, #62709, #77828, #3937, #87516, #71311, #13597, #38445, #36349, #104204, #44398, #12011, #94559, #30349, #63241, #85390, #11470, #77295, #94006, #3406, #69219, #102086, #20167, #16259, #31425, #15194, #90154, #64300, #56708, #47559, #7620, #55115, #72888, #40016 ),
 .UNSPECIFIED., .F., .F.,
 ( 4, 2, 2, 2, 2, 2, 2, 2, 2, 2, 2, 2, 2, 2, 2, 2, 4 ),
 ( 0.01257177810263095975, 0.01335728547384937119, 0.01414279284506778263, 0.01492830021628619580, 0.01571380758750460724, 0.01649931495872301868, 0.01728482232994143011, 0.01807032970115984155, 0.01885583707237825299, 0.01964134444359666443, 0.02042685181481507933, 0.02121235918603348730, 0.02199786655725190221, 0.02278337392847031018, 0.02356888129968872508, 0.02435438867090713652, 0.02513989604212554796 ),
 .UNSPECIFIED. ) ;
#73909=CARTESIAN_POINT ( 'NONE',  ( 4.460876563139990481, -1.165516444892326087, 104.3906876480053398 ) ) ;
#73963=ORIENTED_EDGE ( 'NONE', *, *, #48926, .F. ) ;
#73972=CARTESIAN_POINT ( 'NONE',  ( 5.000000000000000888, -15.67194501421787756, -10.31047629133739818 ) ) ;
#73974=FACE_OUTER_BOUND ( 'NONE', #10933, .T. ) ;
#73999=CARTESIAN_POINT ( 'NONE',  ( -5.167237685039475892, -51.69260020507286413, 40.01460860130989516 ) ) ;
#74007=CARTESIAN_POINT ( 'NONE',  ( -9.204646778667628482, -55.29777711479709978, 30.90975160907398234 ) ) ;
#74023=( NAMED_UNIT ( * ) PLANE_ANGLE_UNIT ( ) SI_UNIT ( $, .RADIAN. ) );
#74026=FILL_AREA_STYLE_COLOUR ( '', #8296 ) ;
#74102=CARTESIAN_POINT ( 'NONE',  ( -3.883877898720302202, -48.93467900693696038, 104.5781496044265282 ) ) ;
#74132=CARTESIAN_POINT ( 'NONE',  ( 0.9999999999999940048, 0.000000000000000000, 101.0455488498966758 ) ) ;
#74137=CARTESIAN_POINT ( 'NONE',  ( -4.568199989557032659, -65.71137023209668371, 13.11834388973587728 ) ) ;
#74151=SURFACE_STYLE_FILL_AREA ( #91428 ) ;
#74156=SURFACE_SIDE_STYLE ('',( #81703 ) ) ;
#74172=PRESENTATION_STYLE_ASSIGNMENT (( #37086 ) ) ;
#74186=CARTESIAN_POINT ( 'NONE',  ( -0.2996719224662260928, -70.51541691410464807, 12.99134206341307163 ) ) ;
#74194=CARTESIAN_POINT ( 'NONE',  ( 3.959695725110176756, -69.40440198710396658, 13.56584679134417293 ) ) ;
#74212=DIRECTION ( 'NONE',  ( 0.000000000000000000, 1.000000000000000000, 0.000000000000000000 ) ) ;
#74215=DIRECTION ( 'NONE',  ( 1.000000000000000000, 0.000000000000000000, 0.000000000000000000 ) ) ;
#74225=ORIENTED_EDGE ( 'NONE', *, *, #83053, .F. ) ;
#74228=CARTESIAN_POINT ( 'NONE',  ( 5.000000000000039968, -12.89614509141023291, 12.11365041472630644 ) ) ;
#74234=TOROIDAL_SURFACE ( 'NONE', #7029, 12.00000000000000000, 2.000000000000000000 ) ;
#74247=FILL_AREA_STYLE ('',( #66158 ) ) ;
#74251=CARTESIAN_POINT ( 'NONE',  ( 4.928386788250681327, -48.42812442315226207, 104.2441249819462712 ) ) ;
#74265=CARTESIAN_POINT ( 'NONE',  ( -4.277293724315427426, -9.465728641413040378, -11.68612602563391079 ) ) ;
#74290=DIRECTION ( 'NONE',  ( -1.000000000000000000, -0.000000000000000000, -0.000000000000000000 ) ) ;
#74302=DIRECTION ( 'NONE',  ( -1.000000000000000000, -0.000000000000000000, -0.000000000000000000 ) ) ;
#74319=CARTESIAN_POINT ( 'NONE',  ( 5.000000000000000000, -15.93202192939576634, -5.930487099830193287 ) ) ;
#74333=STYLED_ITEM ( 'NONE', ( #82058 ), #92949 ) ;
#74335=CARTESIAN_POINT ( 'NONE',  ( 6.999999999999999112, 0.000000000000000000, 0.000000000000000000 ) ) ;
#74346=CARTESIAN_POINT ( 'NONE',  ( -6.105464488525263356, -12.30761336974420317, 12.19688296868001842 ) ) ;
#74355=DIRECTION ( 'NONE',  ( 0.000000000000000000, -1.000000000000000000, 0.000000000000000000 ) ) ;
#74364=CARTESIAN_POINT ( 'NONE',  ( 12.39857089150704006, -3.847148675972121179, 20.49778519109818475 ) ) ;
#74367=B_SPLINE_CURVE_WITH_KNOTS ( 'NONE', 3,
 ( #92388, #68122, #101018, #74608, #18534, #58982, #53414, #25588 ),
 .UNSPECIFIED., .F., .F.,
 ( 4, 2, 2, 4 ),
 ( -1.045097417706059526E-05, 0.0004743348448042788079, 0.0007167277542949298044, 0.0009591206637855809094 ),
 .UNSPECIFIED. ) ;
#74378=ORIENTED_EDGE ( 'NONE', *, *, #74423, .F. ) ;
#74395=FACE_OUTER_BOUND ( 'NONE', #103876, .T. ) ;
#74401=CARTESIAN_POINT ( 'NONE',  ( 9.667921046838758414, -50.82596344167677671, 29.56517872135010094 ) ) ;
#74417=VERTEX_POINT ( 'NONE', #27270 ) ;
#74423=EDGE_CURVE ( 'NONE', #77653, #104941, #38254, .T. ) ;
#74426=CARTESIAN_POINT ( 'NONE',  ( -5.000000000000000888, -50.00000000000000000, 40.07669683062201926 ) ) ;
#74428=CARTESIAN_POINT ( 'NONE',  ( -12.39352808926492067, -3.234829339351946054, 20.63804935124764484 ) ) ;
#74441=DIRECTION ( 'NONE',  ( -1.000000000000000000, -0.000000000000000000, -0.000000000000000000 ) ) ;
#74449=DIRECTION ( 'NONE',  ( 0.000000000000000000, 1.000000000000000000, 0.000000000000000000 ) ) ;
#74454=EDGE_CURVE ( 'NONE', #34973, #18508, #105358, .T. ) ;
#74469=TOROIDAL_SURFACE ( 'NONE', #79639, 13.00000000000000000, 2.000000000000000000 ) ;
#74493=EDGE_CURVE ( 'NONE', #88353, #93333, #45802, .T. ) ;
#74500=CARTESIAN_POINT ( 'NONE',  ( 9.226882652173665988, -54.53219447884240623, 23.14412647329060491 ) ) ;
#74507=CARTESIAN_POINT ( 'NONE',  ( 8.238185353303229874, -12.24652543886333511, 8.668425773002917722 ) ) ;
#74512=CARTESIAN_POINT ( 'NONE',  ( -3.363582653045684712, -48.78526580464421869, 104.5994639297834681 ) ) ;
#74531=CARTESIAN_POINT ( 'NONE',  ( -3.053636405311067836, -53.45138136750625790, 40.66466748881163795 ) ) ;
#74551=SURFACE_SIDE_STYLE ('',( #66467 ) ) ;
#74581=EDGE_LOOP ( 'NONE', ( #36092, #1848, #68286, #89455 ) ) ;
#74582=DIRECTION ( 'NONE',  ( 0.000000000000000000, 1.000000000000000000, 0.000000000000000000 ) ) ;
#74602=CARTESIAN_POINT ( 'NONE',  ( -4.337283319711771057, -10.96666117361756321, -10.25672613774104391 ) ) ;
#74606=CARTESIAN_POINT ( 'NONE',  ( -3.202923538441288187, -1.002156644461976498, 104.2983658136044909 ) ) ;
#74608=CARTESIAN_POINT ( 'NONE',  ( 3.375204959346052025, -0.8899440043431781078, 104.1122719450857375 ) ) ;
#74628=DIRECTION ( 'NONE',  ( -3.469446951953611033E-15, 0.000000000000000000, 1.000000000000000000 ) ) ;
#74650=FILL_AREA_STYLE_COLOUR ( '', #84116 ) ;
#74663=CARTESIAN_POINT ( 'NONE',  ( -4.999999999999801048, -61.23402596802289111, 12.68529909296846370 ) ) ;
#74691=EDGE_CURVE ( 'NONE', #89611, #17242, #101265, .T. ) ;
#74705=AXIS2_PLACEMENT_3D ( 'NONE', #93415, #28179, #4395 ) ;
#74719=CARTESIAN_POINT ( 'NONE',  ( 8.515745267470094859, -14.14492484005115891, 15.87637050603546385 ) ) ;
#74724=CARTESIAN_POINT ( 'NONE',  ( 3.851852197295787317, -68.60299753987145266, 13.53085478509467166 ) ) ;
#74728=( NAMED_UNIT ( * ) SI_UNIT ( $, .STERADIAN. ) SOLID_ANGLE_UNIT ( ) );
#74755=CARTESIAN_POINT ( 'NONE',  ( 5.000000000000039968, -14.06131484383594099, 13.29904837184988509 ) ) ;
#74831=CYLINDRICAL_SURFACE ( 'NONE', #89409, 7.000000000000006217 ) ;
#74842=TOROIDAL_SURFACE ( 'NONE', #33539, 5.999999999999996447, 4.000000000000000000 ) ;
#74890=EDGE_LOOP ( 'NONE', ( #98010, #99556, #14282, #25797 ) ) ;
#74920=CARTESIAN_POINT ( 'NONE',  ( 4.363347285238665663, -66.51195625152190871, 13.14303842901982122 ) ) ;
#74940=EDGE_CURVE ( 'NONE', #66555, #19188, #26250, .T. ) ;
#74945=CARTESIAN_POINT ( 'NONE',  ( 1.000000000000000222, -5.000000000000000000, -14.14213562373095101 ) ) ;
#74954=CARTESIAN_POINT ( 'NONE',  ( -12.24137076217897757, -2.657276045107078932, 20.68757701188024356 ) ) ;
#74971=CARTESIAN_POINT ( 'NONE',  ( -15.94126187130347816, -2.914874698625427030, 14.71615789485484527 ) ) ;
#75004=CARTESIAN_POINT ( 'NONE',  ( -13.49954484221011519, -52.22483108233568316, 30.71121296612578888 ) ) ;
#75022=CARTESIAN_POINT ( 'NONE',  ( 9.300615953693611715, -55.29760853177170077, 23.32435243128603730 ) ) ;
#75026=CARTESIAN_POINT ( 'NONE',  ( 0.000000000000000000, -78.00000000000000000, 27.00000000000000000 ) ) ;
#75034=CARTESIAN_POINT ( 'NONE',  ( -3.499286860954911482, -49.14195911236761560, 104.2445795335841723 ) ) ;
#75053=CARTESIAN_POINT ( 'NONE',  ( -6.835395722631245619, -47.88907770483961457, 39.21814578782241512 ) ) ;
#75056=( BOUNDED_SURFACE ( )  B_SPLINE_SURFACE ( 3, 2, ( 
 ( #35205, #61061, #68077 ),
 ( #3348, #36811, #100968 ),
 ( #2802, #69157, #102028 ),
 ( #93955, #27665, #35750 ),
 ( #69674, #51878, #60539 ),
 ( #102574, #61602, #92340 ),
 ( #19041, #84796, #68632 ),
 ( #73842, #75439, #99718 ),
 ( #33412, #43084, #100244 ),
 ( #25328, #67884, #18295 ),
 ( #91117, #59809, #26409 ),
 ( #8039, #83004, #58744 ),
 ( #34498, #40951, #59275 ),
 ( #50099, #81920, #99170 ),
 ( #100773, #1531, #67365 ),
 ( #57643, #35021, #50608 ),
 ( #106736, #65759, #26936 ),
 ( #24790, #9099, #32884 ),
 ( #42007, #58192, #9627 ),
 ( #49566, #92150, #33956 ),
 ( #10169, #98640, #16674 ),
 ( #90564, #51151, #42536 ),
 ( #75973, #17227, #82474 ),
 ( #974, #84069, #8575 ),
 ( #41477, #2068, #74364 ),
 ( #92690, #49022, #443 ) ),
 .UNSPECIFIED., .F., .F., .T. ) 
 B_SPLINE_SURFACE_WITH_KNOTS ( ( 4, 2, 2, 2, 2, 2, 2, 2, 2, 2, 2, 2, 4 ),
 ( 3, 3 ),
 ( 0.01269614743543319955, 0.01645309493989140920, 0.01739233181600596118, 0.01833156869212051315, 0.02021004244434962058, 0.02114927932046417602, 0.02208851619657872800, 0.02302775307269327998, 0.02396698994880783196, 0.02490622682492238393, 0.02584546370103693591, 0.02678470057715148789, 0.02772393745326604333 ),
 ( 0.000000000000000000, 1.000000000000000000 ),
 .UNSPECIFIED. ) 
 GEOMETRIC_REPRESENTATION_ITEM ( )  RATIONAL_B_SPLINE_SURFACE ( (
 ( 1.000000000000000000, 0.7779866052154990053, 1.000000000000000000),
 ( 1.000000000000000000, 0.7555083041612958850, 1.000000000000000000),
 ( 1.000000000000000000, 0.7303672838383610255, 1.000000000000000000),
 ( 1.000000000000000000, 0.6962732919722572911, 1.000000000000000000),
 ( 1.000000000000000000, 0.6893100548033399555, 1.000000000000000000),
 ( 1.000000000000000000, 0.6750693062836214953, 1.000000000000000000),
 ( 1.000000000000000000, 0.6677720645066671512, 1.000000000000000000),
 ( 1.000000000000000000, 0.6457877037097499162, 1.000000000000000000),
 ( 1.000000000000000000, 0.6308753259117235723, 1.000000000000000000),
 ( 1.000000000000000000, 0.6084032687353759794, 1.000000000000000000),
 ( 1.000000000000000000, 0.6008606624260669493, 1.000000000000000000),
 ( 1.000000000000000000, 0.5861844014193601238, 1.000000000000000000),
 ( 1.000000000000000000, 0.5790246786810088198, 1.000000000000000000),
 ( 1.000000000000000000, 0.5652570769870747247, 1.000000000000000000),
 ( 1.000000000000000000, 0.5586479634791106097, 1.000000000000000000),
 ( 1.000000000000000000, 0.5462697778676210980, 1.000000000000000000),
 ( 1.000000000000000000, 0.5405574414742128075, 1.000000000000000000),
 ( 1.000000000000000000, 0.5306463036818965806, 1.000000000000000000),
 ( 1.000000000000000000, 0.5264056264176346644, 1.000000000000000000),
 ( 1.000000000000000000, 0.5196980651061768874, 1.000000000000000000),
 ( 1.000000000000000000, 0.5172505343756695906, 1.000000000000000000),
 ( 1.000000000000000000, 0.5145634736035570311, 1.000000000000000000),
 ( 1.000000000000000000, 0.5142842565703922286, 1.000000000000000000),
 ( 1.000000000000000000, 0.5159055935738563470, 1.000000000000000000),
 ( 1.000000000000000000, 0.5178303183804268128, 1.000000000000000000),
 ( 1.000000000000000000, 0.5207636911093219689, 1.000000000000000000) ) ) 
 REPRESENTATION_ITEM ( '' )  SURFACE ( )  );
#75058=ORIENTED_EDGE ( 'NONE', *, *, #91727, .F. ) ;
#75087=( NAMED_UNIT ( * ) PLANE_ANGLE_UNIT ( ) SI_UNIT ( $, .RADIAN. ) );
#75102=ORIENTED_EDGE ( 'NONE', *, *, #3193, .F. ) ;
#75131=CARTESIAN_POINT ( 'NONE',  ( -1.467430646253637727, -3.559797132994073943E-15, 101.6319755442054458 ) ) ;
#75165=CARTESIAN_POINT ( 'NONE',  ( -3.787335548944444241, -48.90784695949694338, 104.1352136098598606 ) ) ;
#75187=ORIENTED_EDGE ( 'NONE', *, *, #91945, .F. ) ;
#75188=ORIENTED_EDGE ( 'NONE', *, *, #5716, .T. ) ;
#75233=MECHANICAL_DESIGN_GEOMETRIC_PRESENTATION_REPRESENTATION('',(#80396),#73462);
#75239=CARTESIAN_POINT ( 'NONE',  ( 3.453949035417619218, -49.16871745132488059, 44.00840514944384552 ) ) ;
#75257=CARTESIAN_POINT ( 'NONE',  ( 4.618707958157409088, -65.43970587102317893, 13.10267263298003648 ) ) ;
#75277=( GEOMETRIC_REPRESENTATION_CONTEXT ( 3 ) GLOBAL_UNCERTAINTY_ASSIGNED_CONTEXT ( ( #96632 ) ) GLOBAL_UNIT_ASSIGNED_CONTEXT ( ( #57067, #64140, #72205 ) ) REPRESENTATION_CONTEXT ( 'NONE', 'WORKASPACE' ) );
#75288=EDGE_CURVE ( 'NONE', #3119, #43338, #97805, .T. ) ;
#75292=CARTESIAN_POINT ( 'NONE',  ( 5.000000000000000000, -14.08559933050961632, 11.75736354680376472 ) ) ;
#75302=AXIS2_PLACEMENT_3D ( 'NONE', #25083, #49855, #39142 ) ;
#75304=UNCERTAINTY_MEASURE_WITH_UNIT (LENGTH_MEASURE( 1.000000000000000082E-05 ), #42, 'distance_accuracy_value', 'NONE');
#75310=CARTESIAN_POINT ( 'NONE',  ( 6.147350651869627924, 3.811648262644351526E-18, 18.77631036323126423 ) ) ;
#75317=UNCERTAINTY_MEASURE_WITH_UNIT (LENGTH_MEASURE( 1.000000000000000082E-05 ), #36232, 'distance_accuracy_value', 'NONE');
#75357=VECTOR ( 'NONE', #46880, 1000.000000000000000 ) ;
#75373=DIRECTION ( 'NONE',  ( 0.000000000000000000, 0.000000000000000000, 1.000000000000000000 ) ) ;
#75404=CYLINDRICAL_SURFACE ( 'NONE', #103184, 4.000000000000000000 ) ;
#75412=EDGE_LOOP ( 'NONE', ( #20023, #77471 ) ) ;
#75413=ORIENTED_EDGE ( 'NONE', *, *, #39839, .T. ) ;
#75434=MECHANICAL_DESIGN_GEOMETRIC_PRESENTATION_REPRESENTATION('',(#68525),#106375);
#75439=CARTESIAN_POINT ( 'NONE',  ( 9.493622844526626636, -1.977828722490834634, 15.48005331695811648 ) ) ;
#75441=PRESENTATION_STYLE_ASSIGNMENT (( #77581 ) ) ;
#75467=CARTESIAN_POINT ( 'NONE',  ( 5.175128423391567978, -10.69566144610013225, -10.53077195007407596 ) ) ;
#75512=ORIENTED_EDGE ( 'NONE', *, *, #74423, .T. ) ;
#75515=UNCERTAINTY_MEASURE_WITH_UNIT (LENGTH_MEASURE( 1.000000000000000082E-05 ), #72696, 'distance_accuracy_value', 'NONE');
#75523=FILL_AREA_STYLE_COLOUR ( '', #46232 ) ;
#75554=CARTESIAN_POINT ( 'NONE',  ( -5.000000000000000000, -14.43224336012844589, 12.18680852295256933 ) ) ;
#75563=ORIENTED_EDGE ( 'NONE', *, *, #28464, .T. ) ;
#75573=CARTESIAN_POINT ( 'NONE',  ( -3.564365538402600730, -1.135065884989842067, 104.5953911288829659 ) ) ;
#75597=CIRCLE ( 'NONE', #103165, 9.999999999999998224 ) ;
#75626=FACE_OUTER_BOUND ( 'NONE', #2244, .T. ) ;
#75635=EDGE_CURVE ( 'NONE', #30914, #25416, #106415, .T. ) ;
#75648=ORIENTED_EDGE ( 'NONE', *, *, #63460, .T. ) ;
#75667=CARTESIAN_POINT ( 'NONE',  ( 3.454253436624934892, -0.8414180287960449922, 103.7259032015043232 ) ) ;
#75670=CARTESIAN_POINT ( 'NONE',  ( -3.216749358080555954, -8.903395928605739584, -12.12543985758685672 ) ) ;
#75672=CARTESIAN_POINT ( 'NONE',  ( -12.73573943988818336, -9.919073743022268630, 11.26376837308747803 ) ) ;
#75673=CARTESIAN_POINT ( 'NONE',  ( -5.961320375100140012, -13.36618214390666814, 13.51689209302656813 ) ) ;
#75700=CARTESIAN_POINT ( 'NONE',  ( 3.040119806627095578, -0.8312265419168590741, 104.0101162232625995 ) ) ;
#75705=UNCERTAINTY_MEASURE_WITH_UNIT (LENGTH_MEASURE( 1.000000000000000082E-05 ), #15752, 'distance_accuracy_value', 'NONE');
#75706=STYLED_ITEM ( 'NONE', ( #77088 ), #77159 ) ;
#75721=PRESENTATION_STYLE_ASSIGNMENT (( #25625 ) ) ;
#75728=DIRECTION ( 'NONE',  ( 0.000000000000000000, 1.000000000000000000, 0.000000000000000000 ) ) ;
#75753=CARTESIAN_POINT ( 'NONE',  ( 0.7777777777777719059, -54.00000000000000000, 40.97837836547555668 ) ) ;
#75803=CARTESIAN_POINT ( 'NONE',  ( 5.330865973525591883, -66.88151609583364632, 14.05427752368915861 ) ) ;
#75820=SURFACE_STYLE_FILL_AREA ( #42928 ) ;
#75850=CARTESIAN_POINT ( 'NONE',  ( 6.073849149975367290, -15.27114203292411432, 14.38605564242082302 ) ) ;
#75926=LINE ( 'NONE', #60306, #13456 ) ;
#75936=ORIENTED_EDGE ( 'NONE', *, *, #77028, .T. ) ;
#75973=CARTESIAN_POINT ( 'NONE',  ( 15.92287723967830004, -2.181747968925803249, 14.84254035400510752 ) ) ;
#75975=( NAMED_UNIT ( * ) SI_UNIT ( $, .STERADIAN. ) SOLID_ANGLE_UNIT ( ) );
#76010=DIRECTION ( 'NONE',  ( 0.9984555975339683975, 9.637352644315584150E-17, 0.05555555555555554553 ) ) ;
#76016=EDGE_LOOP ( 'NONE', ( #5951, #12832, #32091 ) ) ;
#76019=FACE_OUTER_BOUND ( 'NONE', #78382, .T. ) ;
#76022=PRESENTATION_STYLE_ASSIGNMENT (( #16734 ) ) ;
#76042=SURFACE_STYLE_USAGE ( .BOTH. , #28075 ) ;
#76050=CARTESIAN_POINT ( 'NONE',  ( 1.000000000000000444, -52.55160771104127093, 2.953793101315682623 ) ) ;
#76052=DIRECTION ( 'NONE',  ( 0.000000000000000000, 0.000000000000000000, -1.000000000000000000 ) ) ;
#76060=SURFACE_SIDE_STYLE ('',( #76592 ) ) ;
#76070=EDGE_CURVE ( 'NONE', #14235, #71609, #101361, .T. ) ;
#76097=CARTESIAN_POINT ( 'NONE',  ( -3.358578016107228947, -0.9723468250023499237, 104.2746939430698205 ) ) ;
#76104=CARTESIAN_POINT ( 'NONE',  ( 11.88147559491878269, -10.57770090359279003, 10.63809983876897824 ) ) ;
#76111=UNCERTAINTY_MEASURE_WITH_UNIT (LENGTH_MEASURE( 1.000000000000000082E-05 ), #10225, 'distance_accuracy_value', 'NONE');
#76134=VERTEX_POINT ( 'NONE', #59364 ) ;
#76136=CARTESIAN_POINT ( 'NONE',  ( 0.000000000000000000, -50.00000000000000000, 112.0000000000000000 ) ) ;
#76141=UNCERTAINTY_MEASURE_WITH_UNIT (LENGTH_MEASURE( 1.000000000000000082E-05 ), #23130, 'distance_accuracy_value', 'NONE');
#76145=CARTESIAN_POINT ( 'NONE',  ( -4.051286199644071218, -1.398729870307597878, 103.8758286790405236 ) ) ;
#76156=ADVANCED_FACE ( 'NONE', ( #26491 ), #86933, .F. ) ;
#76161=CARTESIAN_POINT ( 'NONE',  ( -5.000000000000000000, -54.98008964862484760, 9.870798784359230638 ) ) ;
#76179=AXIS2_PLACEMENT_3D ( 'NONE', #91789, #17910, #50762 ) ;
#76196=CARTESIAN_POINT ( 'NONE',  ( 3.352941176471718965, -1.200583151107622815, 104.5794940929782797 ) ) ;
#76198=PRESENTATION_STYLE_ASSIGNMENT (( #43316 ) ) ;
#76201=CARTESIAN_POINT ( 'NONE',  ( -15.08194089903437352, -6.425657694783502905, 13.55734734230695970 ) ) ;
#76219=( NAMED_UNIT ( * ) PLANE_ANGLE_UNIT ( ) SI_UNIT ( $, .RADIAN. ) );
#76229=CARTESIAN_POINT ( 'NONE',  ( 1.232060836821106786, -0.008527515973728574603, 101.3403412146573004 ) ) ;
#76236=( LENGTH_UNIT ( ) NAMED_UNIT ( * ) SI_UNIT ( .MILLI., .METRE. ) );
#76282=CARTESIAN_POINT ( 'NONE',  ( 4.001372801367517162, -48.64733069984636415, 43.58293009944993202 ) ) ;
#76322=CARTESIAN_POINT ( 'NONE',  ( -1.888156768555025566, -49.90642900039781438, 101.9303284617053578 ) ) ;
#76353=CARTESIAN_POINT ( 'NONE',  ( 5.000000000000039968, -13.46492586503063293, 12.82257630554847694 ) ) ;
#76359=EDGE_CURVE ( 'NONE', #77653, #52640, #41307, .T. ) ;
#76368=CARTESIAN_POINT ( 'NONE',  ( -13.72588371288480857, -57.01106425417226120, 29.76328409196439750 ) ) ;
#76398=CARTESIAN_POINT ( 'NONE',  ( 5.285714285714282923, 0.1991252733425875887, 103.1763305333244318 ) ) ;
#76406=AXIS2_PLACEMENT_3D ( 'NONE', #41776, #91409, #17522 ) ;
#76410=MECHANICAL_DESIGN_GEOMETRIC_PRESENTATION_REPRESENTATION('',(#72933),#50531);
#76414=CARTESIAN_POINT ( 'NONE',  ( -4.628159615119684211, -2.310801729693849005, 102.5435725457685834 ) ) ;
#76437=CARTESIAN_POINT ( 'NONE',  ( 6.311611455838505691, -49.69043234645462803, 39.49845025518488484 ) ) ;
#76464=( NAMED_UNIT ( * ) SI_UNIT ( $, .STERADIAN. ) SOLID_ANGLE_UNIT ( ) );
#76479=CARTESIAN_POINT ( 'NONE',  ( 0.000000000000000000, -50.00000000000000000, 112.0000000000000000 ) ) ;
#76503=SURFACE_STYLE_USAGE ( .BOTH. , #102381 ) ;
#76545=DIRECTION ( 'NONE',  ( 0.000000000000000000, 0.000000000000000000, -1.000000000000000000 ) ) ;
#76549=CARTESIAN_POINT ( 'NONE',  ( 8.999999999999994671, -46.00000000000000000, 42.58845726811989607 ) ) ;
#76553=( GEOMETRIC_REPRESENTATION_CONTEXT ( 3 ) GLOBAL_UNCERTAINTY_ASSIGNED_CONTEXT ( ( #76111 ) ) GLOBAL_UNIT_ASSIGNED_CONTEXT ( ( #10225, #83577, #43141 ) ) REPRESENTATION_CONTEXT ( 'NONE', 'WORKASPACE' ) );
#76587=PRESENTATION_STYLE_ASSIGNMENT (( #83614 ) ) ;
#76592=SURFACE_STYLE_FILL_AREA ( #34590 ) ;
#76601=CIRCLE ( 'NONE', #804, 15.00000000000000000 ) ;
#76626=CARTESIAN_POINT ( 'NONE',  ( -3.279721613087240417, -0.7058048543959732912, 103.5044187069696306 ) ) ;
#76628=LINE ( 'NONE', #27607, #49910 ) ;
#76631=CIRCLE ( 'NONE', #35340, 4.000000000000003553 ) ;
#76661=CARTESIAN_POINT ( 'NONE',  ( 1.509254614533404926, -49.97510739924324952, 101.6144273468640478 ) ) ;
#76671=ADVANCED_FACE ( 'NONE', ( #91296 ), #18074, .F. ) ;
#76680=CARTESIAN_POINT ( 'NONE',  ( -3.567967761888314548, -0.9297753284056393674, 103.4762329555118185 ) ) ;
#76690=SURFACE_STYLE_FILL_AREA ( #51348 ) ;
#76707=EDGE_CURVE ( 'NONE', #5701, #77653, #68733, .T. ) ;
#76717=CARTESIAN_POINT ( 'NONE',  ( 1.714505518806294638E-15, -78.00000000000000000, 13.00000000000000000 ) ) ;
#76724=VERTEX_POINT ( 'NONE', #85872 ) ;
#76729=FILL_AREA_STYLE ('',( #33645 ) ) ;
#76733=CARTESIAN_POINT ( 'NONE',  ( -14.46338899916045406, -7.735849041625655786, 12.85468258354162963 ) ) ;
#76769=CARTESIAN_POINT ( 'NONE',  ( 5.833333333391885311, -3.737948356782987869, 103.8776713793679107 ) ) ;
#76782=VERTEX_POINT ( 'NONE', #69666 ) ;
#76792=DIRECTION ( 'NONE',  ( 0.000000000000000000, 0.000000000000000000, 1.000000000000000000 ) ) ;
#76806=DIRECTION ( 'NONE',  ( -1.000000000000000000, -0.000000000000000000, -0.000000000000000000 ) ) ;
#76812=CARTESIAN_POINT ( 'NONE',  ( 2.206083527337586947, -53.79085494686012225, 40.82659048662283396 ) ) ;
#76840=B_SPLINE_CURVE_WITH_KNOTS ( 'NONE', 3,
 ( #49309, #16428, #64983, #89798, #98921, #25080, #8331, #83814, #57938, #41235, #82758, #8860 ),
 .UNSPECIFIED., .F., .F.,
 ( 4, 2, 2, 2, 2, 4 ),
 ( 0.01037482654577543718, 0.01123049164366662390, 0.01208615674155781063, 0.01251398929050340399, 0.01294182183944899735, 0.01379748693734018233 ),
 .UNSPECIFIED. ) ;
#76907=ORIENTED_EDGE ( 'NONE', *, *, #797, .T. ) ;
#76952=VERTEX_POINT ( 'NONE', #29249 ) ;
#76974=EDGE_CURVE ( 'NONE', #17242, #104368, #22922, .T. ) ;
#76984=AXIS2_PLACEMENT_3D ( 'NONE', #32161, #88273, #80683 ) ;
#77018=DIRECTION ( 'NONE',  ( -1.000000000000000000, 0.000000000000000000, 0.000000000000000000 ) ) ;
#77020=( LENGTH_UNIT ( ) NAMED_UNIT ( * ) SI_UNIT ( .MILLI., .METRE. ) );
#77022=DIRECTION ( 'NONE',  ( 0.000000000000000000, 0.000000000000000000, 1.000000000000000000 ) ) ;
#77028=EDGE_CURVE ( 'NONE', #11109, #5281, #44893, .T. ) ;
#77043=CARTESIAN_POINT ( 'NONE',  ( 3.352941176470587425, -48.79941684889505638, 104.5794940929807382 ) ) ;
#77068=CARTESIAN_POINT ( 'NONE',  ( 2.374770270499908964, -6.910312371746204718, -13.35351085777521085 ) ) ;
#77072=TOROIDAL_SURFACE ( 'NONE', #3004, 17.00000000000000000, 2.000000000000000000 ) ;
#77086=ORIENTED_EDGE ( 'NONE', *, *, #7797, .F. ) ;
#77088=PRESENTATION_STYLE_ASSIGNMENT (( #68481 ) ) ;
#77091=VERTEX_POINT ( 'NONE', #36148 ) ;
#77094=DIRECTION ( 'NONE',  ( 1.000000000000000000, 0.000000000000000000, -0.000000000000000000 ) ) ;
#77102=FILL_AREA_STYLE ('',( #12883 ) ) ;
#77118=PRESENTATION_STYLE_ASSIGNMENT (( #35636 ) ) ;
#77133=CARTESIAN_POINT ( 'NONE',  ( 0.000000000000000000, -4.000000000000003553, 112.0000000000000000 ) ) ;
#77151=SURFACE_STYLE_USAGE ( .BOTH. , #78723 ) ;
#77154=DIRECTION ( 'NONE',  ( -1.000000000000000000, 0.000000000000000000, 0.000000000000000000 ) ) ;
#77159=ADVANCED_FACE ( 'NONE', ( #92739 ), #103279, .T. ) ;
#77198=CARTESIAN_POINT ( 'NONE',  ( 4.999999999999999112, -58.90829211404609111, 11.71895889478539665 ) ) ;
#77200=AXIS2_PLACEMENT_3D ( 'NONE', #46499, #79393, #5510 ) ;
#77203=MECHANICAL_DESIGN_GEOMETRIC_PRESENTATION_REPRESENTATION('',(#49619),#23868);
#77231=( NAMED_UNIT ( * ) PLANE_ANGLE_UNIT ( ) SI_UNIT ( $, .RADIAN. ) );
#77282=DIRECTION ( 'NONE',  ( -1.000000000000000000, 0.000000000000000000, 0.000000000000000000 ) ) ;
#77295=CARTESIAN_POINT ( 'NONE',  ( 14.00175760317098117, -58.00025725680810496, 26.85746939222903151 ) ) ;
#77305=CARTESIAN_POINT ( 'NONE',  ( 1.289261528792995382, -0.01360727255291783316, 101.4143542463165204 ) ) ;
#77313=( NAMED_UNIT ( * ) PLANE_ANGLE_UNIT ( ) SI_UNIT ( $, .RADIAN. ) );
#77341=CARTESIAN_POINT ( 'NONE',  ( -9.269255467170962604, -55.04472406073652024, 23.24713075214419433 ) ) ;
#77359=CARTESIAN_POINT ( 'NONE',  ( 2.783573587432064400, -49.58977995685751239, 44.41792197296597777 ) ) ;
#77378=CARTESIAN_POINT ( 'NONE',  ( -2.409582269539474186, -53.72452336040274901, 40.79253407940785081 ) ) ;
#77385=ORIENTED_EDGE ( 'NONE', *, *, #86409, .T. ) ;
#77407=( GEOMETRIC_REPRESENTATION_CONTEXT ( 3 ) GLOBAL_UNCERTAINTY_ASSIGNED_CONTEXT ( ( #101717 ) ) GLOBAL_UNIT_ASSIGNED_CONTEXT ( ( #35068, #51740, #67418 ) ) REPRESENTATION_CONTEXT ( 'NONE', 'WORKASPACE' ) );
#77438=CARTESIAN_POINT ( 'NONE',  ( 6.531352669123184462, -12.73774374834599321, -7.942415274083415078 ) ) ;
#77449=ORIENTED_EDGE ( 'NONE', *, *, #14366, .F. ) ;
#77452=CARTESIAN_POINT ( 'NONE',  ( 6.920567593065738876, -12.35473601147218403, 8.513547508574102807 ) ) ;
#77458=( NAMED_UNIT ( * ) SI_UNIT ( $, .STERADIAN. ) SOLID_ANGLE_UNIT ( ) );
#77471=ORIENTED_EDGE ( 'NONE', *, *, #1284, .T. ) ;
#77500=SURFACE_STYLE_USAGE ( .BOTH. , #52673 ) ;
#77508=AXIS2_PLACEMENT_3D ( 'NONE', #46112, #94679, #36985 ) ;
#77516=EDGE_CURVE ( 'NONE', #85444, #12840, #106530, .T. ) ;
#77520=DIRECTION ( 'NONE',  ( 0.000000000000000000, 0.000000000000000000, -1.000000000000000000 ) ) ;
#77522=CARTESIAN_POINT ( 'NONE',  ( 5.918685970911453431, -50.53352564182060291, 39.68924167665423397 ) ) ;
#77559=B_SPLINE_CURVE_WITH_KNOTS ( 'NONE', 3,
 ( #59687, #75310, #1407, #51571, #43495, #35432, #16555, #49438, #98524, #24671, #77984, #19794, #102795, #102255, #85561, #53185, #68847, #11097, #94173, #85013, #20338, #44022 ),
 .UNSPECIFIED., .F., .F.,
 ( 4, 2, 2, 2, 2, 2, 2, 2, 2, 2, 4 ),
 ( 0.000000000000000000, 0.002352169759828700267, 0.003528254639743051702, 0.004704339519657403136, 0.005292381959614579287, 0.005880424399571757173, 0.007056509279486109475, 0.007644551719443283891, 0.008232594159400459174, 0.008820636599357634458, 0.009408679039314809742 ),
 .UNSPECIFIED. ) ;
#77563=CIRCLE ( 'NONE', #53469, 17.00000000000000000 ) ;
#77581=SURFACE_STYLE_USAGE ( .BOTH. , #36100 ) ;
#77584=( LENGTH_UNIT ( ) NAMED_UNIT ( * ) SI_UNIT ( .MILLI., .METRE. ) );
#77606=CARTESIAN_POINT ( 'NONE',  ( 4.442085480450892909, -13.39242828886014358, -9.057376035804651337 ) ) ;
#77627=SURFACE_SIDE_STYLE ('',( #100295 ) ) ;
#77642=CARTESIAN_POINT ( 'NONE',  ( 0.9999999999999941158, -1.734723475976807094E-15, 101.0455488498966758 ) ) ;
#77644=EDGE_CURVE ( 'NONE', #11338, #2153, #57635, .T. ) ;
#77653=VERTEX_POINT ( 'NONE', #61739 ) ;
#77657=EDGE_LOOP ( 'NONE', ( #101449, #82243 ) ) ;
#77658=CARTESIAN_POINT ( 'NONE',  ( -8.953164881677507125, -1.467082799477942734, 15.49915330648462231 ) ) ;
#77665=( GEOMETRIC_REPRESENTATION_CONTEXT ( 3 ) GLOBAL_UNCERTAINTY_ASSIGNED_CONTEXT ( ( #81727 ) ) GLOBAL_UNIT_ASSIGNED_CONTEXT ( ( #78317, #23838, #88545 ) ) REPRESENTATION_CONTEXT ( 'NONE', 'WORKASPACE' ) );
#77687=CARTESIAN_POINT ( 'NONE',  ( -2.669532029060316614, -70.32879813054786666, 13.25462063025687165 ) ) ;
#77696=DIRECTION ( 'NONE',  ( 0.000000000000000000, 1.000000000000000000, -1.224646799147353207E-16 ) ) ;
#77739=CARTESIAN_POINT ( 'NONE',  ( 4.999999999999999112, -53.41517366205636108, 9.165057039496462110 ) ) ;
#77752=AXIS2_PLACEMENT_3D ( 'NONE', #31818, #17231, #56591 ) ;
#77759=CARTESIAN_POINT ( 'NONE',  ( -3.963177594439675655, -1.288758772720862256, 103.9032426698856995 ) ) ;
#77770=CARTESIAN_POINT ( 'NONE',  ( -4.324913936355902599, -48.88822604074822920, 104.4044995709990076 ) ) ;
#77808=CARTESIAN_POINT ( 'NONE',  ( 0.9999999999999997780, -26.91905550219523846, -6.087553237117470317 ) ) ;
#77821=MECHANICAL_DESIGN_GEOMETRIC_PRESENTATION_REPRESENTATION('',(#24499),#317);
#77828=CARTESIAN_POINT ( 'NONE',  ( 13.38886880393120116, -54.52389483426509287, 31.09159242423791270 ) ) ;
#77832=FILL_AREA_STYLE_COLOUR ( '', #61374 ) ;
#77855=SURFACE_STYLE_USAGE ( .BOTH. , #87027 ) ;
#77874=CARTESIAN_POINT ( 'NONE',  ( -9.728434877168217199, -57.17846926216942194, 24.67462639010848946 ) ) ;
#77887=DIRECTION ( 'NONE',  ( 0.000000000000000000, 0.000000000000000000, 1.000000000000000000 ) ) ;
#77892=CARTESIAN_POINT ( 'NONE',  ( 1.726903458799834867, -50.00449021765935953, 40.95332780868852041 ) ) ;
#77897=( GEOMETRIC_REPRESENTATION_CONTEXT ( 3 ) GLOBAL_UNCERTAINTY_ASSIGNED_CONTEXT ( ( #83698 ) ) GLOBAL_UNIT_ASSIGNED_CONTEXT ( ( #44970, #101599, #69764 ) ) REPRESENTATION_CONTEXT ( 'NONE', 'WORKASPACE' ) );
#77901=VECTOR ( 'NONE', #16771, 1000.000000000000000 ) ;
#77944=MECHANICAL_DESIGN_GEOMETRIC_PRESENTATION_REPRESENTATION('',(#72702),#12405);
#77962=CIRCLE ( 'NONE', #91743, 2.000000000000000000 ) ;
#77966=CARTESIAN_POINT ( 'NONE',  ( 5.413502513818780670, -11.02777463356547472, -10.18306091005958791 ) ) ;
#77984=CARTESIAN_POINT ( 'NONE',  ( 10.68122111649761052, -0.9711149147263152814, 20.28324505696595637 ) ) ;
#78001=SURFACE_STYLE_USAGE ( .BOTH. , #37046 ) ;
#78023=CARTESIAN_POINT ( 'NONE',  ( -4.970849588242775674, -3.447900702885855928, 102.2755693391596026 ) ) ;
#78024=( NAMED_UNIT ( * ) SI_UNIT ( $, .STERADIAN. ) SOLID_ANGLE_UNIT ( ) );
#78036=FILL_AREA_STYLE ('',( #102849 ) ) ;
#78095=B_SPLINE_CURVE_WITH_KNOTS ( 'NONE', 3,
 ( #49505, #17165, #57581, #39844, #32292, #82413, #32825, #914 ),
 .UNSPECIFIED., .F., .F.,
 ( 4, 2, 2, 4 ),
 ( -1.406834188357377339E-05, 0.0004804345972576498734, 0.0007276860668282617408, 0.0009749375363988734998 ),
 .UNSPECIFIED. ) ;
#78101=CARTESIAN_POINT ( 'NONE',  ( -10.05401422878392204, -11.60173371080193050, 9.516791662972487131 ) ) ;
#78111=ORIENTED_EDGE ( 'NONE', *, *, #81982, .F. ) ;
#78118=EDGE_CURVE ( 'NONE', #67342, #550, #99884, .T. ) ;
#78122=ORIENTED_EDGE ( 'NONE', *, *, #510, .T. ) ;
#78138=DIRECTION ( 'NONE',  ( -0.7142857142857136354, -0.6998542122237659813, 0.000000000000000000 ) ) ;
#78161=CARTESIAN_POINT ( 'NONE',  ( 3.035724950089473850, -0.5466957598722548273, 103.2067224559505831 ) ) ;
#78163=FACE_OUTER_BOUND ( 'NONE', #7603, .T. ) ;
#78174=CARTESIAN_POINT ( 'NONE',  ( -9.346883474190137875, -3.134074240396935274, 14.76168387817866368 ) ) ;
#78184=DIRECTION ( 'NONE',  ( 0.000000000000000000, 1.000000000000000000, 0.000000000000000000 ) ) ;
#78189=DIRECTION ( 'NONE',  ( -1.000000000000000000, -0.000000000000000000, -0.000000000000000000 ) ) ;
#78205=CARTESIAN_POINT ( 'NONE',  ( -5.897959690130281096, -64.39611687089356451, 14.30281393798261114 ) ) ;
#78206=PRESENTATION_STYLE_ASSIGNMENT (( #103026 ) ) ;
#78210=FILL_AREA_STYLE_COLOUR ( '', #66815 ) ;
#78232=CARTESIAN_POINT ( 'NONE',  ( -7.000000000000000000, -80.00000000000000000, 12.61250543006184088 ) ) ;
#78289=CARTESIAN_POINT ( 'NONE',  ( -5.000000000000000000, -38.85524261681796787, 2.940510229002995857 ) ) ;
#78290=DIRECTION ( 'NONE',  ( 0.8660254037844389297, -0.000000000000000000, 0.4999999999999998890 ) ) ;
#78298=( GEOMETRIC_REPRESENTATION_CONTEXT ( 3 ) GLOBAL_UNCERTAINTY_ASSIGNED_CONTEXT ( ( #34760 ) ) GLOBAL_UNIT_ASSIGNED_CONTEXT ( ( #76236, #77313, #70288 ) ) REPRESENTATION_CONTEXT ( 'NONE', 'WORKASPACE' ) );
#78311=CARTESIAN_POINT ( 'NONE',  ( -3.054195049253882743, -0.8450860964495454652, 104.0345731970086121 ) ) ;
#78317=( LENGTH_UNIT ( ) NAMED_UNIT ( * ) SI_UNIT ( .MILLI., .METRE. ) );
#78329=FILL_AREA_STYLE ('',( #4987 ) ) ;
#78364=CARTESIAN_POINT ( 'NONE',  ( 5.437321008177463888, -2.342832151771340854, 104.0362115404844303 ) ) ;
#78382=EDGE_LOOP ( 'NONE', ( #75648, #62219, #35289, #71294 ) ) ;
#78419=DIRECTION ( 'NONE',  ( 0.000000000000000000, 1.000000000000000000, 0.000000000000000000 ) ) ;
#78427=CARTESIAN_POINT ( 'NONE',  ( -2.788175468594526141, -49.58758714223310449, 44.41557376465305396 ) ) ;
#78519=CARTESIAN_POINT ( 'NONE',  ( -1.356500113650659367, -70.62225732679223711, 13.06381631859566816 ) ) ;
#78522=ORIENTED_EDGE ( 'NONE', *, *, #69675, .F. ) ;
#78546=DIRECTION ( 'NONE',  ( 0.000000000000000000, 1.000000000000000000, 0.000000000000000000 ) ) ;
#78580=ORIENTED_EDGE ( 'NONE', *, *, #57222, .T. ) ;
#78618=CARTESIAN_POINT ( 'NONE',  ( -6.594435029803459969, -7.011724847875096422, 13.88183737994264177 ) ) ;
#78621=CARTESIAN_POINT ( 'NONE',  ( 3.358578016107375053, -49.02765317499759590, 104.2746939430699200 ) ) ;
#78625=EDGE_CURVE ( 'NONE', #104368, #63843, #77563, .T. ) ;
#78647=ADVANCED_FACE ( 'NONE', ( #78163 ), #13413, .F. ) ;
#78657=CIRCLE ( 'NONE', #45954, 7.000000000000006217 ) ;
#78663=AXIS2_PLACEMENT_3D ( 'NONE', #55501, #74355, #64689 ) ;
#78667=( NAMED_UNIT ( * ) PLANE_ANGLE_UNIT ( ) SI_UNIT ( $, .RADIAN. ) );
#78677=B_SPLINE_CURVE_WITH_KNOTS ( 'NONE', 3,
 ( #79442, #46028, #70830, #89136, #87552, #47593, #78910, #80490, #55668, #104783, #39000, #105317, #54087, #14160, #46548, #29866, #56197, #62745, #72924, #23361 ),
 .UNSPECIFIED., .F., .F.,
 ( 4, 2, 2, 2, 2, 2, 2, 2, 2, 4 ),
 ( 0.000000000000000000, 0.0008428829220942208418, 0.001685765844188442551, 0.002528648766282664152, 0.003371531688376885969, 0.004214414610471107353, 0.005057297532565329171, 0.005478738993612435743, 0.005900180454659542315, 0.006743063376753731172 ),
 .UNSPECIFIED. ) ;
#78679=CARTESIAN_POINT ( 'NONE',  ( -30.00000000000000000, -54.00000000000000711, 31.11721482942554928 ) ) ;
#78680=CARTESIAN_POINT ( 'NONE',  ( 2.519529083135021441, -0.4213828544525365372, 103.1541576364168122 ) ) ;
#78691=CARTESIAN_POINT ( 'NONE',  ( -10.32127027360808569, -0.7831254332910545513, 20.16036387503780958 ) ) ;
#78693=EDGE_CURVE ( 'NONE', #97345, #4171, #78095, .T. ) ;
#78719=CARTESIAN_POINT ( 'NONE',  ( -5.608211814930418093, -65.93615317932940911, 14.17185745138047537 ) ) ;
#78723=SURFACE_SIDE_STYLE ('',( #11327 ) ) ;
#78728=CARTESIAN_POINT ( 'NONE',  ( -13.95281146043403098, -50.20507689203379442, 25.82616780902253950 ) ) ;
#78749=STYLED_ITEM ( 'NONE', ( #27570 ), #15853 ) ;
#78756=CARTESIAN_POINT ( 'NONE',  ( 4.302760725356077565, -48.89765558026142145, 104.4121068519184945 ) ) ;
#78814=CARTESIAN_POINT ( 'NONE',  ( -4.460876563139970941, -48.83448355510768835, 104.3906876480053256 ) ) ;
#78815=CARTESIAN_POINT ( 'NONE',  ( -1.000000000000000000, -10.14983348571115229, -12.32139453386699657 ) ) ;
#78858=FACE_OUTER_BOUND ( 'NONE', #54031, .T. ) ;
#78873=CIRCLE ( 'NONE', #32405, 0.5000000000000004441 ) ;
#78886=FACE_OUTER_BOUND ( 'NONE', #94273, .T. ) ;
#78910=CARTESIAN_POINT ( 'NONE',  ( -3.041362414359006117, -49.44898643135800143, 44.27295612633997024 ) ) ;
#78918=EDGE_CURVE ( 'NONE', #33663, #27751, #43226, .T. ) ;
#78961=CARTESIAN_POINT ( 'NONE',  ( -4.888678503699334321, -52.01088711094052286, 40.11975448313368275 ) ) ;
#79040=AXIS2_PLACEMENT_3D ( 'NONE', #38477, #62233, #45506 ) ;
#79061=CARTESIAN_POINT ( 'NONE',  ( -1.000000000000770495, -69.59657292934927852, 12.76848391599230581 ) ) ;
#79066=EDGE_CURVE ( 'NONE', #3905, #43590, #36862, .T. ) ;
#79093=CARTESIAN_POINT ( 'NONE',  ( 13.76566278825922574, -50.82203498049078405, 29.56014984665260670 ) ) ;
#79114=CARTESIAN_POINT ( 'NONE',  ( -1.569964449840315579, -49.94642998360953356, 101.7846783319226773 ) ) ;
#79131=CARTESIAN_POINT ( 'NONE',  ( -4.399054598113282921, -1.887557197752925964, 102.7269706464928021 ) ) ;
#79160=FILL_AREA_STYLE_COLOUR ( '', #4578 ) ;
#79197=ORIENTED_EDGE ( 'NONE', *, *, #92680, .F. ) ;
#79210=ORIENTED_EDGE ( 'NONE', *, *, #46775, .T. ) ;
#79222=( NAMED_UNIT ( * ) PLANE_ANGLE_UNIT ( ) SI_UNIT ( $, .RADIAN. ) );
#79235=CARTESIAN_POINT ( 'NONE',  ( -12.28040651794425386, -2.772380348077450041, 20.68240731548373645 ) ) ;
#79238=COLOUR_RGB ( '', 0.08235294, 0.09019608, 0.10196078) ;
#79241=ORIENTED_EDGE ( 'NONE', *, *, #98877, .F. ) ;
#79264=CARTESIAN_POINT ( 'NONE',  ( -2.179633855064840198, -70.50537186176407545, 13.16847616745739558 ) ) ;
#79275=AXIS2_PLACEMENT_3D ( 'NONE', #86425, #95040, #21177 ) ;
#79282=EDGE_LOOP ( 'NONE', ( #16829, #26970, #67768, #98736 ) ) ;
#79290=( NAMED_UNIT ( * ) PLANE_ANGLE_UNIT ( ) SI_UNIT ( $, .RADIAN. ) );
#79296=UNCERTAINTY_MEASURE_WITH_UNIT (LENGTH_MEASURE( 1.000000000000000082E-05 ), #58061, 'distance_accuracy_value', 'NONE');
#79313=CARTESIAN_POINT ( 'NONE',  ( 5.000000000000000000, -60.71953810597794643, 12.61250543007074931 ) ) ;
#79323=PRESENTATION_STYLE_ASSIGNMENT (( #103084 ) ) ;
#79348=CARTESIAN_POINT ( 'NONE',  ( -4.370066673350128106, -48.86972780289094942, 104.3945758574409837 ) ) ;
#79350=CARTESIAN_POINT ( 'NONE',  ( -5.000000000000000000, -41.56343021050086861, 4.051462231091807809 ) ) ;
#79373=CARTESIAN_POINT ( 'NONE',  ( -1.468752096361644721, -0.02845455281367775119, 101.6458968146023096 ) ) ;
#79377=( NAMED_UNIT ( * ) PLANE_ANGLE_UNIT ( ) SI_UNIT ( $, .RADIAN. ) );
#79393=DIRECTION ( 'NONE',  ( 0.000000000000000000, 1.000000000000000000, 0.000000000000000000 ) ) ;
#79402=ORIENTED_EDGE ( 'NONE', *, *, #61643, .F. ) ;
#79442=CARTESIAN_POINT ( 'NONE',  ( -1.000000000000000444, -50.00000000000000000, 44.97220075561142494 ) ) ;
#79450=AXIS2_PLACEMENT_3D ( 'NONE', #61286, #54755, #53711 ) ;
#79463=DIRECTION ( 'NONE',  ( 0.000000000000000000, 1.000000000000000000, 0.000000000000000000 ) ) ;
#79493=CARTESIAN_POINT ( 'NONE',  ( -11.55614992315287637, -8.838057010478776121, 19.09125476800991450 ) ) ;
#79505=CIRCLE ( 'NONE', #77752, 4.000000000000003553 ) ;
#79512=PRESENTATION_STYLE_ASSIGNMENT (( #46615 ) ) ;
#79516=ORIENTED_EDGE ( 'NONE', *, *, #36388, .T. ) ;
#79523=DIRECTION ( 'NONE',  ( 0.6505632072693968704, 0.6639782930160459395, -0.3686466326319198794 ) ) ;
#79541=STYLED_ITEM ( 'NONE', ( #39343 ), #8466 ) ;
#79567=CARTESIAN_POINT ( 'NONE',  ( 12.53023694619758466, 1.820302489804639157, 14.89061371906986864 ) ) ;
#79578=B_SPLINE_CURVE_WITH_KNOTS ( 'NONE', 3,
 ( #44266, #59394, #25999, #27052, #51805, #75554, #68550, #34074, #92255, #43721, #34609, #92801, #99277, #99826, #58860, #35131, #18410, #84716 ),
 .UNSPECIFIED., .F., .F.,
 ( 4, 2, 2, 2, 2, 2, 2, 2, 4 ),
 ( 0.000000000000000000, 0.0005503281002746097895, 0.001100656200549219579, 0.001650984300823829260, 0.002201312401098439158, 0.002751640501373049056, 0.003301968601647658520, 0.003852296701922268418, 0.004402624802196878316 ),
 .UNSPECIFIED. ) ;
#79595=SURFACE_STYLE_FILL_AREA ( #6766 ) ;
#79617=CARTESIAN_POINT ( 'NONE',  ( 13.80732344291479663, -50.82138033104836694, 24.67475631203899411 ) ) ;
#79632=PRESENTATION_STYLE_ASSIGNMENT (( #69962 ) ) ;
#79639=AXIS2_PLACEMENT_3D ( 'NONE', #91045, #50025, #106665 ) ;
#79662=CARTESIAN_POINT ( 'NONE',  ( -4.581218816254563286, -2.199133564524444306, 103.5404609598622301 ) ) ;
#79683=CARTESIAN_POINT ( 'NONE',  ( 1.140727867604837575, -70.62093189267218918, 13.04401102971384141 ) ) ;
#79691=CARTESIAN_POINT ( 'NONE',  ( -11.12687447062504376, -11.05336892415653161, 10.14262434277811487 ) ) ;
#79723=SURFACE_SIDE_STYLE ('',( #45252 ) ) ;
#79728=STYLED_ITEM ( 'NONE', ( #80655 ), #29376 ) ;
#79762=CARTESIAN_POINT ( 'NONE',  ( -8.661288751401347241, -0.2443065738830995925, 19.58558484236875330 ) ) ;
#79769=EDGE_LOOP ( 'NONE', ( #40258, #101547, #57010 ) ) ;
#79782=CARTESIAN_POINT ( 'NONE',  ( -5.000000000000000000, -60.71953810597282342, 12.61250543006821978 ) ) ;
#79793=( BOUNDED_SURFACE ( )  B_SPLINE_SURFACE ( 3, 2, ( 
 ( #46777, #96408, #47297 ),
 ( #80722, #98503, #97980 ),
 ( #89892, #73696, #96922 ),
 ( #6839, #32749, #48356 ),
 ( #5783, #80194, #39238 ),
 ( #39763, #56441, #81248 ),
 ( #71569, #40276, #48880 ),
 ( #72112, #81774, #24653 ),
 ( #57505, #13864, #105021 ),
 ( #100636, #66684, #33273 ),
 ( #83924, #82863, #41336 ),
 ( #42397, #51007, #66143 ),
 ( #58046, #74228, #99025 ),
 ( #75292, #68284, #26796 ),
 ( #59666, #51553, #27340 ),
 ( #1385, #9486, #1929 ),
 ( #34353, #76353, #25188 ),
 ( #67227, #34880, #2466 ),
 ( #90969, #10559, #91501 ),
 ( #100104, #74755, #17078 ),
 ( #49954, #8959, #26270 ),
 ( #49422, #41867, #59133 ),
 ( #82325, #16531, #8436 ),
 ( #305, #92547, #92015 ),
 ( #18694, #43476, #84466 ),
 ( #25743, #835, #33806 ) ),
 .UNSPECIFIED., .F., .F., .F. ) 
 B_SPLINE_SURFACE_WITH_KNOTS ( ( 4, 2, 2, 2, 2, 2, 2, 2, 2, 2, 2, 2, 4 ),
 ( 3, 3 ),
 ( 0.000000000000000000, 0.0005478302971555681824, 0.001095660594311136365, 0.001643490891466704547, 0.001917406040044488530, 0.002191321188622272730, 0.002465236337200056929, 0.002739151485777841129, 0.003013066634355625328, 0.003286981782933409094, 0.003560896931511192860, 0.003834812080088977060, 0.004382642377244545459 ),
 ( 0.000000000000000000, 1.000000000000000000 ),
 .UNSPECIFIED. ) 
 GEOMETRIC_REPRESENTATION_ITEM ( )  RATIONAL_B_SPLINE_SURFACE ( (
 ( 1.000000000000000000, 0.7071067811865475727, 1.000000000000000000),
 ( 1.000000000000000000, 0.7205633224823966287, 1.000000000000000000),
 ( 1.000000000000000000, 0.7338046748641109396, 1.000000000000000000),
 ( 1.000000000000000000, 0.7598569482830193067, 1.000000000000000000),
 ( 1.000000000000000000, 0.7728059803406955863, 1.000000000000000000),
 ( 1.000000000000000000, 0.7970392697933029735, 1.000000000000000000),
 ( 1.000000000000000000, 0.8084357292879545964, 1.000000000000000000),
 ( 1.000000000000000000, 0.8242617997986435574, 1.000000000000000000),
 ( 1.000000000000000000, 0.8292815833602860121, 1.000000000000000000),
 ( 1.000000000000000000, 0.8385524799112056282, 1.000000000000000000),
 ( 1.000000000000000000, 0.8428399694378527762, 1.000000000000000000),
 ( 1.000000000000000000, 0.8506757475334101315, 1.000000000000000000),
 ( 1.000000000000000000, 0.8542245152659933005, 1.000000000000000000),
 ( 1.000000000000000000, 0.8604965487139695224, 1.000000000000000000),
 ( 1.000000000000000000, 0.8631692933856440764, 1.000000000000000000),
 ( 1.000000000000000000, 0.8674535388007971193, 1.000000000000000000),
 ( 1.000000000000000000, 0.8690878299427966525, 1.000000000000000000),
 ( 1.000000000000000000, 0.8713061800473307361, 1.000000000000000000),
 ( 1.000000000000000000, 0.8718871419634350861, 1.000000000000000000),
 ( 1.000000000000000000, 0.8719209662387901183, 1.000000000000000000),
 ( 1.000000000000000000, 0.8713887681177869826, 1.000000000000000000),
 ( 1.000000000000000000, 0.8692752663532745672, 1.000000000000000000),
 ( 1.000000000000000000, 0.8676790533738619748, 1.000000000000000000),
 ( 1.000000000000000000, 0.8614089247988900855, 1.000000000000000000),
 ( 1.000000000000000000, 0.8553884691243911487, 1.000000000000000000),
 ( 1.000000000000000000, 0.8477912478906596272, 1.000000000000000000) ) ) 
 REPRESENTATION_ITEM ( '' )  SURFACE ( )  );
#79851=CARTESIAN_POINT ( 'NONE',  ( -9.771873710511815858, -50.53670347359850723, 29.13520411490522122 ) ) ;
#79866=( LENGTH_UNIT ( ) NAMED_UNIT ( * ) SI_UNIT ( .MILLI., .METRE. ) );
#79876=CARTESIAN_POINT ( 'NONE',  ( -5.000000000005099920, -10.14983348571164434, -12.32139453386874450 ) ) ;
#79897=CARTESIAN_POINT ( 'NONE',  ( -0.9999999999999943379, -1.409462824231155764E-15, 101.0455488498966758 ) ) ;
#79901=PRESENTATION_STYLE_ASSIGNMENT (( #4431 ) ) ;
#79913=CARTESIAN_POINT ( 'NONE',  ( 0.9999999999999997780, -67.04094093997568393, 11.34959271885065135 ) ) ;
#79985=AXIS2_PLACEMENT_3D ( 'NONE', #13612, #70283, #55131 ) ;
#79991=MECHANICAL_DESIGN_GEOMETRIC_PRESENTATION_REPRESENTATION('',(#85233),#78298);
#80002=DIRECTION ( 'NONE',  ( 0.000000000000000000, 1.000000000000000000, 0.000000000000000000 ) ) ;
#80006=ORIENTED_EDGE ( 'NONE', *, *, #20879, .F. ) ;
#80016=CARTESIAN_POINT ( 'NONE',  ( -6.593526337342319188, -48.85592895810358982, 39.35043480061310106 ) ) ;
#80026=CARTESIAN_POINT ( 'NONE',  ( 0.000000000000000000, -46.00000000000000000, 112.0000000000000000 ) ) ;
#80065=PLANE ( 'NONE',  #38921 ) ;
#80071=AXIS2_PLACEMENT_3D ( 'NONE', #59043, #9390, #52524 ) ;
#80093=DIRECTION ( 'NONE',  ( 0.000000000000000000, -0.8363101477004211137, 0.5482566341169980983 ) ) ;
#80128=EDGE_LOOP ( 'NONE', ( #33916, #15398, #7020, #69905 ) ) ;
#80166=SURFACE_STYLE_USAGE ( .BOTH. , #105513 ) ;
#80171=DIRECTION ( 'NONE',  ( 0.000000000000000000, 1.000000000000000000, 0.000000000000000000 ) ) ;
#80182=CARTESIAN_POINT ( 'NONE',  ( 4.225138137263999560, -1.061190178712521082, 104.4756818702664134 ) ) ;
#80183=( NAMED_UNIT ( * ) SI_UNIT ( $, .STERADIAN. ) SOLID_ANGLE_UNIT ( ) );
#80194=CARTESIAN_POINT ( 'NONE',  ( 5.000000000000000888, -12.24669057839810371, 9.804025467456250809 ) ) ;
#80204=CARTESIAN_POINT ( 'NONE',  ( 6.124999999999403144, -61.77251097506463395, 14.41094225130382078 ) ) ;
#80214=CARTESIAN_POINT ( 'NONE',  ( -7.369570678962171328, -14.99279962711093361, 15.08387202298855811 ) ) ;
#80250=CARTESIAN_POINT ( 'NONE',  ( -14.91858118607497019, 1.255821567010171884E-17, 15.00000000000000000 ) ) ;
#80258=AXIS2_PLACEMENT_3D ( 'NONE', #46741, #13829, #94379 ) ;
#80259=CARTESIAN_POINT ( 'NONE',  ( 3.801077171203084859, -1.110903940591797756, 104.1059035333591112 ) ) ;
#80283=SURFACE_STYLE_FILL_AREA ( #88405 ) ;
#80306=EDGE_LOOP ( 'NONE', ( #39412, #68078, #18462, #20120 ) ) ;
#80308=CARTESIAN_POINT ( 'NONE',  ( -5.000000000000079936, -12.24669057839772535, 9.804025467455284470 ) ) ;
#80310=ORIENTED_EDGE ( 'NONE', *, *, #76070, .F. ) ;
#80314=CARTESIAN_POINT ( 'NONE',  ( 3.105145020734076500, -49.42984310587327457, 103.2828773998820395 ) ) ;
#80331=STYLED_ITEM ( 'NONE', ( #71920 ), #65823 ) ;
#80343=UNCERTAINTY_MEASURE_WITH_UNIT (LENGTH_MEASURE( 1.000000000000000082E-05 ), #92908, 'distance_accuracy_value', 'NONE');
#80358=CARTESIAN_POINT ( 'NONE',  ( 13.45079846400083312, -54.00000000000000711, 23.11721482942554928 ) ) ;
#80377=CARTESIAN_POINT ( 'NONE',  ( -9.215420734788352775, -53.73283515818290823, 23.11721482942554928 ) ) ;
#80380=DIRECTION ( 'NONE',  ( -0.000000000000000000, -0.5482566341170008739, -0.8363101477004192263 ) ) ;
#80396=STYLED_ITEM ( 'NONE', ( #64586 ), #100988 ) ;
#80409=CARTESIAN_POINT ( 'NONE',  ( -4.999999999999993783, -46.00000000000000000, 102.2532056551910387 ) ) ;
#80424=CARTESIAN_POINT ( 'NONE',  ( -1.276674890354437375, -1.417245842567761834E-15, 101.3108517956189161 ) ) ;
#80439=CARTESIAN_POINT ( 'NONE',  ( 0.000000000000000000, 0.000000000000000000, 27.00000000000000000 ) ) ;
#80459=CARTESIAN_POINT ( 'NONE',  ( 3.375199637455089441, -49.11004099528027922, 104.1123102281673170 ) ) ;
#80469=CARTESIAN_POINT ( 'NONE',  ( 5.000000000000000000, -65.46413530816580817, 15.04248154712246688 ) ) ;
#80490=CARTESIAN_POINT ( 'NONE',  ( -3.455451579656851013, -49.16755827892872333, 44.00736102010382922 ) ) ;
#80502=CARTESIAN_POINT ( 'NONE',  ( -3.454253436624922458, -49.15858197120396511, 103.7259032015043090 ) ) ;
#80514=CARTESIAN_POINT ( 'NONE',  ( 4.970849588242775674, -3.447900702885856816, 102.2755693391596594 ) ) ;
#80520=EDGE_CURVE ( 'NONE', #97138, #44023, #46170, .T. ) ;
#80542=CARTESIAN_POINT ( 'NONE',  ( -6.125000000000002665, -15.62228920881133654, 14.41094225130411211 ) ) ;
#80602=( GEOMETRIC_REPRESENTATION_CONTEXT ( 3 ) GLOBAL_UNCERTAINTY_ASSIGNED_CONTEXT ( ( #72177 ) ) GLOBAL_UNIT_ASSIGNED_CONTEXT ( ( #23153, #72726, #31770 ) ) REPRESENTATION_CONTEXT ( 'NONE', 'WORKASPACE' ) );
#80616=( NAMED_UNIT ( * ) SI_UNIT ( $, .STERADIAN. ) SOLID_ANGLE_UNIT ( ) );
#80634=CARTESIAN_POINT ( 'NONE',  ( -4.176044994242080755, -67.08026818686849424, 13.14625702355704640 ) ) ;
#80644=( GEOMETRIC_REPRESENTATION_CONTEXT ( 3 ) GLOBAL_UNCERTAINTY_ASSIGNED_CONTEXT ( ( #103116 ) ) GLOBAL_UNIT_ASSIGNED_CONTEXT ( ( #36334, #62185, #93473 ) ) REPRESENTATION_CONTEXT ( 'NONE', 'WORKASPACE' ) );
#80653=( LENGTH_UNIT ( ) NAMED_UNIT ( * ) SI_UNIT ( .MILLI., .METRE. ) );
#80655=PRESENTATION_STYLE_ASSIGNMENT (( #40204 ) ) ;
#80673=STYLED_ITEM ( 'NONE', ( #76587 ), #44780 ) ;
#80683=DIRECTION ( 'NONE',  ( 0.000000000000000000, 0.000000000000000000, -1.000000000000000000 ) ) ;
#80700=CARTESIAN_POINT ( 'NONE',  ( 0.000000000000000000, -4.000000000000003553, 27.00000000000000000 ) ) ;
#80710=CARTESIAN_POINT ( 'NONE',  ( 4.284822031654965890, -1.092833614412281218, 104.4267991316945086 ) ) ;
#80713=CARTESIAN_POINT ( 'NONE',  ( -4.999999999999993783, -3.737948356800065319, 102.2532056550983128 ) ) ;
#80722=CARTESIAN_POINT ( 'NONE',  ( 5.000000000000000000, -14.11573700085330074, 9.475244962104019564 ) ) ;
#80731=AXIS2_PLACEMENT_3D ( 'NONE', #44062, #68340, #18209 ) ;
#80741=CARTESIAN_POINT ( 'NONE',  ( -4.971301086608930220, -62.51774646881273867, 12.85295273510877934 ) ) ;
#80779=CARTESIAN_POINT ( 'NONE',  ( -4.581218816254734705, -47.80086643547572578, 103.5404609598622443 ) ) ;
#80788=UNCERTAINTY_MEASURE_WITH_UNIT (LENGTH_MEASURE( 1.000000000000000082E-05 ), #50578, 'distance_accuracy_value', 'NONE');
#80793=( GEOMETRIC_REPRESENTATION_CONTEXT ( 3 ) GLOBAL_UNCERTAINTY_ASSIGNED_CONTEXT ( ( #46923 ) ) GLOBAL_UNIT_ASSIGNED_CONTEXT ( ( #70827, #62742, #54607 ) ) REPRESENTATION_CONTEXT ( 'NONE', 'WORKASPACE' ) );
#80796=( NAMED_UNIT ( * ) PLANE_ANGLE_UNIT ( ) SI_UNIT ( $, .RADIAN. ) );
#80836=CARTESIAN_POINT ( 'NONE',  ( -3.352941176470600304, -1.200583151104954283, 104.5794940929807524 ) ) ;
#80842=VERTEX_POINT ( 'NONE', #42305 ) ;
#80847=CARTESIAN_POINT ( 'NONE',  ( -5.000000000000161648, -12.33523449218733958, 10.71643274012945568 ) ) ;
#80872=CARTESIAN_POINT ( 'NONE',  ( 9.113097280746996987, -54.00000000000000711, 31.11721482942554928 ) ) ;
#80907=CARTESIAN_POINT ( 'NONE',  ( 9.677525045153895888, -50.98682064026158400, 24.47381311117452185 ) ) ;
#80924=CARTESIAN_POINT ( 'NONE',  ( 3.158718764008467961, -10.09043921932089205, -11.69018217342268251 ) ) ;
#80960=CARTESIAN_POINT ( 'NONE',  ( -7.117280438721564906, 3.124991324735574061, 14.67116533570241188 ) ) ;
#80993=CARTESIAN_POINT ( 'NONE',  ( -4.245164436738296132, -1.071807799196663913, 104.4592797835085349 ) ) ;
#81019=CARTESIAN_POINT ( 'NONE',  ( 0.000000000000000000, -48.79941684889506348, 112.0000000000000000 ) ) ;
#81031=CARTESIAN_POINT ( 'NONE',  ( -3.415272820067190462, -49.17042331394952726, 103.8818871663241339 ) ) ;
#81060=SURFACE_STYLE_FILL_AREA ( #71378 ) ;
#81074=CARTESIAN_POINT ( 'NONE',  ( -8.507502983303869115, -14.15209590839079290, 15.87009613063079883 ) ) ;
#81076=CARTESIAN_POINT ( 'NONE',  ( -6.784314825330817200, -48.10473606785564726, 39.24654408518340887 ) ) ;
#81080=AXIS2_PLACEMENT_3D ( 'NONE', #9001, #92054, #83429 ) ;
#81100=VERTEX_POINT ( 'NONE', #80502 ) ;
#81160=SURFACE_SIDE_STYLE ('',( #64991 ) ) ;
#81166=CARTESIAN_POINT ( 'NONE',  ( -3.410363394089228173, -69.13634986858798470, 13.41598603787099186 ) ) ;
#81208=CARTESIAN_POINT ( 'NONE',  ( -0.3201071873350568309, -69.98621145874830063, 12.99022420585184712 ) ) ;
#81221=DIRECTION ( 'NONE',  ( 1.000000000000000000, 0.000000000000000000, 0.000000000000000000 ) ) ;
#81232=EDGE_LOOP ( 'NONE', ( #43332, #19564, #41241, #9797, #35552, #89061, #62837, #12058, #36507, #65738, #89303, #6326, #27621, #75563 ) ) ;
#81236=CARTESIAN_POINT ( 'NONE',  ( 4.551587301587304957, -1.200583151104947843, 104.4018401814738155 ) ) ;
#81238=CARTESIAN_POINT ( 'NONE',  ( -4.348929473936903101, -1.784082633676044916, 103.6864098602936082 ) ) ;
#81248=CARTESIAN_POINT ( 'NONE',  ( 6.459500862574912183, -11.87485980093861748, 10.39038571060456917 ) ) ;
#81272=CARTESIAN_POINT ( 'NONE',  ( 5.688569873206568595, -47.04879514976503430, 103.9352763293502022 ) ) ;
#81299=CARTESIAN_POINT ( 'NONE',  ( -4.348929473936721912, -48.21591736632260705, 103.6864098602935513 ) ) ;
#81306=CARTESIAN_POINT ( 'NONE',  ( -3.910186774093565631, -48.93965723599501416, 104.5757226097576194 ) ) ;
#81337=AXIS2_PLACEMENT_3D ( 'NONE', #73057, #32110, #43380 ) ;
#81342=CARTESIAN_POINT ( 'NONE',  ( 30.00000000000000000, 0.000000000000000000, 0.000000000000000000 ) ) ;
#81362=( GEOMETRIC_REPRESENTATION_CONTEXT ( 3 ) GLOBAL_UNCERTAINTY_ASSIGNED_CONTEXT ( ( #52096 ) ) GLOBAL_UNIT_ASSIGNED_CONTEXT ( ( #79866, #83578, #91698 ) ) REPRESENTATION_CONTEXT ( 'NONE', 'WORKASPACE' ) );
#81368=CARTESIAN_POINT ( 'NONE',  ( -5.000000000000000000, -15.25461064037155801, 12.58690023576528816 ) ) ;
#81417=CARTESIAN_POINT ( 'NONE',  ( 3.231361472310781746, -68.72154468990221687, 13.04944395591344275 ) ) ;
#81429=CARTESIAN_POINT ( 'NONE',  ( -9.226882652173665988, -53.46780552115761509, 23.14412647329060491 ) ) ;
#81439=CARTESIAN_POINT ( 'NONE',  ( 4.669237227182971850, -14.10230343174356982, -8.329624332552803878 ) ) ;
#81486=EDGE_CURVE ( 'NONE', #76952, #5281, #29478, .T. ) ;
#81504=ORIENTED_EDGE ( 'NONE', *, *, #52145, .F. ) ;
#81519=CARTESIAN_POINT ( 'NONE',  ( -2.706785074969853877, -49.45229994201851298, 103.4519997648589538 ) ) ;
#81545=CARTESIAN_POINT ( 'NONE',  ( -3.351415491885648024, -49.00496204699513925, 104.3291447875367339 ) ) ;
#81589=CARTESIAN_POINT ( 'NONE',  ( 0.000000000000000000, -4.000000000000003553, 112.0000000000000000 ) ) ;
#81616=CARTESIAN_POINT ( 'NONE',  ( -5.802268690544500451, -3.456390741716395709, 103.8899761878886494 ) ) ;
#81630=ORIENTED_EDGE ( 'NONE', *, *, #49869, .T. ) ;
#81670=AXIS2_PLACEMENT_3D ( 'NONE', #34868, #74212, #33257 ) ;
#81673=( BOUNDED_SURFACE ( )  B_SPLINE_SURFACE ( 3, 2, ( 
 ( #11787, #59304, #69519 ),
 ( #93254, #11249, #51179 ),
 ( #68996, #18324, #3724 ),
 ( #84633, #19417, #19948 ),
 ( #44717, #52251, #28031 ),
 ( #36654, #85162, #77606 ),
 ( #61435, #102407, #27504 ),
 ( #52788, #85714, #44178 ),
 ( #75467, #60900, #9654 ),
 ( #26960, #84098, #1561 ),
 ( #10720, #100800, #10198 ),
 ( #77068, #94331, #20494 ),
 ( #43110, #101871, #93791 ),
 ( #60379, #67914, #36127 ) ),
 .UNSPECIFIED., .F., .F., .F. ) 
 B_SPLINE_SURFACE_WITH_KNOTS ( ( 4, 2, 2, 2, 2, 2, 4 ),
 ( 3, 3 ),
 ( 0.000000000000000000, 0.002028361404254495556, 0.004056722808508991113, 0.006085084212763486669, 0.008113445617017982225, 0.01217016842552697334, 0.01622689123403596445 ),
 ( 0.000000000000000000, 1.000000000000000000 ),
 .UNSPECIFIED. ) 
 GEOMETRIC_REPRESENTATION_ITEM ( )  RATIONAL_B_SPLINE_SURFACE ( (
 ( 1.000000000000000000, 0.7071067811865476838, 1.000000000000000000),
 ( 1.000000000000000000, 0.7270538103684279774, 1.000000000000000000),
 ( 1.000000000000000000, 0.7474775509999233014, 1.000000000000000000),
 ( 1.000000000000000000, 0.7877120837787837671, 1.000000000000000000),
 ( 1.000000000000000000, 0.8076198138824922657, 1.000000000000000000),
 ( 1.000000000000000000, 0.8446812442348378136, 1.000000000000000000),
 ( 1.000000000000000000, 0.8620019270876144724, 1.000000000000000000),
 ( 1.000000000000000000, 0.8939173377915230478, 1.000000000000000000),
 ( 1.000000000000000000, 0.9085622752435040805, 1.000000000000000000),
 ( 1.000000000000000000, 0.9477746975871859103, 1.000000000000000000),
 ( 1.000000000000000000, 0.9672053386932838448, 1.000000000000000000),
 ( 1.000000000000000000, 0.9933317393958381869, 1.000000000000000000),
 ( 1.000000000000000000, 1.000004063029856116, 1.000000000000000000),
 ( 1.000000000000000000, 1.000000000000000000, 1.000000000000000000) ) ) 
 REPRESENTATION_ITEM ( '' )  SURFACE ( )  );
#81683=CARTESIAN_POINT ( 'NONE',  ( -4.857172966777105749, -65.88657749106603490, 13.84720118471725314 ) ) ;
#81693=VECTOR ( 'NONE', #74302, 1000.000000000000000 ) ;
#81703=SURFACE_STYLE_FILL_AREA ( #88767 ) ;
#81727=UNCERTAINTY_MEASURE_WITH_UNIT (LENGTH_MEASURE( 1.000000000000000082E-05 ), #78317, 'distance_accuracy_value', 'NONE');
#81731=COLOUR_RGB ( '', 0.72549020, 0.75294118, 0.79215686) ;
#81741=CIRCLE ( 'NONE', #80071, 1.999999999999999778 ) ;
#81744=CARTESIAN_POINT ( 'NONE',  ( 3.185868710026582118, -70.04133017128596350, 13.36558777622290961 ) ) ;
#81774=CARTESIAN_POINT ( 'NONE',  ( 5.000000000000000888, -12.45789892056853532, 11.15956302481758300 ) ) ;
#81795=CARTESIAN_POINT ( 'NONE',  ( 4.464768147782974594, -48.00301508167390807, 102.6740199126133888 ) ) ;
#81796=EDGE_LOOP ( 'NONE', ( #94040, #12015, #98034, #47675 ) ) ;
#81805=ORIENTED_EDGE ( 'NONE', *, *, #78118, .T. ) ;
#81826=CARTESIAN_POINT ( 'NONE',  ( -4.725902370229717597, -47.47364726308471461, 103.4500010546492490 ) ) ;
#81829=CARTESIAN_POINT ( 'NONE',  ( 2.109905305157752764, -49.78906980863433063, 102.5368276707881137 ) ) ;
#81863=DIRECTION ( 'NONE',  ( 0.000000000000000000, 0.000000000000000000, 1.000000000000000000 ) ) ;
#81874=AXIS2_PLACEMENT_3D ( 'NONE', #19951, #3727, #28033 ) ;
#81891=CARTESIAN_POINT ( 'NONE',  ( -3.351410929237275571, -0.9950782767056199907, 104.3292106331608835 ) ) ;
#81901=CARTESIAN_POINT ( 'NONE',  ( -5.000000000000000000, -15.43644767549520580, 12.61250542914465811 ) ) ;
#81920=CARTESIAN_POINT ( 'NONE',  ( 9.923336144128633407, -3.232982157722304351, 15.16488001955000975 ) ) ;
#81967=STYLED_ITEM ( 'NONE', ( #34225 ), #88446 ) ;
#81972=EDGE_LOOP ( 'NONE', ( #52409, #92111, #106397, #84819 ) ) ;
#81974=CARTESIAN_POINT ( 'NONE',  ( 5.833333333333327708, -46.27176886455111315, 103.8776713793258750 ) ) ;
#81979=SURFACE_STYLE_USAGE ( .BOTH. , #55054 ) ;
#81982=EDGE_CURVE ( 'NONE', #15547, #25416, #25113, .T. ) ;
#81985=EDGE_CURVE ( 'NONE', #27751, #33663, #50200, .T. ) ;
#81987=EDGE_CURVE ( 'NONE', #33722, #97138, #89432, .T. ) ;
#82011=CARTESIAN_POINT ( 'NONE',  ( 0.000000000000000000, -46.00000000000000000, 112.0000000000000000 ) ) ;
#82025=CARTESIAN_POINT ( 'NONE',  ( 30.00000000000000000, 0.000000000000000000, 0.000000000000000000 ) ) ;
#82057=CIRCLE ( 'NONE', #35610, 4.000000000000001776 ) ;
#82058=PRESENTATION_STYLE_ASSIGNMENT (( #50232 ) ) ;
#82071=( NAMED_UNIT ( * ) SI_UNIT ( $, .STERADIAN. ) SOLID_ANGLE_UNIT ( ) );
#82089=CARTESIAN_POINT ( 'NONE',  ( -1.257498747432114650, -53.98194347854916231, 40.94539907224319109 ) ) ;
#82095=CARTESIAN_POINT ( 'NONE',  ( -3.375205455332774385, -49.11005739349737809, 104.1122683773797490 ) ) ;
#82105=CARTESIAN_POINT ( 'NONE',  ( 4.999999999999993783, -4.000000000000003553, 102.2532056551910387 ) ) ;
#82111=( NAMED_UNIT ( * ) PLANE_ANGLE_UNIT ( ) SI_UNIT ( $, .RADIAN. ) );
#82136=VERTEX_POINT ( 'NONE', #90484 ) ;
#82159=ORIENTED_EDGE ( 'NONE', *, *, #25919, .T. ) ;
#82197=CARTESIAN_POINT ( 'NONE',  ( -4.003587701499910168, -48.94962346669722564, 104.5574048719304301 ) ) ;
#82210=( GEOMETRIC_REPRESENTATION_CONTEXT ( 3 ) GLOBAL_UNCERTAINTY_ASSIGNED_CONTEXT ( ( #72004 ) ) GLOBAL_UNIT_ASSIGNED_CONTEXT ( ( #64316, #87528, #12550 ) ) REPRESENTATION_CONTEXT ( 'NONE', 'WORKASPACE' ) );
#82231=CARTESIAN_POINT ( 'NONE',  ( -3.379087390341638741, -69.90378107111884276, 13.41250649815817830 ) ) ;
#82232=CARTESIAN_POINT ( 'NONE',  ( 2.323340773569810391, -49.78385856118777752, 102.3935653434436830 ) ) ;
#82240=CARTESIAN_POINT ( 'NONE',  ( 3.963177594442894858, -48.71124122727862016, 103.9032426698779403 ) ) ;
#82243=ORIENTED_EDGE ( 'NONE', *, *, #5400, .F. ) ;
#82252=( NAMED_UNIT ( * ) PLANE_ANGLE_UNIT ( ) SI_UNIT ( $, .RADIAN. ) );
#82269=CARTESIAN_POINT ( 'NONE',  ( -5.000000000000000000, -42.29207564866745628, 4.347359059871835463 ) ) ;
#82290=CARTESIAN_POINT ( 'NONE',  ( 9.098035229686777470, -13.55677388152806806, 16.35626862400982517 ) ) ;
#82296=CARTESIAN_POINT ( 'NONE',  ( 1.364254058415848236, -70.64897445287397204, 13.05800878275180033 ) ) ;
#82298=FILL_AREA_STYLE ('',( #49389 ) ) ;
#82313=CARTESIAN_POINT ( 'NONE',  ( 5.683639242321874896, -2.934261738049317003, 103.9372442403038264 ) ) ;
#82325=CARTESIAN_POINT ( 'NONE',  ( 5.000000000000000000, -14.98862091075390701, 12.50620160667418368 ) ) ;
#82349=CARTESIAN_POINT ( 'NONE',  ( 4.581218816254647663, -47.80086643547572578, 103.5404609598622443 ) ) ;
#82362=STYLED_ITEM ( 'NONE', ( #12928 ), #26717 ) ;
#82380=EDGE_CURVE ( 'NONE', #57615, #99036, #93086, .T. ) ;
#82413=CARTESIAN_POINT ( 'NONE',  ( 4.147911490760948894, -48.94936983711307477, 104.5115833471886191 ) ) ;
#82424=AXIS2_PLACEMENT_3D ( 'NONE', #82683, #41695, #98337 ) ;
#82427=CARTESIAN_POINT ( 'NONE',  ( -6.633460018062062424, 3.141069750844269759, 14.66750529547399218 ) ) ;
#82443=CARTESIAN_POINT ( 'NONE',  ( -3.386166401410786619, -0.8620773598010494920, 104.0373207615035085 ) ) ;
#82446=ORIENTED_EDGE ( 'NONE', *, *, #77516, .T. ) ;
#82449=CARTESIAN_POINT ( 'NONE',  ( -5.000000000000000000, -13.87446176118090868, 11.25142367425977774 ) ) ;
#82474=CARTESIAN_POINT ( 'NONE',  ( 12.40668049911506721, -3.381773713679836924, 20.61118434233718233 ) ) ;
#82488=ORIENTED_EDGE ( 'NONE', *, *, #46775, .F. ) ;
#82493=( BOUNDED_SURFACE ( )  B_SPLINE_SURFACE ( 3, 2, ( 
 ( #12328, #38754, #24183 ),
 ( #7414, #49475, #106106 ),
 ( #89943, #81299, #48929 ),
 ( #106646, #47872, #8486 ),
 ( #105588, #80779, #97484 ),
 ( #24703, #90478, #40326 ),
 ( #23640, #81826, #56495 ),
 ( #7950, #39813, #65135 ),
 ( #98031, #57026, #25243 ),
 ( #32254, #16047, #16585 ),
 ( #41391, #73209, #32797 ),
 ( #40856, #58098, #89426 ) ),
 .UNSPECIFIED., .F., .F., .F. ) 
 B_SPLINE_SURFACE_WITH_KNOTS ( ( 4, 2, 2, 2, 2, 4 ),
 ( 3, 3 ),
 ( -1.734723475976807094E-18, 0.001187588843296132415, 0.001781383264944199490, 0.002375177686592266565, 0.003562766529888400716, 0.004750355373184534866 ),
 ( 0.000000000000000000, 1.000000000000000000 ),
 .UNSPECIFIED. ) 
 GEOMETRIC_REPRESENTATION_ITEM ( )  RATIONAL_B_SPLINE_SURFACE ( (
 ( 1.000000000000000000, 0.9359444767143318966, 1.000000000000000000),
 ( 1.000000000000000000, 0.9295581727144616169, 1.000000000000000000),
 ( 1.000000000000000000, 0.9234593375674587934, 1.000000000000000000),
 ( 1.000000000000000000, 0.9150808072273582949, 1.000000000000000000),
 ( 1.000000000000000000, 0.9124161408737813117, 1.000000000000000000),
 ( 1.000000000000000000, 0.9074047588826391619, 1.000000000000000000),
 ( 1.000000000000000000, 0.9050663310859912158, 1.000000000000000000),
 ( 1.000000000000000000, 0.8987692007139892469, 1.000000000000000000),
 ( 1.000000000000000000, 0.8954627112851045734, 1.000000000000000000),
 ( 1.000000000000000000, 0.8909338199770817646, 1.000000000000000000),
 ( 1.000000000000000000, 0.8897377579434112560, 1.000000000000000000),
 ( 1.000000000000000000, 0.8897565210026093796, 1.000000000000000000) ) ) 
 REPRESENTATION_ITEM ( '' )  SURFACE ( )  );
#82494=VERTEX_POINT ( 'NONE', #91825 ) ;
#82511=CARTESIAN_POINT ( 'NONE',  ( 9.423567810130279554, -51.98776212902039617, 23.65038982378345622 ) ) ;
#82558=FILL_AREA_STYLE ('',( #75523 ) ) ;
#82604=CARTESIAN_POINT ( 'NONE',  ( 9.442659817596066318, -56.44252752747822655, 30.29540378708609794 ) ) ;
#82610=CARTESIAN_POINT ( 'NONE',  ( 1.000000000000000000, -26.67919295183541095, -6.179716592098927208 ) ) ;
#82613=CARTESIAN_POINT ( 'NONE',  ( 15.90614609307868932, -3.157894736842108863, 14.66382285868950852 ) ) ;
#82650=CARTESIAN_POINT ( 'NONE',  ( -3.566423465315849750, -0.9305320722653663834, 103.5097305745183576 ) ) ;
#82656=( LENGTH_UNIT ( ) NAMED_UNIT ( * ) SI_UNIT ( .MILLI., .METRE. ) );
#82659=FILL_AREA_STYLE ('',( #74026 ) ) ;
#82683=CARTESIAN_POINT ( 'NONE',  ( 0.000000000000000000, -4.000000000000003553, 112.0000000000000000 ) ) ;
#82696=DIRECTION ( 'NONE',  ( 0.000000000000000000, 1.000000000000000000, 0.000000000000000000 ) ) ;
#82710=CARTESIAN_POINT ( 'NONE',  ( -4.442085480450870705, -13.39242828886067826, -9.057376035804495018 ) ) ;
#82758=CARTESIAN_POINT ( 'NONE',  ( -15.94660519413343813, -2.877896041580118691, 14.72412135074108619 ) ) ;
#82765=EDGE_LOOP ( 'NONE', ( #5977, #95315, #91546, #40600, #22032, #99536 ) ) ;
#82773=CARTESIAN_POINT ( 'NONE',  ( -3.958687006365356975, -68.40474125555384433, 13.56240833589197514 ) ) ;
#82793=AXIS2_PLACEMENT_3D ( 'NONE', #93706, #43553, #77520 ) ;
#82829=CARTESIAN_POINT ( 'NONE',  ( 12.06828428419903076, -6.477429270778858772, 19.90153083308154081 ) ) ;
#82834=CARTESIAN_POINT ( 'NONE',  ( 3.350244361011366578, -68.60885486349103246, 13.06616826839196221 ) ) ;
#82847=( LENGTH_UNIT ( ) NAMED_UNIT ( * ) SI_UNIT ( .MILLI., .METRE. ) );
#82853=UNCERTAINTY_MEASURE_WITH_UNIT (LENGTH_MEASURE( 1.000000000000000082E-05 ), #93826, 'distance_accuracy_value', 'NONE');
#82861=EDGE_CURVE ( 'NONE', #40039, #41445, #55489, .T. ) ;
#82863=CARTESIAN_POINT ( 'NONE',  ( 4.999999999999960920, -12.67914701489953622, 11.71967441881639438 ) ) ;
#82880=CARTESIAN_POINT ( 'NONE',  ( 5.990573850131376332, -14.42843120744217877, 14.14171987952399512 ) ) ;
#82884=CARTESIAN_POINT ( 'NONE',  ( 4.999999999999993783, -46.26205164319991070, 102.2532056550983128 ) ) ;
#82886=EDGE_LOOP ( 'NONE', ( #44129, #18757, #81630, #95629 ) ) ;
#82922=SURFACE_STYLE_USAGE ( .BOTH. , #33335 ) ;
#82929=( LENGTH_UNIT ( ) NAMED_UNIT ( * ) SI_UNIT ( .MILLI., .METRE. ) );
#82930=( NAMED_UNIT ( * ) SI_UNIT ( $, .STERADIAN. ) SOLID_ANGLE_UNIT ( ) );
#82998=ADVANCED_FACE ( 'NONE', ( #15663 ), #16196, .T. ) ;
#83004=CARTESIAN_POINT ( 'NONE',  ( 9.960411669762633480, -2.966372377354413281, 15.28833013202438451 ) ) ;
#83013=UNCERTAINTY_MEASURE_WITH_UNIT (LENGTH_MEASURE( 1.000000000000000082E-05 ), #44311, 'distance_accuracy_value', 'NONE');
#83018=CARTESIAN_POINT ( 'NONE',  ( -0.9999999999999943379, 0.000000000000000000, 101.0455488498966758 ) ) ;
#83053=EDGE_CURVE ( 'NONE', #76724, #12840, #21159, .T. ) ;
#83060=DIRECTION ( 'NONE',  ( -1.000000000000000000, -0.000000000000000000, -0.000000000000000000 ) ) ;
#83082=( LENGTH_UNIT ( ) NAMED_UNIT ( * ) SI_UNIT ( .MILLI., .METRE. ) );
#83112=( GEOMETRIC_REPRESENTATION_CONTEXT ( 3 ) GLOBAL_UNCERTAINTY_ASSIGNED_CONTEXT ( ( #93411 ) ) GLOBAL_UNIT_ASSIGNED_CONTEXT ( ( #46948, #5957, #24830 ) ) REPRESENTATION_CONTEXT ( 'NONE', 'WORKASPACE' ) );
#83134=CARTESIAN_POINT ( 'NONE',  ( -4.284822031655025398, -1.092833614412312304, 104.4267991316944517 ) ) ;
#83142=CARTESIAN_POINT ( 'NONE',  ( 10.87267833667801398, -11.19338281451489081, 9.987533465452024473 ) ) ;
#83146=CARTESIAN_POINT ( 'NONE',  ( -3.054195049253744187, -49.15491390355075652, 104.0345731970081147 ) ) ;
#83196=CARTESIAN_POINT ( 'NONE',  ( -5.000000000000000000, -65.47006268292325615, 15.04566776836145614 ) ) ;
#83233=CARTESIAN_POINT ( 'NONE',  ( -5.596957125887390028, -2.684245481662593580, 103.9718581041641698 ) ) ;
#83235=CARTESIAN_POINT ( 'NONE',  ( -4.837657582855711347, -12.04835165414239739, -8.962574246965099078 ) ) ;
#83307=CARTESIAN_POINT ( 'NONE',  ( 4.284822031654944574, -48.90716638558773610, 104.4267991316944943 ) ) ;
#83312=MECHANICAL_DESIGN_GEOMETRIC_PRESENTATION_REPRESENTATION('',(#24743),#86801);
#83359=CARTESIAN_POINT ( 'NONE',  ( 2.762373655041346687, -70.28365225073746103, 13.27352019214896828 ) ) ;
#83362=SURFACE_STYLE_FILL_AREA ( #82298 ) ;
#83372=EDGE_LOOP ( 'NONE', ( #92327, #64039, #66863, #28878 ) ) ;
#83414=CARTESIAN_POINT ( 'NONE',  ( 5.833333333333329485, -50.00000000000000000, 103.8776713793258608 ) ) ;
#83418=EDGE_CURVE ( 'NONE', #25863, #76724, #34993, .T. ) ;
#83429=DIRECTION ( 'NONE',  ( 0.000000000000000000, 0.000000000000000000, 1.000000000000000000 ) ) ;
#83443=ORIENTED_EDGE ( 'NONE', *, *, #93290, .F. ) ;
#83447=PRESENTATION_STYLE_ASSIGNMENT (( #82922 ) ) ;
#83452=COLOUR_RGB ( '', 0.31764706, 0.68627451, 0.89019608) ;
#83459=( GEOMETRIC_REPRESENTATION_CONTEXT ( 3 ) GLOBAL_UNCERTAINTY_ASSIGNED_CONTEXT ( ( #75705 ) ) GLOBAL_UNIT_ASSIGNED_CONTEXT ( ( #15752, #25482, #82071 ) ) REPRESENTATION_CONTEXT ( 'NONE', 'WORKASPACE' ) );
#83502=EDGE_LOOP ( 'NONE', ( #10146, #82488, #99262, #103830 ) ) ;
#83510=DIRECTION ( 'NONE',  ( 0.000000000000000000, 1.000000000000000000, 0.000000000000000000 ) ) ;
#83511=B_SPLINE_CURVE_WITH_KNOTS ( 'NONE', 3,
 ( #8254, #7718, #48178, #64913, #72981, #105887 ),
 .UNSPECIFIED., .F., .F.,
 ( 4, 2, 4 ),
 ( 8.673617379884035472E-19, 0.0003910247833730961706, 0.0007820495667461914739 ),
 .UNSPECIFIED. ) ;
#83523=STYLED_ITEM ( 'NONE', ( #61517 ), #56475 ) ;
#83577=( NAMED_UNIT ( * ) PLANE_ANGLE_UNIT ( ) SI_UNIT ( $, .RADIAN. ) );
#83578=( NAMED_UNIT ( * ) PLANE_ANGLE_UNIT ( ) SI_UNIT ( $, .RADIAN. ) );
#83601=CARTESIAN_POINT ( 'NONE',  ( -12.39875862467593848, -3.846090740250397655, 20.49813959098556282 ) ) ;
#83602=STYLED_ITEM ( 'NONE', ( #58386 ), #13526 ) ;
#83614=SURFACE_STYLE_USAGE ( .BOTH. , #52315 ) ;
#83627=CARTESIAN_POINT ( 'NONE',  ( -4.506266729858579012, -1.182839587743470977, 104.3949571352749643 ) ) ;
#83655=CARTESIAN_POINT ( 'NONE',  ( 12.57292557173279590, -10.06217675253460975, 11.13464401508594115 ) ) ;
#83660=UNCERTAINTY_MEASURE_WITH_UNIT (LENGTH_MEASURE( 1.000000000000000082E-05 ), #67984, 'distance_accuracy_value', 'NONE');
#83662=CARTESIAN_POINT ( 'NONE',  ( -1.909182100399782422, -49.86416495494171386, 102.2488568920577734 ) ) ;
#83679=DIRECTION ( 'NONE',  ( 0.000000000000000000, 0.000000000000000000, -1.000000000000000000 ) ) ;
#83681=CARTESIAN_POINT ( 'NONE',  ( 5.000000000000000000, -42.29200263518463032, 4.347328673565829860 ) ) ;
#83697=CARTESIAN_POINT ( 'NONE',  ( -3.702395615612349200, -1.049538900538678154, 103.3251893371222536 ) ) ;
#83698=UNCERTAINTY_MEASURE_WITH_UNIT (LENGTH_MEASURE( 1.000000000000000082E-05 ), #44970, 'distance_accuracy_value', 'NONE');
#83716=CARTESIAN_POINT ( 'NONE',  ( -5.000000000005067946, -59.33879011280326665, 7.480853745603068816 ) ) ;
#83744=AXIS2_PLACEMENT_3D ( 'NONE', #9889, #60078, #92942 ) ;
#83758=( NAMED_UNIT ( * ) PLANE_ANGLE_UNIT ( ) SI_UNIT ( $, .RADIAN. ) );
#83773=CARTESIAN_POINT ( 'NONE',  ( 14.85870402376584742, -6.955274255831150221, 13.29338602724358509 ) ) ;
#83785=CARTESIAN_POINT ( 'NONE',  ( 1.459339698542529762, -0.03374778880127472791, 101.6368042612139249 ) ) ;
#83786=CARTESIAN_POINT ( 'NONE',  ( 3.566423465315838204, -49.06946792773464239, 103.5097305745183434 ) ) ;
#83798=SURFACE_STYLE_FILL_AREA ( #96939 ) ;
#83800=UNCERTAINTY_MEASURE_WITH_UNIT (LENGTH_MEASURE( 1.000000000000000082E-05 ), #3972, 'distance_accuracy_value', 'NONE');
#83814=CARTESIAN_POINT ( 'NONE',  ( -15.89515006508820960, -2.031693691641069055, 14.86243156795516640 ) ) ;
#83830=DIRECTION ( 'NONE',  ( 0.000000000000000000, 1.000000000000000000, 0.000000000000000000 ) ) ;
#83832=ORIENTED_EDGE ( 'NONE', *, *, #14482, .F. ) ;
#83836=CARTESIAN_POINT ( 'NONE',  ( 3.801077171203065319, -48.88909605940821734, 104.1059035333590828 ) ) ;
#83845=CARTESIAN_POINT ( 'NONE',  ( 4.999999999999995559, -46.00000000000000000, 42.58845726811990318 ) ) ;
#83846=COLOUR_RGB ( '', 0.72549020, 0.75294118, 0.79215686) ;
#83882=EDGE_CURVE ( 'NONE', #74417, #39260, #11872, .T. ) ;
#83889=CARTESIAN_POINT ( 'NONE',  ( -3.454253436624922458, -49.15858197120396511, 103.7259032015043090 ) ) ;
#83892=CARTESIAN_POINT ( 'NONE',  ( 5.795768137672492770, -65.04849424565485094, 14.25540627950699246 ) ) ;
#83910=AXIS2_PLACEMENT_3D ( 'NONE', #104605, #15593, #49009 ) ;
#83924=CARTESIAN_POINT ( 'NONE',  ( 5.000000000000000000, -13.89959410954354802, 11.33893914917864087 ) ) ;
#83925=CARTESIAN_POINT ( 'NONE',  ( 30.00000000000000000, 0.000000000000000000, 9.000000000000000000 ) ) ;
#83938=CARTESIAN_POINT ( 'NONE',  ( -5.833333333333328596, -46.00000000000000000, 103.8776713793258608 ) ) ;
#84042=CARTESIAN_POINT ( 'NONE',  ( -4.225130582364203136, -1.061186173226825069, 104.4756880579355283 ) ) ;
#84053=CYLINDRICAL_SURFACE ( 'NONE', #54701, 4.000000000000000000 ) ;
#84058=( GEOMETRIC_REPRESENTATION_CONTEXT ( 3 ) GLOBAL_UNCERTAINTY_ASSIGNED_CONTEXT ( ( #48054 ) ) GLOBAL_UNIT_ASSIGNED_CONTEXT ( ( #77020, #29962, #93210 ) ) REPRESENTATION_CONTEXT ( 'NONE', 'WORKASPACE' ) );
#84069=CARTESIAN_POINT ( 'NONE',  ( 9.300691195493925534, -2.624086112765174672, 14.76496043385272827 ) ) ;
#84098=CARTESIAN_POINT ( 'NONE',  ( 3.717184411742878503, -9.782292260247256621, -11.42823731287383637 ) ) ;
#84110=STYLED_ITEM ( 'NONE', ( #99800 ), #76156 ) ;
#84116=COLOUR_RGB ( '', 0.40784314, 0.44705882, 0.49803922) ;
#84136=CIRCLE ( 'NONE', #9373, 11.00000000000001066 ) ;
#84167=DIRECTION ( 'NONE',  ( 0.000000000000000000, 1.000000000000000000, 0.000000000000000000 ) ) ;
#84174=ORIENTED_EDGE ( 'NONE', *, *, #11163, .T. ) ;
#84181=EDGE_LOOP ( 'NONE', ( #80310, #38106 ) ) ;
#84209=FILL_AREA_STYLE ('',( #85824 ) ) ;
#84210=CARTESIAN_POINT ( 'NONE',  ( 9.478973614161615657, -11.83509979120333178, 9.222223356601535471 ) ) ;
#84235=CARTESIAN_POINT ( 'NONE',  ( 0.000000000000000000, -78.00000000000000000, 37.00000000000000000 ) ) ;
#84240=EDGE_LOOP ( 'NONE', ( #19912, #102507, #103307, #90547 ) ) ;
#84242=FACE_OUTER_BOUND ( 'NONE', #2498, .T. ) ;
#84255=LINE ( 'NONE', #35743, #18749 ) ;
#84259=CARTESIAN_POINT ( 'NONE',  ( -27.99999999999999645, 0.000000000000000000, 0.000000000000000000 ) ) ;
#84266=SURFACE_STYLE_USAGE ( .BOTH. , #91309 ) ;
#84302=CARTESIAN_POINT ( 'NONE',  ( 3.358578016107284014, -0.9723468250019194903, 104.2746939430690389 ) ) ;
#84305=CARTESIAN_POINT ( 'NONE',  ( -6.708832649680421589, -13.06702039274563454, -7.389177399647482325 ) ) ;
#84309=CARTESIAN_POINT ( 'NONE',  ( -8.188359067971299865, -12.25820946039680592, 8.650503056542792280 ) ) ;
#84310=CARTESIAN_POINT ( 'NONE',  ( -6.594225035609122543, -11.92007582869070426, 9.808253832663700322 ) ) ;
#84327=SURFACE_SIDE_STYLE ('',( #100498 ) ) ;
#84343=CARTESIAN_POINT ( 'NONE',  ( 3.857142857142854986, -1.200583151104943624, 103.1763305333244176 ) ) ;
#84391=CARTESIAN_POINT ( 'NONE',  ( 4.165510012636465476, -48.44870269470101221, 43.44044287971949103 ) ) ;
#84444=CIRCLE ( 'NONE', #79275, 2.000000000000000000 ) ;
#84466=CARTESIAN_POINT ( 'NONE',  ( 6.073384266099709272, -15.26795065999747436, 14.38582946077996283 ) ) ;
#84543=DIRECTION ( 'NONE',  ( 0.000000000000000000, -1.000000000000000000, 0.000000000000000000 ) ) ;
#84581=( NAMED_UNIT ( * ) SI_UNIT ( $, .STERADIAN. ) SOLID_ANGLE_UNIT ( ) );
#84594=DIRECTION ( 'NONE',  ( 0.000000000000000000, 0.000000000000000000, 1.000000000000000000 ) ) ;
#84612=CARTESIAN_POINT ( 'NONE',  ( 3.841398122528194126, -48.92777529680783033, 104.5835869663331579 ) ) ;
#84633=CARTESIAN_POINT ( 'NONE',  ( 6.708832649680419813, -13.06702039274575888, -7.389177399647247846 ) ) ;
#84662=FACE_OUTER_BOUND ( 'NONE', #106086, .T. ) ;
#84681=FILL_AREA_STYLE ('',( #2143 ) ) ;
#84706=CARTESIAN_POINT ( 'NONE',  ( -4.284822031654928587, -1.092833614412262122, 104.4267991316945370 ) ) ;
#84710=DIRECTION ( 'NONE',  ( 0.000000000000000000, 0.000000000000000000, 1.000000000000000000 ) ) ;
#84716=CARTESIAN_POINT ( 'NONE',  ( -5.000000000000000000, -14.21727251091160404, 9.320362779991915758 ) ) ;
#84747=UNCERTAINTY_MEASURE_WITH_UNIT (LENGTH_MEASURE( 1.000000000000000082E-05 ), #70043, 'distance_accuracy_value', 'NONE');
#84768=CARTESIAN_POINT ( 'NONE',  ( 1.276500347551263737, -50.00000000000000000, 101.3106844269525340 ) ) ;
#84773=PRESENTATION_STYLE_ASSIGNMENT (( #33579 ) ) ;
#84783=CARTESIAN_POINT ( 'NONE',  ( -3.454253436624934004, -0.8414180287960428828, 103.7259032015043232 ) ) ;
#84796=CARTESIAN_POINT ( 'NONE',  ( 9.081552814318261113, -1.588707212875608343, 15.49454491418383739 ) ) ;
#84800=CARTESIAN_POINT ( 'NONE',  ( -5.000000000000000000, -68.02685735654881682, 16.47960771717093209 ) ) ;
#84818=MECHANICAL_DESIGN_GEOMETRIC_PRESENTATION_REPRESENTATION('',(#2111),#77897);
#84819=ORIENTED_EDGE ( 'NONE', *, *, #93623, .F. ) ;
#84820=ADVANCED_FACE ( 'NONE', ( #41974 ), #26536, .T. ) ;
#84829=( NAMED_UNIT ( * ) PLANE_ANGLE_UNIT ( ) SI_UNIT ( $, .RADIAN. ) );
#84839=CARTESIAN_POINT ( 'NONE',  ( -7.599068113629535937, -12.41377559130418717, 8.423488589708485463 ) ) ;
#84851=CARTESIAN_POINT ( 'NONE',  ( 10.90053399926999766, -11.19007817188768072, 9.996270789008875113 ) ) ;
#84872=CARTESIAN_POINT ( 'NONE',  ( 4.725902370230581795, -2.526352736915794761, 103.4500010546506559 ) ) ;
#84873=AXIS2_PLACEMENT_3D ( 'NONE', #101604, #3440, #21251 ) ;
#84879=ORIENTED_EDGE ( 'NONE', *, *, #55932, .T. ) ;
#84885=DIRECTION ( 'NONE',  ( -0.8257009859296325915, 0.000000000000000000, -0.5641080409237514415 ) ) ;
#84921=CARTESIAN_POINT ( 'NONE',  ( 1.625799246043344359, -50.01537087125233683, 40.95671946476290515 ) ) ;
#84945=EDGE_LOOP ( 'NONE', ( #35769, #101221, #50391, #73963 ) ) ;
#84997=CARTESIAN_POINT ( 'NONE',  ( 1.678729582439481227, -5.952306540456972606, -13.77787289860723696 ) ) ;
#85010=CARTESIAN_POINT ( 'NONE',  ( -13.83891950279925354, -57.46707097098471451, 29.12888379965242081 ) ) ;
#85013=CARTESIAN_POINT ( 'NONE',  ( 12.41665141885566470, -3.617041646665052568, 20.56186768168683088 ) ) ;
#85020=UNCERTAINTY_MEASURE_WITH_UNIT (LENGTH_MEASURE( 1.000000000000000082E-05 ), #62566, 'distance_accuracy_value', 'NONE');
#85059=CARTESIAN_POINT ( 'NONE',  ( -4.999999999999993783, -3.723962137281044971, 102.2532056551910529 ) ) ;
#85095=VERTEX_POINT ( 'NONE', #10021 ) ;
#85105=ADVANCED_FACE ( 'NONE', ( #41323 ), #92002, .F. ) ;
#85108=ORIENTED_EDGE ( 'NONE', *, *, #37199, .T. ) ;
#85112=CARTESIAN_POINT ( 'NONE',  ( -5.000000000000000000, -15.62228920881132765, 12.61250543006183911 ) ) ;
#85137=CARTESIAN_POINT ( 'NONE',  ( 3.349796915291911148, -48.86785030187898826, 104.5044954676193214 ) ) ;
#85162=CARTESIAN_POINT ( 'NONE',  ( 4.962899348968470292, -12.37352932398349381, -8.506080509221449759 ) ) ;
#85168=( BOUNDED_SURFACE ( )  B_SPLINE_SURFACE ( 3, 2, ( 
 ( #11560, #103771, #37489 ),
 ( #20257, #36434, #45029 ),
 ( #62796, #4023, #103249 ),
 ( #13686, #70352, #12620 ),
 ( #77378, #95685, #52556 ),
 ( #87604, #45557, #4550 ),
 ( #54667, #95166, #44491 ),
 ( #29394, #36950, #78427 ),
 ( #69304, #46596, #21299 ),
 ( #54136, #2945, #87077 ),
 ( #13150, #35899, #68776 ),
 ( #78961, #101656, #27815 ),
 ( #60684, #93571, #19719 ),
 ( #53104, #102178, #28327 ),
 ( #69818, #86027, #61204 ),
 ( #12097, #102715, #94648 ),
 ( #28879, #61750, #15290 ),
 ( #80016, #7187, #22885 ),
 ( #64390, #56254, #40102 ),
 ( #81076, #97266, #88132 ),
 ( #55722, #23411, #48175 ),
 ( #89188, #71936, #14214 ),
 ( #31509, #48701, #47644 ),
 ( #64908, #63863, #6126 ) ),
 .UNSPECIFIED., .F., .F., .F. ) 
 B_SPLINE_SURFACE_WITH_KNOTS ( ( 4, 2, 2, 2, 2, 2, 2, 2, 2, 2, 2, 4 ),
 ( 3, 3 ),
 ( 0.005037129470918477389, 0.006635042084548149581, 0.007433998391362986111, 0.008232954698177821773, 0.009830867311807493097, 0.01062982361862232876, 0.01142877992543716442, 0.01302669253906683575, 0.01462460515269650881, 0.01542356145951134447, 0.01622251776632618187, 0.01782043037995585319 ),
 ( 0.000000000000000000, 1.000000000000000000 ),
 .UNSPECIFIED. ) 
 GEOMETRIC_REPRESENTATION_ITEM ( )  RATIONAL_B_SPLINE_SURFACE ( (
 ( 1.000000000000000000, 0.7071067811865475727, 1.000000000000000000),
 ( 1.000000000000000000, 0.7084299270926217584, 1.000000000000000000),
 ( 1.000000000000000000, 0.7118707319821261370, 1.000000000000000000),
 ( 1.000000000000000000, 0.7196931121702430101, 1.000000000000000000),
 ( 1.000000000000000000, 0.7227437164891366006, 1.000000000000000000),
 ( 1.000000000000000000, 0.7296388212890008163, 1.000000000000000000),
 ( 1.000000000000000000, 0.7334745704062100025, 1.000000000000000000),
 ( 1.000000000000000000, 0.7457129707556888754, 1.000000000000000000),
 ( 1.000000000000000000, 0.7549127490209673885, 1.000000000000000000),
 ( 1.000000000000000000, 0.7694591811115146784, 1.000000000000000000),
 ( 1.000000000000000000, 0.7744510510067527109, 1.000000000000000000),
 ( 1.000000000000000000, 0.7843714700247860216, 1.000000000000000000),
 ( 1.000000000000000000, 0.7893201836189067677, 1.000000000000000000),
 ( 1.000000000000000000, 0.8039615404448176017, 1.000000000000000000),
 ( 1.000000000000000000, 0.8134756678392851548, 1.000000000000000000),
 ( 1.000000000000000000, 0.8310114419075367298, 1.000000000000000000),
 ( 1.000000000000000000, 0.8387987601958035722, 1.000000000000000000),
 ( 1.000000000000000000, 0.8485725036619826689, 1.000000000000000000),
 ( 1.000000000000000000, 0.8515123028897164659, 1.000000000000000000),
 ( 1.000000000000000000, 0.8566700882282884955, 1.000000000000000000),
 ( 1.000000000000000000, 0.8588953665494961642, 1.000000000000000000),
 ( 1.000000000000000000, 0.8642157076431438156, 1.000000000000000000),
 ( 1.000000000000000000, 0.8660228936532952115, 1.000000000000000000),
 ( 1.000000000000000000, 0.8660254037844388186, 1.000000000000000000) ) ) 
 REPRESENTATION_ITEM ( '' )  SURFACE ( )  );
#85186=MECHANICAL_DESIGN_GEOMETRIC_PRESENTATION_REPRESENTATION('',(#24920),#14560);
#85197=FACE_OUTER_BOUND ( 'NONE', #31151, .T. ) ;
#85233=STYLED_ITEM ( 'NONE', ( #101590 ), #85431 ) ;
#85236=STYLED_ITEM ( 'NONE', ( #71486 ), #13091 ) ;
#85244=( NAMED_UNIT ( * ) SI_UNIT ( $, .STERADIAN. ) SOLID_ANGLE_UNIT ( ) );
#85296=VERTEX_POINT ( 'NONE', #64450 ) ;
#85298=PRESENTATION_STYLE_ASSIGNMENT (( #18463 ) ) ;
#85311=MECHANICAL_DESIGN_GEOMETRIC_PRESENTATION_REPRESENTATION('',(#83523),#31890);
#85317=DIRECTION ( 'NONE',  ( -1.000000000000000000, 0.000000000000000000, 0.000000000000000000 ) ) ;
#85358=CARTESIAN_POINT ( 'NONE',  ( 0.000000000000000000, -78.00000000000000000, 27.00000000000000000 ) ) ;
#85375=CARTESIAN_POINT ( 'NONE',  ( -6.033336773385747698, -14.92884390011200502, 14.31563199681415632 ) ) ;
#85390=CARTESIAN_POINT ( 'NONE',  ( 13.98725534264629466, -57.97295057622655179, 27.65002740835610240 ) ) ;
#85394=VERTEX_POINT ( 'NONE', #68708 ) ;
#85401=CARTESIAN_POINT ( 'NONE',  ( 2.109839796630671227, -0.2109020744221661026, 102.5367317923686556 ) ) ;
#85409=CARTESIAN_POINT ( 'NONE',  ( 5.833333333333327708, -4.000000000000004441, 103.8776713793258608 ) ) ;
#85419=PRESENTATION_STYLE_ASSIGNMENT (( #77855 ) ) ;
#85431=ADVANCED_FACE ( 'NONE', ( #36369 ), #34781, .F. ) ;
#85444=VERTEX_POINT ( 'NONE', #71860 ) ;
#85450=ORIENTED_EDGE ( 'NONE', *, *, #33854, .T. ) ;
#85452=MECHANICAL_DESIGN_GEOMETRIC_PRESENTATION_REPRESENTATION('',(#42389),#44098);
#85454=CARTESIAN_POINT ( 'NONE',  ( 6.354875581175684296, -49.58570828476184289, 39.47587273802374597 ) ) ;
#85466=STYLED_ITEM ( 'NONE', ( #85298 ), #89040 ) ;
#85479=( NAMED_UNIT ( * ) PLANE_ANGLE_UNIT ( ) SI_UNIT ( $, .RADIAN. ) );
#85512=( LENGTH_UNIT ( ) NAMED_UNIT ( * ) SI_UNIT ( .MILLI., .METRE. ) );
#85540=CARTESIAN_POINT ( 'NONE',  ( -4.551587301587304957, -1.200583151104947843, 104.4018401814738155 ) ) ;
#85561=CARTESIAN_POINT ( 'NONE',  ( 11.96163940603816123, -2.124851113821345727, 20.65895591259675612 ) ) ;
#85605=( NAMED_UNIT ( * ) PLANE_ANGLE_UNIT ( ) SI_UNIT ( $, .RADIAN. ) );
#85614=CARTESIAN_POINT ( 'NONE',  ( 13.38905016575103168, -53.47246454263770943, 31.09099597011418226 ) ) ;
#85636=TOROIDAL_SURFACE ( 'NONE', #54560, 12.00000000000000000, 2.000000000000000000 ) ;
#85645=ADVANCED_FACE ( 'NONE', ( #589 ), #42295, .T. ) ;
#85713=STYLED_ITEM ( 'NONE', ( #47573 ), #38054 ) ;
#85714=CARTESIAN_POINT ( 'NONE',  ( 4.524610880511400701, -11.34578236400706430, -9.835134842095726526 ) ) ;
#85751=CARTESIAN_POINT ( 'NONE',  ( 2.705399370281793114, -0.5466957599951438596, 103.4497616813456204 ) ) ;
#85764=CARTESIAN_POINT ( 'NONE',  ( -13.08498522490498495, 1.516837759881986880, 14.92390867749982064 ) ) ;
#85770=ORIENTED_EDGE ( 'NONE', *, *, #45394, .T. ) ;
#85771=CARTESIAN_POINT ( 'NONE',  ( 3.857142857142850101, -48.79941684889506348, 103.1763305333244176 ) ) ;
#85782=( LENGTH_UNIT ( ) NAMED_UNIT ( * ) SI_UNIT ( .MILLI., .METRE. ) );
#85795=ORIENTED_EDGE ( 'NONE', *, *, #5591, .F. ) ;
#85797=FACE_OUTER_BOUND ( 'NONE', #8981, .T. ) ;
#85805=CARTESIAN_POINT ( 'NONE',  ( -13.80753398876933247, -50.82042416759918524, 24.67600335260435074 ) ) ;
#85824=FILL_AREA_STYLE_COLOUR ( '', #100185 ) ;
#85829=UNCERTAINTY_MEASURE_WITH_UNIT (LENGTH_MEASURE( 1.000000000000000082E-05 ), #18046, 'distance_accuracy_value', 'NONE');
#85859=DIRECTION ( 'NONE',  ( 1.224646799147353454E-16, 0.000000000000000000, -1.000000000000000000 ) ) ;
#85872=CARTESIAN_POINT ( 'NONE',  ( 5.385673916453011856, 0.000000000000000000, 18.57417562100670949 ) ) ;
#85874=ORIENTED_EDGE ( 'NONE', *, *, #13852, .F. ) ;
#85883=( GEOMETRIC_REPRESENTATION_CONTEXT ( 3 ) GLOBAL_UNCERTAINTY_ASSIGNED_CONTEXT ( ( #24712 ) ) GLOBAL_UNIT_ASSIGNED_CONTEXT ( ( #85782, #2701, #18387 ) ) REPRESENTATION_CONTEXT ( 'NONE', 'WORKASPACE' ) );
#85921=EDGE_CURVE ( 'NONE', #3119, #18508, #19496, .T. ) ;
#85922=CARTESIAN_POINT ( 'NONE',  ( 3.349796915312611478, -1.132149698119323311, 104.5044954676210125 ) ) ;
#85959=SURFACE_STYLE_USAGE ( .BOTH. , #28809 ) ;
#85973=SURFACE_STYLE_FILL_AREA ( #42825 ) ;
#85975=PRESENTATION_STYLE_ASSIGNMENT (( #10974 ) ) ;
#85988=CARTESIAN_POINT ( 'NONE',  ( -9.378256585906134646, -55.78346096903717211, 23.52725134406122720 ) ) ;
#86007=CARTESIAN_POINT ( 'NONE',  ( 2.629190634011728367, -49.75653670290434150, 40.87823124498205374 ) ) ;
#86020=VECTOR ( 'NONE', #34776, 1000.000000000000000 ) ;
#86027=CARTESIAN_POINT ( 'NONE',  ( -3.711585775949200805, -49.05321961974463818, 40.67751789774135318 ) ) ;
#86051=EDGE_CURVE ( 'NONE', #57919, #88345, #29673, .T. ) ;
#86073=AXIS2_PLACEMENT_3D ( 'NONE', #101805, #100738, #2570 ) ;
#86098=CARTESIAN_POINT ( 'NONE',  ( -13.53382989543471560, -56.00915974862302704, 30.58576288564093915 ) ) ;
#86160=CARTESIAN_POINT ( 'NONE',  ( 13.38090213880806978, -53.73807135754422859, 31.11721482942555639 ) ) ;
#86161=CARTESIAN_POINT ( 'NONE',  ( 5.000000000000000000, -15.25461064142281487, 12.58690022914873374 ) ) ;
#86174=VERTEX_POINT ( 'NONE', #80872 ) ;
#86225=FACE_OUTER_BOUND ( 'NONE', #3133, .T. ) ;
#86229=CARTESIAN_POINT ( 'NONE',  ( 3.883877898720186739, -48.93467900693710959, 104.5781496044256471 ) ) ;
#86234=ORIENTED_EDGE ( 'NONE', *, *, #76359, .F. ) ;
#86285=CARTESIAN_POINT ( 'NONE',  ( 1.468822083365074915, -0.02842019993896785848, 101.6459669435634936 ) ) ;
#86299=CARTESIAN_POINT ( 'NONE',  ( -10.64183635766278435, -0.9494289261200415941, 20.26979409943867694 ) ) ;
#86306=MECHANICAL_DESIGN_GEOMETRIC_PRESENTATION_REPRESENTATION('',(#44961),#77665);
#86356=CARTESIAN_POINT ( 'NONE',  ( -1.788439362206281746, -69.58817794431396919, 12.85214533551791938 ) ) ;
#86403=ADVANCED_FACE ( 'NONE', ( #12301 ), #1637, .F. ) ;
#86409=EDGE_CURVE ( 'NONE', #87879, #214, #15493, .T. ) ;
#86421=DIRECTION ( 'NONE',  ( 0.000000000000000000, 0.000000000000000000, -1.000000000000000000 ) ) ;
#86425=CARTESIAN_POINT ( 'NONE',  ( 1.469576158976823947E-15, -78.00000000000000000, 15.00000000000000000 ) ) ;
#86439=ORIENTED_EDGE ( 'NONE', *, *, #88929, .F. ) ;
#86443=CARTESIAN_POINT ( 'NONE',  ( -3.215218824033863498, -1.016378598479024120, 104.3206516315225798 ) ) ;
#86462=CARTESIAN_POINT ( 'NONE',  ( 30.00000000000000000, 0.000000000000000000, -13.00000000000000000 ) ) ;
#86484=ORIENTED_EDGE ( 'NONE', *, *, #81486, .F. ) ;
#86485=DIRECTION ( 'NONE',  ( -2.742080092235280244E-17, -0.000000000000000000, 1.000000000000000000 ) ) ;
#86487=CARTESIAN_POINT ( 'NONE',  ( 9.171168021175072127, -55.04774845291035490, 30.98659277684255997 ) ) ;
#86493=CARTESIAN_POINT ( 'NONE',  ( 3.857142857142850545, -1.200583151104938517, 103.1763305333244318 ) ) ;
#86496=ORIENTED_EDGE ( 'NONE', *, *, #10979, .T. ) ;
#86498=CARTESIAN_POINT ( 'NONE',  ( 4.586789253316277737, -2.224716758486257717, 102.5764008378948091 ) ) ;
#86499=CARTESIAN_POINT ( 'NONE',  ( -3.534854068998068310, -48.92952247113088049, 104.4405781011824530 ) ) ;
#86527=TOROIDAL_SURFACE ( 'NONE', #39983, 5.999999999999996447, 4.000000000000000000 ) ;
#86534=ORIENTED_EDGE ( 'NONE', *, *, #78693, .T. ) ;
#86535=FILL_AREA_STYLE ('',( #61727 ) ) ;
#86540=CARTESIAN_POINT ( 'NONE',  ( 3.355259093261282022, -49.33750271349889971, 40.75586556368205748 ) ) ;
#86555=CARTESIAN_POINT ( 'NONE',  ( -1.000000000000000000, -69.59657292933731298, 12.76848391598547394 ) ) ;
#86561=( NAMED_UNIT ( * ) SI_UNIT ( $, .STERADIAN. ) SOLID_ANGLE_UNIT ( ) );
#86572=DIRECTION ( 'NONE',  ( 0.000000000000000000, 0.000000000000000000, 1.000000000000000000 ) ) ;
#86575=CYLINDRICAL_SURFACE ( 'NONE', #62427, 14.00000000000000178 ) ;
#86632=CARTESIAN_POINT ( 'NONE',  ( -13.95408269174820148, -57.87006985093267986, 28.16184020435892421 ) ) ;
#86651=CARTESIAN_POINT ( 'NONE',  ( -1.759014387761618226, -70.05783877895481737, 13.10925274558140252 ) ) ;
#86672=CARTESIAN_POINT ( 'NONE',  ( -4.175533140205453186, -1.555218955346044929, 102.9090322054120747 ) ) ;
#86684=SURFACE_SIDE_STYLE ('',( #53757 ) ) ;
#86685=CARTESIAN_POINT ( 'NONE',  ( 5.000000000000000000, -13.90268927582264347, 9.980021952846888311 ) ) ;
#86751=CARTESIAN_POINT ( 'NONE',  ( -12.30664161282574831, -4.730394409147478996, 20.32424246445631510 ) ) ;
#86754=CARTESIAN_POINT ( 'NONE',  ( 4.003587701500182838, -48.94962346669694142, 104.5574048719321780 ) ) ;
#86771=ORIENTED_EDGE ( 'NONE', *, *, #16509, .T. ) ;
#86788=EDGE_LOOP ( 'NONE', ( #81805, #13919 ) ) ;
#86801=( GEOMETRIC_REPRESENTATION_CONTEXT ( 3 ) GLOBAL_UNCERTAINTY_ASSIGNED_CONTEXT ( ( #2340 ) ) GLOBAL_UNIT_ASSIGNED_CONTEXT ( ( #36595, #60322, #76464 ) ) REPRESENTATION_CONTEXT ( 'NONE', 'WORKASPACE' ) );
#86803=SURFACE_STYLE_USAGE ( .BOTH. , #93286 ) ;
#86823=CARTESIAN_POINT ( 'NONE',  ( -14.83485053268217158, 0.1083361287566932396, 15.00090388149735254 ) ) ;
#86841=CARTESIAN_POINT ( 'NONE',  ( -3.454253436624922458, -49.15858197120396511, 103.7259032015043090 ) ) ;
#86849=CARTESIAN_POINT ( 'NONE',  ( -6.611670918688361098, -11.93296314122861190, 9.735702799542698571 ) ) ;
#86850=FILL_AREA_STYLE_COLOUR ( '', #38111 ) ;
#86858=CARTESIAN_POINT ( 'NONE',  ( -13.69909788704105935, -51.35317944603409046, 24.10694589033532154 ) ) ;
#86876=CARTESIAN_POINT ( 'NONE',  ( -4.220606381948455166, -66.96246410476639710, 13.14687599345784896 ) ) ;
#86907=CARTESIAN_POINT ( 'NONE',  ( 3.677391134430175512, -48.98477995422159381, 104.0097548473154916 ) ) ;
#86933=B_SPLINE_SURFACE_WITH_KNOTS ( 'NONE', 3, 1, ( 
 ( #92226, #10772 ),
 ( #68515, #76050 ),
 ( #100860, #36713 ),
 ( #69578, #101924 ) ),
 .UNSPECIFIED., .F., .F., .F.,
 ( 4, 4 ),
 ( 2, 2 ),
 ( 0.000000000000000000, 0.9982556956955090932 ),
 ( 0.000000000000000000, 1.000000000000000000 ),
 .UNSPECIFIED. ) ;
#86962=EDGE_CURVE ( 'NONE', #27782, #63587, #97379, .T. ) ;
#86964=CARTESIAN_POINT ( 'NONE',  ( -3.499286860947127931, -0.8580408876376250937, 104.2445795335848544 ) ) ;
#87007=CARTESIAN_POINT ( 'NONE',  ( 5.000000000000000888, -48.52751354257630823, 2.643394033337469473 ) ) ;
#87027=SURFACE_SIDE_STYLE ('',( #85973 ) ) ;
#87041=B_SPLINE_CURVE_WITH_KNOTS ( 'NONE', 3,
 ( #22118, #103546, #38822, #54430, #104595, #78205, #37255, #78719, #46889, #87376, #12925, #46375, #70118, #103025, #30749, #4321, #77687, #79264, #29693, #21599, #52867, #94946 ),
 .UNSPECIFIED., .F., .F.,
 ( 4, 2, 2, 2, 2, 2, 2, 2, 2, 2, 4 ),
 ( 0.000000000000000000, 0.001580156024417029908, 0.003160312048834081067, 0.004740468073251132008, 0.006320624097668182950, 0.007900780122085233892, 0.009480936146502284834, 0.01027101415871079643, 0.01106109217091930629, 0.01185117018312781788, 0.01264124819533632947 ),
 .UNSPECIFIED. ) ;
#87059=AXIS2_PLACEMENT_3D ( 'NONE', #13014, #69688, #22219 ) ;
#87070=CARTESIAN_POINT ( 'NONE',  ( -1.000000000000000000, -63.14890303517896086, 9.346194641685219295 ) ) ;
#87077=CARTESIAN_POINT ( 'NONE',  ( -3.338674867580755379, -49.24767650228190519, 44.08270169569225061 ) ) ;
#87109=DIRECTION ( 'NONE',  ( -0.7142857142857134134, 0.6998542122237662033, 0.000000000000000000 ) ) ;
#87112=ADVANCED_FACE ( 'NONE', ( #46698 ), #94171, .F. ) ;
#87124=VERTEX_POINT ( 'NONE', #41788 ) ;
#87147=CARTESIAN_POINT ( 'NONE',  ( -5.802268690544502228, -46.54360925828362383, 103.8899761878886636 ) ) ;
#87159=ORIENTED_EDGE ( 'NONE', *, *, #76070, .T. ) ;
#87198=ADVANCED_FACE ( 'NONE', ( #1300 ), #15922, .T. ) ;
#87214=CARTESIAN_POINT ( 'NONE',  ( 3.505862197715610140, -0.8815186120392470848, 103.6125913840232329 ) ) ;
#87271=CARTESIAN_POINT ( 'NONE',  ( -11.87389578517861288, -10.58298652339508372, 10.63284064146614405 ) ) ;
#87306=CARTESIAN_POINT ( 'NONE',  ( -6.891666673413887896E-15, -70.53271932724189242, 13.00000000000000000 ) ) ;
#87314=( GEOMETRIC_REPRESENTATION_CONTEXT ( 3 ) GLOBAL_UNCERTAINTY_ASSIGNED_CONTEXT ( ( #51563 ) ) GLOBAL_UNIT_ASSIGNED_CONTEXT ( ( #92316, #42715, #100416 ) ) REPRESENTATION_CONTEXT ( 'NONE', 'WORKASPACE' ) );
#87315=COLOUR_RGB ( '', 0.09019608, 0.27058824, 0.51372549) ;
#87334=CARTESIAN_POINT ( 'NONE',  ( 2.122576366386045521, -0.2161414388924163821, 102.5552564100479032 ) ) ;
#87348=CARTESIAN_POINT ( 'NONE',  ( -9.275681565049682220, -2.829365477041055676, 14.74133895328401245 ) ) ;
#87376=CARTESIAN_POINT ( 'NONE',  ( -5.139041025450133304, -67.43305464250801151, 13.97603388998033580 ) ) ;
#87377=CARTESIAN_POINT ( 'NONE',  ( 0.000000000000000000, -78.00000000000000000, 27.00000000000000000 ) ) ;
#87404=CARTESIAN_POINT ( 'NONE',  ( -4.667584529657848869, -65.20519645549873644, 13.09134375087143809 ) ) ;
#87431=STYLED_ITEM ( 'NONE', ( #58321 ), #29400 ) ;
#87465=CARTESIAN_POINT ( 'NONE',  ( -5.000000000000000000, -3.274064727865673152, -10.50970520401928177 ) ) ;
#87498=SURFACE_SIDE_STYLE ('',( #47012 ) ) ;
#87516=CARTESIAN_POINT ( 'NONE',  ( 13.44292909870241459, -55.29335566891484888, 30.91132584605806244 ) ) ;
#87528=( NAMED_UNIT ( * ) PLANE_ANGLE_UNIT ( ) SI_UNIT ( $, .RADIAN. ) );
#87552=CARTESIAN_POINT ( 'NONE',  ( -2.345389088905535324, -49.77582587123195879, 44.62432230782176390 ) ) ;
#87560=COLOUR_RGB ( '', 0.09019608, 0.27058824, 0.51372549) ;
#87604=CARTESIAN_POINT ( 'NONE',  ( -2.802997532626366972, -53.56901273344412573, 40.71799139369159803 ) ) ;
#87621=SURFACE_STYLE_FILL_AREA ( #103265 ) ;
#87654=SURFACE_SIDE_STYLE ('',( #63390 ) ) ;
#87703=DIRECTION ( 'NONE',  ( -0.000000000000000000, -1.000000000000000000, -0.000000000000000000 ) ) ;
#87734=CARTESIAN_POINT ( 'NONE',  ( 13.97203307284001994, -50.12825479938464923, 26.07838388608699631 ) ) ;
#87747=( NAMED_UNIT ( * ) PLANE_ANGLE_UNIT ( ) SI_UNIT ( $, .RADIAN. ) );
#87752=ORIENTED_EDGE ( 'NONE', *, *, #15917, .F. ) ;
#87757=FILL_AREA_STYLE ('',( #31135 ) ) ;
#87772=CARTESIAN_POINT ( 'NONE',  ( -4.750186375023972118, -1.378107633083692329, 104.3180500829675026 ) ) ;
#87801=CARTESIAN_POINT ( 'NONE',  ( -12.00539508356256491, -6.854840103463671674, 19.79463260135151614 ) ) ;
#87827=CARTESIAN_POINT ( 'NONE',  ( -1.112596765064915338, -50.00000000000000711, 101.1535177161686647 ) ) ;
#87840=DIRECTION ( 'NONE',  ( 1.000000000000000000, 0.000000000000000000, 0.000000000000000000 ) ) ;
#87850=CARTESIAN_POINT ( 'NONE',  ( 3.454253436624936668, -0.8414180287960456583, 103.7259032015043232 ) ) ;
#87862=DIRECTION ( 'NONE',  ( 1.000000000000000000, -0.000000000000000000, -0.000000000000000000 ) ) ;
#87872=CARTESIAN_POINT ( 'NONE',  ( -8.503038991956803017, 2.981673336380457950, 14.70105501402611381 ) ) ;
#87875=CIRCLE ( 'NONE', #58630, 1.999999999999998890 ) ;
#87879=VERTEX_POINT ( 'NONE', #5380 ) ;
#87895=ORIENTED_EDGE ( 'NONE', *, *, #64455, .T. ) ;
#87901=SURFACE_STYLE_FILL_AREA ( #71170 ) ;
#87932=DIRECTION ( 'NONE',  ( 0.000000000000000000, 0.000000000000000000, 1.000000000000000000 ) ) ;
#87955=EDGE_CURVE ( 'NONE', #8366, #76134, #52570, .T. ) ;
#87967=CARTESIAN_POINT ( 'NONE',  ( -9.423772032809306864, -51.98692372519796834, 23.65101655106710510 ) ) ;
#87991=CARTESIAN_POINT ( 'NONE',  ( -1.000000000000000000, -15.67301612170368053, -10.31008658363377251 ) ) ;
#88007=STYLED_ITEM ( 'NONE', ( #75721 ), #12305 ) ;
#88009=VERTEX_POINT ( 'NONE', #79782 ) ;
#88012=CARTESIAN_POINT ( 'NONE',  ( -1.257803174883066255, -3.680419541196005571E-09, 101.3280723980861495 ) ) ;
#88050=ORIENTED_EDGE ( 'NONE', *, *, #44309, .F. ) ;
#88058=CARTESIAN_POINT ( 'NONE',  ( 5.000000000000000888, -67.35888985736187351, 11.51944599242068890 ) ) ;
#88102=ORIENTED_EDGE ( 'NONE', *, *, #13287, .T. ) ;
#88132=CARTESIAN_POINT ( 'NONE',  ( -4.861345245134582882, -47.05236803399135681, 42.74555668121053742 ) ) ;
#88179=PRESENTATION_STYLE_ASSIGNMENT (( #6173 ) ) ;
#88258=ORIENTED_EDGE ( 'NONE', *, *, #5467, .T. ) ;
#88259=DIRECTION ( 'NONE',  ( 0.000000000000000000, 1.000000000000000000, 0.000000000000000000 ) ) ;
#88273=DIRECTION ( 'NONE',  ( 1.000000000000000000, 0.000000000000000000, 0.000000000000000000 ) ) ;
#88281=MECHANICAL_DESIGN_GEOMETRIC_PRESENTATION_REPRESENTATION('',(#31492),#52160);
#88302=CARTESIAN_POINT ( 'NONE',  ( -5.238409285680481808, -1.996984918271471621, 104.1169421774614108 ) ) ;
#88303=ORIENTED_EDGE ( 'NONE', *, *, #10656, .F. ) ;
#88312=( LENGTH_UNIT ( ) NAMED_UNIT ( * ) SI_UNIT ( .MILLI., .METRE. ) );
#88317=SURFACE_STYLE_FILL_AREA ( #55387 ) ;
#88326=EDGE_LOOP ( 'NONE', ( #18797, #59903, #97945, #30538 ) ) ;
#88333=CARTESIAN_POINT ( 'NONE',  ( -10.09376787920347418, -12.27809184049766600, 17.28929750330553716 ) ) ;
#88339=EDGE_CURVE ( 'NONE', #85095, #11338, #103919, .T. ) ;
#88345=VERTEX_POINT ( 'NONE', #14279 ) ;
#88353=VERTEX_POINT ( 'NONE', #38590 ) ;
#88384=SURFACE_STYLE_FILL_AREA ( #13931 ) ;
#88405=FILL_AREA_STYLE ('',( #63610 ) ) ;
#88423=CARTESIAN_POINT ( 'NONE',  ( 5.833333333333329485, -4.000000000000003553, 103.8776713793258608 ) ) ;
#88431=CARTESIAN_POINT ( 'NONE',  ( -5.000000000000000000, -13.82147230827991713, 10.98112731479256254 ) ) ;
#88446=ADVANCED_FACE ( 'NONE', ( #18023 ), #5333, .F. ) ;
#88540=SURFACE_STYLE_FILL_AREA ( #55602 ) ;
#88543=DIRECTION ( 'NONE',  ( 0.000000000000000000, 0.000000000000000000, 1.000000000000000000 ) ) ;
#88545=( NAMED_UNIT ( * ) SI_UNIT ( $, .STERADIAN. ) SOLID_ANGLE_UNIT ( ) );
#88552=( LENGTH_UNIT ( ) NAMED_UNIT ( * ) SI_UNIT ( .MILLI., .METRE. ) );
#88553=CARTESIAN_POINT ( 'NONE',  ( 1.000000000000000000, -59.21823443913439178, 7.425173686811099572 ) ) ;
#88612=ORIENTED_EDGE ( 'NONE', *, *, #48050, .F. ) ;
#88643=DIRECTION ( 'NONE',  ( 0.000000000000000000, 1.000000000000000000, 0.000000000000000000 ) ) ;
#88645=CARTESIAN_POINT ( 'NONE',  ( -1.000000000000000000, -48.56827653474476136, 2.661071982226036692 ) ) ;
#88719=CARTESIAN_POINT ( 'NONE',  ( -0.8750000000009734435, -70.58759490697451611, 13.02737050516266315 ) ) ;
#88729=FACE_OUTER_BOUND ( 'NONE', #12499, .T. ) ;
#88730=SURFACE_STYLE_FILL_AREA ( #56331 ) ;
#88746=CARTESIAN_POINT ( 'NONE',  ( -6.125000000795022714, -61.26994199106662364, 14.41094225169091558 ) ) ;
#88767=FILL_AREA_STYLE ('',( #48285 ) ) ;
#88818=CARTESIAN_POINT ( 'NONE',  ( 5.596957125887390028, -2.684245481662592692, 103.9718581041641698 ) ) ;
#88819=CARTESIAN_POINT ( 'NONE',  ( 3.510275272315894757, -1.149081201640936190, 104.5952116206559737 ) ) ;
#88820=CARTESIAN_POINT ( 'NONE',  ( -4.792515968931456705, -2.702239074782535777, 102.4138677444059766 ) ) ;
#88857=SURFACE_SIDE_STYLE ('',( #71071 ) ) ;
#88866=VERTEX_POINT ( 'NONE', #20359 ) ;
#88902=SURFACE_STYLE_USAGE ( .BOTH. , #12873 ) ;
#88923=CARTESIAN_POINT ( 'NONE',  ( -6.125000000000000888, -80.00000000000000000, 14.41094225130411033 ) ) ;
#88929=EDGE_CURVE ( 'NONE', #56114, #46770, #71488, .T. ) ;
#88937=ORIENTED_EDGE ( 'NONE', *, *, #36312, .T. ) ;
#88954=CARTESIAN_POINT ( 'NONE',  ( -5.963307081834163803, -13.30359940716284761, 13.46515011340851409 ) ) ;
#89021=CARTESIAN_POINT ( 'NONE',  ( -9.995943316031024040, -50.00048584071330282, 27.38809334239569182 ) ) ;
#89030=CARTESIAN_POINT ( 'NONE',  ( 4.919733272805030921, -48.43781863848562352, 104.2477112191711086 ) ) ;
#89037=MECHANICAL_DESIGN_GEOMETRIC_PRESENTATION_REPRESENTATION('',(#28800),#56275);
#89040=ADVANCED_FACE ( 'NONE', ( #33187 ), #96991, .T. ) ;
#89042=CARTESIAN_POINT ( 'NONE',  ( -0.7777777777777781232, -54.00000000000000711, 40.97837836547555668 ) ) ;
#89061=ORIENTED_EDGE ( 'NONE', *, *, #48050, .T. ) ;
#89069=UNCERTAINTY_MEASURE_WITH_UNIT (LENGTH_MEASURE( 1.000000000000000082E-05 ), #17184, 'distance_accuracy_value', 'NONE');
#89110=CARTESIAN_POINT ( 'NONE',  ( -3.384215095276410512, -0.8669809812618441969, 104.0501775326196707 ) ) ;
#89115=CARTESIAN_POINT ( 'NONE',  ( 4.999999999994901856, -10.14931581695978657, -12.32157755740035121 ) ) ;
#89116=CARTESIAN_POINT ( 'NONE',  ( 8.642845603823378298, -4.454434588728953592, 14.41908465074281231 ) ) ;
#89136=CARTESIAN_POINT ( 'NONE',  ( -2.087655452114465682, -49.85878286479394461, 44.72580038709070749 ) ) ;
#89141=CARTESIAN_POINT ( 'NONE',  ( -3.454253436624930451, -0.8414180287960395521, 103.7259032015043232 ) ) ;
#89188=CARTESIAN_POINT ( 'NONE',  ( -6.958956728584277940, -47.06078234015144091, 39.14832407461615560 ) ) ;
#89219=COLOUR_RGB ( '', 0.09019608, 0.27058824, 0.51372549) ;
#89222=AXIS2_PLACEMENT_3D ( 'NONE', #27560, #78184, #20551 ) ;
#89266=EDGE_CURVE ( 'NONE', #103837, #86174, #49644, .T. ) ;
#89284=CARTESIAN_POINT ( 'NONE',  ( -4.810465484628549504, -64.26601022681093411, 13.02425015433478706 ) ) ;
#89303=ORIENTED_EDGE ( 'NONE', *, *, #33808, .T. ) ;
#89348=COLOUR_RGB ( '', 0.08235294, 0.09019608, 0.10196078) ;
#89363=CARTESIAN_POINT ( 'NONE',  ( -4.928386788250540995, -1.571875576847017397, 104.2441249819467686 ) ) ;
#89392=DIRECTION ( 'NONE',  ( 0.000000000000000000, 0.000000000000000000, -1.000000000000000000 ) ) ;
#89396=CARTESIAN_POINT ( 'NONE',  ( 4.399054598113104397, -48.11244280224734382, 102.7269706464928021 ) ) ;
#89409=AXIS2_PLACEMENT_3D ( 'NONE', #26354, #67306, #75373 ) ;
#89410=CARTESIAN_POINT ( 'NONE',  ( -1.000000000000000222, -5.000000000000000000, -14.14213562373095101 ) ) ;
#89426=CARTESIAN_POINT ( 'NONE',  ( -5.833333333333327708, -46.00000000000000000, 103.8776713793258608 ) ) ;
#89432=LINE ( 'NONE', #6355, #3726 ) ;
#89455=ORIENTED_EDGE ( 'NONE', *, *, #37286, .F. ) ;
#89465=CARTESIAN_POINT ( 'NONE',  ( -5.385673916453012744, -4.336808689942017736E-16, 15.34388420865771785 ) ) ;
#89476=FACE_OUTER_BOUND ( 'NONE', #13242, .T. ) ;
#89490=CARTESIAN_POINT ( 'NONE',  ( -6.031968554556153883, -14.91855978929569559, 14.31416968664639988 ) ) ;
#89517=UNCERTAINTY_MEASURE_WITH_UNIT (LENGTH_MEASURE( 1.000000000000000082E-05 ), #714, 'distance_accuracy_value', 'NONE');
#89546=SURFACE_STYLE_FILL_AREA ( #17791 ) ;
#89547=CARTESIAN_POINT ( 'NONE',  ( 9.301012663197237629, -52.69978924280226096, 23.32537848786287782 ) ) ;
#89553=CARTESIAN_POINT ( 'NONE',  ( 0.000000000000000000, -46.00000000000000000, 112.0000000000000000 ) ) ;
#89571=CIRCLE ( 'NONE', #63719, 2.000000000000000000 ) ;
#89596=ORIENTED_EDGE ( 'NONE', *, *, #5015, .F. ) ;
#89606=CARTESIAN_POINT ( 'NONE',  ( -14.91858118607497019, 1.255821567010171884E-17, 15.00000000000000000 ) ) ;
#89611=VERTEX_POINT ( 'NONE', #40857 ) ;
#89632=DIRECTION ( 'NONE',  ( 0.000000000000000000, 0.000000000000000000, 1.000000000000000000 ) ) ;
#89639=SURFACE_STYLE_FILL_AREA ( #24406 ) ;
#89652=CARTESIAN_POINT ( 'NONE',  ( -1.238932115526321320, -50.00000000000000000, 101.3452916561192296 ) ) ;
#89673=CARTESIAN_POINT ( 'NONE',  ( -4.874120320015572716, -52.04554131839427811, 40.12882148314245256 ) ) ;
#89679=ORIENTED_EDGE ( 'NONE', *, *, #99818, .T. ) ;
#89711=EDGE_LOOP ( 'NONE', ( #44000, #71671, #68335, #37976 ) ) ;
#89722=AXIS2_PLACEMENT_3D ( 'NONE', #89553, #31863, #15649 ) ;
#89796=MECHANICAL_DESIGN_GEOMETRIC_PRESENTATION_REPRESENTATION('',(#15707),#103567);
#89798=CARTESIAN_POINT ( 'NONE',  ( -15.54886886242640998, -0.9489809227296597260, 14.97197842136719181 ) ) ;
#89812=CARTESIAN_POINT ( 'NONE',  ( -2.361588828579537225, -69.88257940272585245, 13.19812034727280370 ) ) ;
#89824=CARTESIAN_POINT ( 'NONE',  ( 4.999999998541157176, -46.36031008665895570, 40.27905619190705977 ) ) ;
#89861=CARTESIAN_POINT ( 'NONE',  ( 10.25662953440644110, -12.00964996486999325, 17.46101989419365452 ) ) ;
#89867=CARTESIAN_POINT ( 'NONE',  ( 1.737810032903332802, -69.62561923041629086, 12.84439221602053571 ) ) ;
#89873=CARTESIAN_POINT ( 'NONE',  ( 4.571008445750557314, -47.80671748343183936, 102.5889671997070849 ) ) ;
#89892=CARTESIAN_POINT ( 'NONE',  ( 5.000000000000000000, -14.03284112244661941, 9.638321536847527682 ) ) ;
#89903=VECTOR ( 'NONE', #45047, 1000.000000000000000 ) ;
#89913=CARTESIAN_POINT ( 'NONE',  ( 5.238409285680604377, -48.00301508172830722, 104.1169421774613539 ) ) ;
#89921=EDGE_CURVE ( 'NONE', #34686, #30914, #11825, .T. ) ;
#89943=CARTESIAN_POINT ( 'NONE',  ( -4.188755055078890344, -48.42812442300444076, 102.8981131900555113 ) ) ;
#89947=CARTESIAN_POINT ( 'NONE',  ( 1.898667928446299280, -49.86745472351331188, 102.2341000961458803 ) ) ;
#89992=VERTEX_POINT ( 'NONE', #10089 ) ;
#90011=CARTESIAN_POINT ( 'NONE',  ( -4.999999999999440448, -15.32190040641671303, 13.82401333429963231 ) ) ;
#90062=CARTESIAN_POINT ( 'NONE',  ( 1.227477900293065805, -69.63323560895928210, 12.78939886615606447 ) ) ;
#90068=FACE_OUTER_BOUND ( 'NONE', #88326, .T. ) ;
#90073=CARTESIAN_POINT ( 'NONE',  ( -9.981808881366681874, -50.02775323464795321, 27.65604031336897251 ) ) ;
#90085=CARTESIAN_POINT ( 'NONE',  ( 5.000000000000000888, -15.60834519661176856, -6.449721054204996307 ) ) ;
#90150=VERTEX_POINT ( 'NONE', #61323 ) ;
#90154=CARTESIAN_POINT ( 'NONE',  ( 13.66213079746738934, -56.44306380163116188, 23.93919572553859609 ) ) ;
#90164=CARTESIAN_POINT ( 'NONE',  ( 9.821751540093583088, -57.46817456407566027, 25.10730599066359758 ) ) ;
#90172=CARTESIAN_POINT ( 'NONE',  ( 9.147394621530509085, -3.304799994669868735, 14.67325677361586322 ) ) ;
#90185=ORIENTED_EDGE ( 'NONE', *, *, #40161, .F. ) ;
#90197=( BOUNDED_SURFACE ( )  B_SPLINE_SURFACE ( 3, 2, ( 
 ( #97952, #24101, #14358 ),
 ( #56943, #13308, #9457 ),
 ( #57474, #59105, #49926 ),
 ( #99535, #66653, #41309 ),
 ( #17048, #91985, #83892 ),
 ( #75257, #25712, #8934 ),
 ( #18123, #98995, #50978 ),
 ( #1359, #91472, #100607 ),
 ( #34321, #58012, #75803 ),
 ( #809, #42912, #67197 ),
 ( #33242, #8405, #41838 ),
 ( #90400, #66115, #58574 ),
 ( #17588, #10005, #49386 ),
 ( #40773, #74724, #33777 ),
 ( #82834, #26767, #74194 ),
 ( #32718, #26242, #1898 ),
 ( #50448, #274, #81744 ),
 ( #34853, #16502, #83359 ),
 ( #42371, #100074, #67721 ),
 ( #89867, #65587, #98474 ),
 ( #25159, #15973, #82296 ),
 ( #90938, #48851, #7866 ) ),
 .UNSPECIFIED., .F., .F., .F. ) 
 B_SPLINE_SURFACE_WITH_KNOTS ( ( 4, 2, 2, 2, 2, 2, 2, 2, 2, 2, 4 ),
 ( 3, 3 ),
 ( 9.575673587391975161E-16, 0.003256072800435538209, 0.004884109200652828747, 0.005698127400761473366, 0.006512145600870118851, 0.007326163800978764337, 0.008140182001087408956, 0.009768218401304699927, 0.01058223660141334455, 0.01139625480152198916, 0.01302429120173928014 ),
 ( 0.000000000000000000, 1.000000000000000000 ),
 .UNSPECIFIED. ) 
 GEOMETRIC_REPRESENTATION_ITEM ( )  RATIONAL_B_SPLINE_SURFACE ( (
 ( 1.000000000000000000, 0.8477912478910073490, 1.000000000000000000),
 ( 1.000000000000000000, 0.8670434152227779467, 1.000000000000000000),
 ( 1.000000000000000000, 0.8843226860176298665, 1.000000000000000000),
 ( 1.000000000000000000, 0.9072812172742162895, 1.000000000000000000),
 ( 1.000000000000000000, 0.9144387507582195651, 1.000000000000000000),
 ( 1.000000000000000000, 0.9243937791762486533, 1.000000000000000000),
 ( 1.000000000000000000, 0.9275815810102141512, 1.000000000000000000),
 ( 1.000000000000000000, 0.9336849299333107588, 1.000000000000000000),
 ( 1.000000000000000000, 0.9366082457614915979, 1.000000000000000000),
 ( 1.000000000000000000, 0.9420647132138212365, 1.000000000000000000),
 ( 1.000000000000000000, 0.9446105283158728882, 1.000000000000000000),
 ( 1.000000000000000000, 0.9493321006897598169, 1.000000000000000000),
 ( 1.000000000000000000, 0.9515192386868923657, 1.000000000000000000),
 ( 1.000000000000000000, 0.9574223867891574757, 1.000000000000000000),
 ( 1.000000000000000000, 0.9604696041222584579, 1.000000000000000000),
 ( 1.000000000000000000, 0.9638146532777485120, 1.000000000000000000),
 ( 1.000000000000000000, 0.9646961637823425750, 1.000000000000000000),
 ( 1.000000000000000000, 0.9660383415586468736, 1.000000000000000000),
 ( 1.000000000000000000, 0.9665040966128550792, 1.000000000000000000),
 ( 1.000000000000000000, 0.9673053536378352080, 1.000000000000000000),
 ( 1.000000000000000000, 0.9670582897025716829, 1.000000000000000000),
 ( 1.000000000000000000, 0.9661530732048717596, 1.000000000000000000) ) ) 
 REPRESENTATION_ITEM ( '' )  SURFACE ( )  );
#90204=CARTESIAN_POINT ( 'NONE',  ( -9.113097280746998763, -54.26319141364687937, 31.11721482942555639 ) ) ;
#90228=B_SPLINE_CURVE_WITH_KNOTS ( 'NONE', 3,
 ( #91701, #66890, #42067, #99229, #67427, #25397, #26465, #8637, #50665, #1045, #9690, #17286, #50161, #41538, #74954, #42600, #74428, #58253, #504, #91181 ),
 .UNSPECIFIED., .F., .F.,
 ( 4, 2, 2, 2, 2, 2, 2, 2, 2, 4 ),
 ( 0.000000000000000000, 0.002366343802433873607, 0.003549515703650809543, 0.004732687604867745479, 0.005915859506084680981, 0.007099031407301617351, 0.007690617357910085536, 0.008282203308518552853, 0.008873789259127021906, 0.009465375209735490958 ),
 .UNSPECIFIED. ) ;
#90230=MANIFOLD_SOLID_BREP ( 'Cut-Extrude1', #20583 ) ;
#90273=DIRECTION ( 'NONE',  ( 2.742080092235280244E-17, 0.000000000000000000, -1.000000000000000000 ) ) ;
#90287=DIRECTION ( 'NONE',  ( 0.000000000000000000, 0.000000000000000000, 1.000000000000000000 ) ) ;
#90309=FILL_AREA_STYLE ('',( #57395 ) ) ;
#90333=CARTESIAN_POINT ( 'NONE',  ( -2.429940952537731125, -69.36428444796445092, 12.93557570994918571 ) ) ;
#90342=SURFACE_STYLE_USAGE ( .BOTH. , #65006 ) ;
#90375=CARTESIAN_POINT ( 'NONE',  ( 15.84496339826243272, -1.752972784076425317, 14.89969185729413859 ) ) ;
#90400=CARTESIAN_POINT ( 'NONE',  ( 4.004501244502223223, -67.47611191202615544, 13.13598341573225703 ) ) ;
#90406=CARTESIAN_POINT ( 'NONE',  ( 4.448407490268952991, -48.03096409756968654, 102.6871849564181218 ) ) ;
#90418=ORIENTED_EDGE ( 'NONE', *, *, #78918, .T. ) ;
#90423=CIRCLE ( 'NONE', #61186, 4.000000000000001776 ) ;
#90431=ORIENTED_EDGE ( 'NONE', *, *, #91599, .T. ) ;
#90435=ADVANCED_FACE ( 'NONE', ( #57568 ), #55971, .F. ) ;
#90446=B_SPLINE_CURVE_WITH_KNOTS ( 'NONE', 3,
 ( #10299, #76626, #58876, #100375, #43738, #52896, #92818, #101452, #91768, #3286, #17890, #28129 ),
 .UNSPECIFIED., .F., .F.,
 ( 4, 2, 2, 2, 2, 4 ),
 ( 0.0005290297149009433276, 0.001465496285715521931, 0.002401962856530100426, 0.003338429427344679137, 0.003806662712751983455, 0.004274895998159287773 ),
 .UNSPECIFIED. ) ;
#90457=ORIENTED_EDGE ( 'NONE', *, *, #66887, .F. ) ;
#90478=CARTESIAN_POINT ( 'NONE',  ( -4.680975426248548565, -47.58422982932144407, 103.4780497728483368 ) ) ;
#90484=CARTESIAN_POINT ( 'NONE',  ( 0.000000000000000000, -4.000000000000003553, 119.0000000000000142 ) ) ;
#90485=UNCERTAINTY_MEASURE_WITH_UNIT (LENGTH_MEASURE( 1.000000000000000082E-05 ), #54746, 'distance_accuracy_value', 'NONE');
#90493=FILL_AREA_STYLE_COLOUR ( '', #44655 ) ;
#90515=DIRECTION ( 'NONE',  ( 0.000000000000000000, 1.000000000000000000, 0.000000000000000000 ) ) ;
#90531=EDGE_LOOP ( 'NONE', ( #15217, #44226 ) ) ;
#90537=STYLED_ITEM ( 'NONE', ( #30877 ), #35733 ) ;
#90545=CARTESIAN_POINT ( 'NONE',  ( -5.000000000000000000, -13.83542193917759633, 11.07282995724388286 ) ) ;
#90547=ORIENTED_EDGE ( 'NONE', *, *, #82861, .F. ) ;
#90550=CARTESIAN_POINT ( 'NONE',  ( -30.00000000000000000, -54.00000000000000711, 27.11721482942554928 ) ) ;
#90564=CARTESIAN_POINT ( 'NONE',  ( 15.88393779855022281, -1.939575830182636684, 14.87604252415763106 ) ) ;
#90596=CARTESIAN_POINT ( 'NONE',  ( 1.797535115058627619, -69.58639455773389670, 12.85324246208445587 ) ) ;
#90605=CARTESIAN_POINT ( 'NONE',  ( 9.113097280746996987, -54.00000000000000711, 31.11721482942554928 ) ) ;
#90644=VECTOR ( 'NONE', #86485, 1000.000000000000000 ) ;
#90661=LINE ( 'NONE', #50195, #77901 ) ;
#90672=CYLINDRICAL_SURFACE ( 'NONE', #4389, 9.000000000000000000 ) ;
#90691=AXIS2_PLACEMENT_3D ( 'NONE', #4115, #94189, #13774 ) ;
#90704=( NAMED_UNIT ( * ) PLANE_ANGLE_UNIT ( ) SI_UNIT ( $, .RADIAN. ) );
#90708=( LENGTH_UNIT ( ) NAMED_UNIT ( * ) SI_UNIT ( .MILLI., .METRE. ) );
#90711=SURFACE_STYLE_FILL_AREA ( #23881 ) ;
#90716=CARTESIAN_POINT ( 'NONE',  ( -3.678498789084922116, -48.98362606748378312, 104.0112638849150812 ) ) ;
#90749=CARTESIAN_POINT ( 'NONE',  ( 3.857142857142850545, -1.200583151104938517, 103.1763305333244318 ) ) ;
#90830=MECHANICAL_DESIGN_GEOMETRIC_PRESENTATION_REPRESENTATION('',(#95986),#23706);
#90840=VECTOR ( 'NONE', #78189, 1000.000000000000000 ) ;
#90847=CIRCLE ( 'NONE', #59837, 11.00000000000001066 ) ;
#90875=CARTESIAN_POINT ( 'NONE',  ( -4.911511084989005127, -63.26970332188709989, 12.93090383856629444 ) ) ;
#90884=AXIS2_PLACEMENT_3D ( 'NONE', #69113, #68583, #28144 ) ;
#90913=CARTESIAN_POINT ( 'NONE',  ( -5.000000000000000888, -58.90829880881958047, 11.71896219753489810 ) ) ;
#90928=( GEOMETRIC_REPRESENTATION_CONTEXT ( 3 ) GLOBAL_UNCERTAINTY_ASSIGNED_CONTEXT ( ( #9549 ) ) GLOBAL_UNIT_ASSIGNED_CONTEXT ( ( #65546, #97902, #98948 ) ) REPRESENTATION_CONTEXT ( 'NONE', 'WORKASPACE' ) );
#90934=CARTESIAN_POINT ( 'NONE',  ( 11.96261933146057821, -7.078120104440478677, 19.72315005431197221 ) ) ;
#90938=CARTESIAN_POINT ( 'NONE',  ( 0.9999999999999993339, -69.59657292934915063, 12.76848391599223120 ) ) ;
#90969=CARTESIAN_POINT ( 'NONE',  ( 5.000000000000000000, -14.50704001784992059, 12.23934196172798394 ) ) ;
#90985=( NAMED_UNIT ( * ) PLANE_ANGLE_UNIT ( ) SI_UNIT ( $, .RADIAN. ) );
#90988=ORIENTED_EDGE ( 'NONE', *, *, #37286, .T. ) ;
#90989=CARTESIAN_POINT ( 'NONE',  ( 4.725902370230407712, -47.47364726308473593, 103.4500010546506417 ) ) ;
#91045=CARTESIAN_POINT ( 'NONE',  ( 27.99999999999999645, 0.000000000000000000, 0.000000000000000000 ) ) ;
#91077=FILL_AREA_STYLE_COLOUR ( '', #56491 ) ;
#91117=CARTESIAN_POINT ( 'NONE',  ( 13.08519678395057184, 1.516754868601839501, 14.92392294744104575 ) ) ;
#91148=SURFACE_SIDE_STYLE ('',( #58772 ) ) ;
#91157=CARTESIAN_POINT ( 'NONE',  ( 9.226722513859208163, -53.47035606567975918, 23.14374324513729064 ) ) ;
#91181=CARTESIAN_POINT ( 'NONE',  ( -12.37144696128342147, -4.000000000000003553, 20.44658103856077602 ) ) ;
#91182=MECHANICAL_DESIGN_GEOMETRIC_PRESENTATION_REPRESENTATION('',(#72218),#67000);
#91196=( NAMED_UNIT ( * ) SI_UNIT ( $, .STERADIAN. ) SOLID_ANGLE_UNIT ( ) );
#91202=MECHANICAL_DESIGN_GEOMETRIC_PRESENTATION_REPRESENTATION('',(#75706),#77407);
#91225=EDGE_CURVE ( 'NONE', #42316, #89611, #59920, .T. ) ;
#91257=CARTESIAN_POINT ( 'NONE',  ( 5.369276582105083406, -15.91634619257528627, 14.07054258737598573 ) ) ;
#91258=CARTESIAN_POINT ( 'NONE',  ( -1.000000000000000000, -69.59657292933731298, 12.76848391598547394 ) ) ;
#91278=CARTESIAN_POINT ( 'NONE',  ( -1.725809793176851681, -53.91240363267208124, 40.89521640499670241 ) ) ;
#91296=FACE_OUTER_BOUND ( 'NONE', #21031, .T. ) ;
#91309=SURFACE_SIDE_STYLE ('',( #60543 ) ) ;
#91345=ORIENTED_EDGE ( 'NONE', *, *, #5015, .T. ) ;
#91348=CARTESIAN_POINT ( 'NONE',  ( -5.232798140227934880, -1.976627073750570673, 104.1190344879413914 ) ) ;
#91351=CARTESIAN_POINT ( 'NONE',  ( 6.125000000000000888, -80.00000000000000000, 14.41094225130411033 ) ) ;
#91364=CARTESIAN_POINT ( 'NONE',  ( 15.86067392853018632, -3.472586522186453806, 14.59605311390719784 ) ) ;
#91373=CARTESIAN_POINT ( 'NONE',  ( 1.898590314185344186, -0.1325191295835281280, 102.2339902357106780 ) ) ;
#91379=CARTESIAN_POINT ( 'NONE',  ( -3.438773559904606980, -49.17061000814768335, 103.7823003339747601 ) ) ;
#91392=FILL_AREA_STYLE_COLOUR ( '', #106584 ) ;
#91398=PRESENTATION_STYLE_ASSIGNMENT (( #58494 ) ) ;
#91401=ORIENTED_EDGE ( 'NONE', *, *, #21945, .T. ) ;
#91409=DIRECTION ( 'NONE',  ( 0.9984555975339683975, -0.000000000000000000, -0.05555555555555529573 ) ) ;
#91420=CARTESIAN_POINT ( 'NONE',  ( 4.051286199644065888, -48.60127012969240212, 103.8758286790405378 ) ) ;
#91428=FILL_AREA_STYLE ('',( #58523 ) ) ;
#91433=ORIENTED_EDGE ( 'NONE', *, *, #91607, .T. ) ;
#91438=CARTESIAN_POINT ( 'NONE',  ( 30.00000000000000000, 3.157894736842105754, 14.66382285868951030 ) ) ;
#91466=CARTESIAN_POINT ( 'NONE',  ( 12.24503781984882167, -5.251331492636921894, 20.21097953542564696 ) ) ;
#91472=CARTESIAN_POINT ( 'NONE',  ( 4.752062635003135860, -66.34841433710333547, 13.81155678746845794 ) ) ;
#91485=ORIENTED_EDGE ( 'NONE', *, *, #69631, .T. ) ;
#91492=VERTEX_POINT ( 'NONE', #124 ) ;
#91501=CARTESIAN_POINT ( 'NONE',  ( 5.959251246171458405, -13.44866041637670939, 13.58291813670162362 ) ) ;
#91537=COLOUR_RGB ( '', 0.72549020, 0.75294118, 0.79215686) ;
#91546=ORIENTED_EDGE ( 'NONE', *, *, #66887, .T. ) ;
#91599=EDGE_CURVE ( 'NONE', #67261, #41862, #84444, .T. ) ;
#91600=ORIENTED_EDGE ( 'NONE', *, *, #54863, .F. ) ;
#91607=EDGE_CURVE ( 'NONE', #3985, #8366, #62068, .T. ) ;
#91611=FILL_AREA_STYLE ('',( #34465 ) ) ;
#91669=CARTESIAN_POINT ( 'NONE',  ( 2.232946119676683772, -69.45268377165729135, 12.90885355194285999 ) ) ;
#91682=DIRECTION ( 'NONE',  ( 0.000000000000000000, 0.000000000000000000, 1.000000000000000000 ) ) ;
#91698=( NAMED_UNIT ( * ) SI_UNIT ( $, .STERADIAN. ) SOLID_ANGLE_UNIT ( ) );
#91701=CARTESIAN_POINT ( 'NONE',  ( -5.385673916453011856, 0.000000000000000000, 18.57417562100670949 ) ) ;
#91715=FACE_OUTER_BOUND ( 'NONE', #28918, .T. ) ;
#91727=EDGE_CURVE ( 'NONE', #40703, #51662, #32875, .T. ) ;
#91733=CARTESIAN_POINT ( 'NONE',  ( -3.964299495114179450, -48.70984094615566562, 103.9028936078247085 ) ) ;
#91743=AXIS2_PLACEMENT_3D ( 'NONE', #65686, #66756, #24198 ) ;
#91768=CARTESIAN_POINT ( 'NONE',  ( -1.450088712723273554, -0.02381973979900874755, 101.4852321302689688 ) ) ;
#91771=DIRECTION ( 'NONE',  ( 0.000000000000000000, 0.000000000000000000, 1.000000000000000000 ) ) ;
#91776=CARTESIAN_POINT ( 'NONE',  ( 4.470309410577035791, -8.781697353302565290, 13.55535895067712815 ) ) ;
#91789=CARTESIAN_POINT ( 'NONE',  ( 0.000000000000000000, -78.00000000000000000, 27.00000000000000000 ) ) ;
#91819=FILL_AREA_STYLE_COLOUR ( '', #89348 ) ;
#91825=CARTESIAN_POINT ( 'NONE',  ( -15.90614609307868399, -3.157894736842107530, 14.66382285868950675 ) ) ;
#91826=( NAMED_UNIT ( * ) PLANE_ANGLE_UNIT ( ) SI_UNIT ( $, .RADIAN. ) );
#91863=CARTESIAN_POINT ( 'NONE',  ( 3.352941176471718077, -1.200583151107622815, 104.5794940929782797 ) ) ;
#91865=CARTESIAN_POINT ( 'NONE',  ( -4.312270534944379285, -9.512596744310554797, -11.64851190995530139 ) ) ;
#91883=( GEOMETRIC_REPRESENTATION_CONTEXT ( 3 ) GLOBAL_UNCERTAINTY_ASSIGNED_CONTEXT ( ( #66709 ) ) GLOBAL_UNIT_ASSIGNED_CONTEXT ( ( #67286, #59196, #78024 ) ) REPRESENTATION_CONTEXT ( 'NONE', 'WORKASPACE' ) );
#91898=CARTESIAN_POINT ( 'NONE',  ( -3.369683342533021708, -49.08678202233276977, 104.1613013819151519 ) ) ;
#91941=CARTESIAN_POINT ( 'NONE',  ( 6.999999999999997335, -46.00000000000000000, 39.12435565298214613 ) ) ;
#91945=EDGE_CURVE ( 'NONE', #99731, #47025, #100314, .T. ) ;
#91982=CARTESIAN_POINT ( 'NONE',  ( -1.226484165780726832, -49.99515885551645766, 101.2642634682685951 ) ) ;
#91985=CARTESIAN_POINT ( 'NONE',  ( 5.009049782182684041, -64.84921313000529608, 13.89804781769288944 ) ) ;
#91986=EDGE_CURVE ( 'NONE', #57238, #74417, #60441, .T. ) ;
#92002=PLANE ( 'NONE',  #81670 ) ;
#92009=ORIENTED_EDGE ( 'NONE', *, *, #91599, .F. ) ;
#92015=CARTESIAN_POINT ( 'NONE',  ( 6.031968554556502049, -14.91855978929650561, 14.31416968664684575 ) ) ;
#92025=EDGE_CURVE ( 'NONE', #63587, #91492, #63532, .T. ) ;
#92027=UNCERTAINTY_MEASURE_WITH_UNIT (LENGTH_MEASURE( 1.000000000000000082E-05 ), #82656, 'distance_accuracy_value', 'NONE');
#92033=CARTESIAN_POINT ( 'NONE',  ( 27.99999999999999645, 0.000000000000000000, -11.00000000000000000 ) ) ;
#92054=DIRECTION ( 'NONE',  ( 0.000000000000000000, 1.000000000000000000, 0.000000000000000000 ) ) ;
#92087=CARTESIAN_POINT ( 'NONE',  ( 3.352941176470599860, -1.200583151104954061, 104.5794940929807524 ) ) ;
#92111=ORIENTED_EDGE ( 'NONE', *, *, #64252, .T. ) ;
#92119=SURFACE_STYLE_USAGE ( .BOTH. , #10661 ) ;
#92148=MECHANICAL_DESIGN_GEOMETRIC_PRESENTATION_REPRESENTATION('',(#61222),#2604);
#92150=CARTESIAN_POINT ( 'NONE',  ( 9.397785531853783070, -3.220433213403954831, 14.78444596218915130 ) ) ;
#92179=ORIENTED_EDGE ( 'NONE', *, *, #11163, .F. ) ;
#92187=FACE_OUTER_BOUND ( 'NONE', #21767, .T. ) ;
#92213=CARTESIAN_POINT ( 'NONE',  ( 4.551587301587304957, -1.200583151104947843, 104.4018401814738155 ) ) ;
#92226=CARTESIAN_POINT ( 'NONE',  ( -1.000000000001115108, -69.90918681875037066, 12.94764124286841067 ) ) ;
#92255=CARTESIAN_POINT ( 'NONE',  ( -5.000000000000000000, -13.99331560178746869, 11.59713945945469504 ) ) ;
#92279=CARTESIAN_POINT ( 'NONE',  ( 6.227327457448970094, -7.358135131406661422, 13.83618408075120776 ) ) ;
#92316=( LENGTH_UNIT ( ) NAMED_UNIT ( * ) SI_UNIT ( .MILLI., .METRE. ) );
#92326=FILL_AREA_STYLE_COLOUR ( '', #34033 ) ;
#92327=ORIENTED_EDGE ( 'NONE', *, *, #19855, .T. ) ;
#92340=CARTESIAN_POINT ( 'NONE',  ( 9.045527390509329635, -0.3367924543029778839, 19.71820488350171274 ) ) ;
#92373=DIRECTION ( 'NONE',  ( 0.000000000000000000, 0.000000000000000000, 1.000000000000000000 ) ) ;
#92381=CARTESIAN_POINT ( 'NONE',  ( 4.284822031654965002, -1.092833614412281884, 104.4267991316945086 ) ) ;
#92388=CARTESIAN_POINT ( 'NONE',  ( 3.352941176470599860, -1.200583151104954061, 104.5794940929807524 ) ) ;
#92397=CARTESIAN_POINT ( 'NONE',  ( 7.595889545591794523, -12.40783199751988697, 8.429977207772983760 ) ) ;
#92415=CARTESIAN_POINT ( 'NONE',  ( 5.803898591548207087, -3.468598768277492805, 103.8893302396401026 ) ) ;
#92461=CIRCLE ( 'NONE', #97606, 2.000000000000000000 ) ;
#92463=CARTESIAN_POINT ( 'NONE',  ( 0.9999999999999940048, -50.00000000000000000, 44.97220075561143204 ) ) ;
#92493=CARTESIAN_POINT ( 'NONE',  ( 4.999999999999996447, -46.28647768034126386, 42.58845726811991739 ) ) ;
#92496=CARTESIAN_POINT ( 'NONE',  ( -7.000000000000000000, -60.71953810597521795, 12.61250543006203273 ) ) ;
#92538=ORIENTED_EDGE ( 'NONE', *, *, #100251, .T. ) ;
#92547=CARTESIAN_POINT ( 'NONE',  ( 4.999999999999920064, -15.02849299145039552, 13.75080192255986766 ) ) ;
#92559=VERTEX_POINT ( 'NONE', #49826 ) ;
#92568=SURFACE_STYLE_FILL_AREA ( #99586 ) ;
#92604=CARTESIAN_POINT ( 'NONE',  ( -3.857142857142850989, -1.200583151104938517, 103.1763305333244318 ) ) ;
#92630=CARTESIAN_POINT ( 'NONE',  ( 3.833393730521447829, -52.97426161280114343, 40.46628978130268450 ) ) ;
#92633=DIRECTION ( 'NONE',  ( 2.742080092235280244E-17, 0.000000000000000000, -1.000000000000000000 ) ) ;
#92636=STYLED_ITEM ( 'NONE', ( #719 ), #30042 ) ;
#92680=EDGE_CURVE ( 'NONE', #6033, #44023, #32951, .T. ) ;
#92690=CARTESIAN_POINT ( 'NONE',  ( 15.90614609307868399, -3.157894736842107086, 14.66382285868950852 ) ) ;
#92698=MECHANICAL_DESIGN_GEOMETRIC_PRESENTATION_REPRESENTATION('',(#4860),#80602);
#92733=MECHANICAL_DESIGN_GEOMETRIC_PRESENTATION_REPRESENTATION('',(#68655),#94454);
#92739=FACE_OUTER_BOUND ( 'NONE', #57607, .T. ) ;
#92792=EDGE_CURVE ( 'NONE', #43338, #88345, #19646, .T. ) ;
#92801=CARTESIAN_POINT ( 'NONE',  ( -5.000000000000000000, -13.79686997522500036, 10.70729389128589659 ) ) ;
#92818=CARTESIAN_POINT ( 'NONE',  ( -1.888159750444540430, -0.09357170100955422565, 101.9303315792851947 ) ) ;
#92825=CARTESIAN_POINT ( 'NONE',  ( -9.215420734788356327, -54.00000000000001421, 23.11721482942554928 ) ) ;
#92874=CARTESIAN_POINT ( 'NONE',  ( -27.99999999999999645, 1.836970198721029589E-15, -15.00000000000000000 ) ) ;
#92880=PRESENTATION_STYLE_ASSIGNMENT (( #84266 ) ) ;
#92908=( LENGTH_UNIT ( ) NAMED_UNIT ( * ) SI_UNIT ( .MILLI., .METRE. ) );
#92915=CARTESIAN_POINT ( 'NONE',  ( 4.245164436742090430, -1.071807799196438316, 104.4592797835113061 ) ) ;
#92921=CARTESIAN_POINT ( 'NONE',  ( -6.999999999999975131, -12.54465221550630183, 8.223849511754991681 ) ) ;
#92922=DIRECTION ( 'NONE',  ( 0.000000000000000000, 0.000000000000000000, -1.000000000000000000 ) ) ;
#92939=EDGE_CURVE ( 'NONE', #86174, #103837, #31461, .T. ) ;
#92942=DIRECTION ( 'NONE',  ( 0.000000000000000000, 0.000000000000000000, -1.000000000000000000 ) ) ;
#92949=ADVANCED_FACE ( 'NONE', ( #49153 ), #26786, .F. ) ;
#92960=CARTESIAN_POINT ( 'NONE',  ( -3.384215095276469132, -49.13301901873835220, 104.0501775326191876 ) ) ;
#92969=CARTESIAN_POINT ( 'NONE',  ( 0.9999999999999956701, -4.000000000000000000, 42.58845726811989607 ) ) ;
#92974=VECTOR ( 'NONE', #80171, 1000.000000000000000 ) ;
#92986=CARTESIAN_POINT ( 'NONE',  ( 30.00000000000000000, 0.000000000000000000, 0.000000000000000000 ) ) ;
#92997=EDGE_CURVE ( 'NONE', #62818, #47025, #90446, .T. ) ;
#93006=CARTESIAN_POINT ( 'NONE',  ( 3.733302338951465682, -48.92326939679833231, 43.79944126545571237 ) ) ;
#93032=STYLED_ITEM ( 'NONE', ( #95762 ), #49080 ) ;
#93046=AXIS2_PLACEMENT_3D ( 'NONE', #92969, #67109, #101059 ) ;
#93084=CARTESIAN_POINT ( 'NONE',  ( 3.653337153954944405, -8.634979741397113884, -12.30782724873841083 ) ) ;
#93086=B_SPLINE_CURVE_WITH_KNOTS ( 'NONE', 3,
 ( #67808, #85059, #78023, #93685, #102296, #76414, #37068, #2525, #44609, #86672, #27397, #92604 ),
 .UNSPECIFIED., .F., .F.,
 ( 4, 2, 2, 2, 2, 4 ),
 ( 0.000000000000000000, 0.0008247946606697857024, 0.001649589321339571405, 0.002061986651674464419, 0.002474383982009356782, 0.003299178642679125896 ),
 .UNSPECIFIED. ) ;
#93101=CARTESIAN_POINT ( 'NONE',  ( -13.56225034990342948, -55.77878166967040130, 23.52491571494838851 ) ) ;
#93105=EDGE_LOOP ( 'NONE', ( #92009, #32608, #11198, #23761 ) ) ;
#93132=B_SPLINE_CURVE_WITH_KNOTS ( 'NONE', 3,
 ( #28802, #94573, #20722, #83786, #9898, #68703 ),
 .UNSPECIFIED., .F., .F.,
 ( 4, 2, 4 ),
 ( 0.000000000000000000, 0.0003916983043530463489, 0.0007833966087060926977 ),
 .UNSPECIFIED. ) ;
#93210=( NAMED_UNIT ( * ) SI_UNIT ( $, .STERADIAN. ) SOLID_ANGLE_UNIT ( ) );
#93216=AXIS2_PLACEMENT_3D ( 'NONE', #106461, #65492, #98379 ) ;
#93232=CARTESIAN_POINT ( 'NONE',  ( 3.685905252136403742, -48.95891067205271696, 104.2837900504726036 ) ) ;
#93254=CARTESIAN_POINT ( 'NONE',  ( 6.999999995588868984, -13.84708942052852798, -5.798489586937981777 ) ) ;
#93286=SURFACE_SIDE_STYLE ('',( #70068 ) ) ;
#93290=EDGE_CURVE ( 'NONE', #33722, #57238, #79505, .T. ) ;
#93309=CARTESIAN_POINT ( 'NONE',  ( -15.90614609307868577, -3.157894736842107086, 14.66382285868950852 ) ) ;
#93321=B_SPLINE_CURVE_WITH_KNOTS ( 'NONE', 3,
 ( #84706, #50714, #3261, #42647, #60459, #19487, #83627, #36202 ),
 .UNSPECIFIED., .F., .F.,
 ( 4, 2, 2, 4 ),
 ( 0.000000000000000000, 7.350793746624747918E-05, 0.0001470158749324949584, 0.0002940317498649912720 ),
 .UNSPECIFIED. ) ;
#93325=FACE_OUTER_BOUND ( 'NONE', #9624, .T. ) ;
#93333=VERTEX_POINT ( 'NONE', #64189 ) ;
#93341=SURFACE_SIDE_STYLE ('',( #94410 ) ) ;
#93345=DIRECTION ( 'NONE',  ( -0.000000000000000000, 1.000000000000000000, -0.000000000000000000 ) ) ;
#93348=CARTESIAN_POINT ( 'NONE',  ( -13.53380759260212329, -51.99094200876919558, 30.58586009444553611 ) ) ;
#93365=CARTESIAN_POINT ( 'NONE',  ( -3.841398122528327352, -1.072224703192198536, 104.5835869663332574 ) ) ;
#93401=CARTESIAN_POINT ( 'NONE',  ( 3.471301144393632576, -49.15628846923404183, 103.7432070447315908 ) ) ;
#93411=UNCERTAINTY_MEASURE_WITH_UNIT (LENGTH_MEASURE( 1.000000000000000082E-05 ), #46948, 'distance_accuracy_value', 'NONE');
#93414=CARTESIAN_POINT ( 'NONE',  ( -3.713158817312831594, -1.053630055818222333, 103.2987150069905624 ) ) ;
#93415=CARTESIAN_POINT ( 'NONE',  ( -6.999999999999999112, 0.000000000000000000, 0.000000000000000000 ) ) ;
#93416=ORIENTED_EDGE ( 'NONE', *, *, #1204, .F. ) ;
#93425=FACE_OUTER_BOUND ( 'NONE', #22024, .T. ) ;
#93439=DIRECTION ( 'NONE',  ( -0.000000000000000000, -1.000000000000000000, -0.000000000000000000 ) ) ;
#93470=CARTESIAN_POINT ( 'NONE',  ( 1.000000000000000000, -43.18879712712265473, 0.3952393630211145092 ) ) ;
#93473=( NAMED_UNIT ( * ) SI_UNIT ( $, .STERADIAN. ) SOLID_ANGLE_UNIT ( ) );
#93487=CARTESIAN_POINT ( 'NONE',  ( 15.38483753811592969, -5.586071175641518671, 13.93514129277331115 ) ) ;
#93538=AXIS2_PLACEMENT_3D ( 'NONE', #37849, #71750, #95005 ) ;
#93552=CARTESIAN_POINT ( 'NONE',  ( 4.243523009780798994, -48.34445764549300151, 43.36978758336660178 ) ) ;
#93571=CARTESIAN_POINT ( 'NONE',  ( -3.121913957742261658, -49.49713245390870497, 40.80120573642129500 ) ) ;
#93591=CARTESIAN_POINT ( 'NONE',  ( -3.096826397206294601, -49.41329697661214482, 103.2812258104289640 ) ) ;
#93595=ORIENTED_EDGE ( 'NONE', *, *, #51954, .F. ) ;
#93623=EDGE_CURVE ( 'NONE', #104941, #77653, #67509, .T. ) ;
#93641=CARTESIAN_POINT ( 'NONE',  ( -5.596957125887387363, -47.31575451833741397, 103.9718581041641698 ) ) ;
#93648=PRESENTATION_STYLE_ASSIGNMENT (( #58620 ) ) ;
#93685=CARTESIAN_POINT ( 'NONE',  ( -4.861072549008415677, -2.920843450830509447, 102.3606070684416665 ) ) ;
#93698=CARTESIAN_POINT ( 'NONE',  ( 13.95408269174820148, -50.12993014906734146, 28.16184020435892421 ) ) ;
#93700=DIRECTION ( 'NONE',  ( 0.000000000000000000, 1.000000000000000000, 0.000000000000000000 ) ) ;
#93706=CARTESIAN_POINT ( 'NONE',  ( 27.99999999999999645, 0.000000000000000000, 0.000000000000000000 ) ) ;
#93711=SURFACE_SIDE_STYLE ('',( #30583 ) ) ;
#93724=ORIENTED_EDGE ( 'NONE', *, *, #87955, .F. ) ;
#93726=ADVANCED_FACE ( 'NONE', ( #98396 ), #14198, .T. ) ;
#93756=CARTESIAN_POINT ( 'NONE',  ( 1.927505563446688663, -70.56453101740132183, 13.13085817996164550 ) ) ;
#93762=VERTEX_POINT ( 'NONE', #61144 ) ;
#93768=CARTESIAN_POINT ( 'NONE',  ( 3.369683342532912462, -49.08678202233288346, 104.1613013819149387 ) ) ;
#93791=CARTESIAN_POINT ( 'NONE',  ( 1.459252261608878998, -6.102732174926768671, -13.75226092436929548 ) ) ;
#93810=FILL_AREA_STYLE_COLOUR ( '', #70488 ) ;
#93826=( LENGTH_UNIT ( ) NAMED_UNIT ( * ) SI_UNIT ( .MILLI., .METRE. ) );
#93837=CARTESIAN_POINT ( 'NONE',  ( -12.40685984127932961, -3.384540406130107204, 20.61063982846911102 ) ) ;
#93861=( GEOMETRIC_REPRESENTATION_CONTEXT ( 3 ) GLOBAL_UNCERTAINTY_ASSIGNED_CONTEXT ( ( #59546 ) ) GLOBAL_UNIT_ASSIGNED_CONTEXT ( ( #77584, #37156, #52767 ) ) REPRESENTATION_CONTEXT ( 'NONE', 'WORKASPACE' ) );
#93884=DIRECTION ( 'NONE',  ( 0.000000000000000000, 0.000000000000000000, -1.000000000000000000 ) ) ;
#93898=DIRECTION ( 'NONE',  ( 0.000000000000000000, 1.000000000000000000, 0.000000000000000000 ) ) ;
#93925=CARTESIAN_POINT ( 'NONE',  ( 1.910332202385215838, -49.86383299196077701, 102.2504571675874274 ) ) ;
#93951=DIRECTION ( 'NONE',  ( 0.000000000000000000, 0.000000000000000000, -1.000000000000000000 ) ) ;
#93955=CARTESIAN_POINT ( 'NONE',  ( 9.397061706953902416, 2.827687757435164873, 14.73115738288152166 ) ) ;
#93990=CARTESIAN_POINT ( 'NONE',  ( 3.438773559903462118, -0.8293899918514395786, 103.7823003339744901 ) ) ;
#94006=CARTESIAN_POINT ( 'NONE',  ( 13.99657022045423282, -57.97469379117722355, 26.59685899168112400 ) ) ;
#94027=CARTESIAN_POINT ( 'NONE',  ( -3.349796915293434374, -48.86785030187986223, 104.5044954676190798 ) ) ;
#94040=ORIENTED_EDGE ( 'NONE', *, *, #80520, .T. ) ;
#94042=LINE ( 'NONE', #61706, #86020 ) ;
#94049=ORIENTED_EDGE ( 'NONE', *, *, #33268, .T. ) ;
#94052=CARTESIAN_POINT ( 'NONE',  ( -9.215420734788356327, -54.00000000000001421, 23.11721482942554928 ) ) ;
#94070=ORIENTED_EDGE ( 'NONE', *, *, #96113, .F. ) ;
#94071=CARTESIAN_POINT ( 'NONE',  ( 2.300474593523000433, -49.78500928328203656, 44.63801405044423376 ) ) ;
#94094=( LENGTH_UNIT ( ) NAMED_UNIT ( * ) SI_UNIT ( .MILLI., .METRE. ) );
#94160=( BOUNDED_SURFACE ( )  B_SPLINE_SURFACE ( 3, 2, ( 
 ( #6262, #37636, #72076 ),
 ( #31129, #23026, #70500 ),
 ( #12241, #81208, #74186 ),
 ( #25147, #32709, #40763 ) ),
 .UNSPECIFIED., .F., .F., .F. ) 
 B_SPLINE_SURFACE_WITH_KNOTS ( ( 4, 4 ),
 ( 3, 3 ),
 ( 0.02391116761306513738, 0.02588704022068540056 ),
 ( 0.000000000000000000, 1.000000000000000000 ),
 .UNSPECIFIED. ) 
 GEOMETRIC_REPRESENTATION_ITEM ( )  RATIONAL_B_SPLINE_SURFACE ( (
 ( 1.000000000000000000, 0.9661530732048717596, 1.000000000000000000),
 ( 1.000000000000000000, 0.9668590359504447562, 1.000000000000000000),
 ( 1.000000000000000000, 0.9668459061114134112, 1.000000000000000000),
 ( 1.000000000000000000, 0.9661530732048707604, 1.000000000000000000) ) ) 
 REPRESENTATION_ITEM ( '' )  SURFACE ( )  );
#94166=CYLINDRICAL_SURFACE ( 'NONE', #69768, 7.000000000000006217 ) ;
#94169=AXIS2_PLACEMENT_3D ( 'NONE', #40006, #41595, #7091 ) ;
#94171=( BOUNDED_SURFACE ( )  B_SPLINE_SURFACE ( 3, 2, ( 
 ( #83307, #83836, #32670 ),
 ( #49875, #98942, #26191 ),
 ( #65540, #82240, #66064 ),
 ( #49332, #91420, #41257 ) ),
 .UNSPECIFIED., .F., .F., .T. ) 
 B_SPLINE_SURFACE_WITH_KNOTS ( ( 4, 4 ),
 ( 3, 3 ),
 ( 7.589415207398531038E-19, 0.0009806926547533865134 ),
 ( 0.000000000000000000, 1.000000000000000000 ),
 .UNSPECIFIED. ) 
 GEOMETRIC_REPRESENTATION_ITEM ( )  RATIONAL_B_SPLINE_SURFACE ( (
 ( 1.000000000000000000, 0.9603284238771502279, 1.000000000000000000),
 ( 1.000000000000000000, 0.9551945799212738786, 1.000000000000000000),
 ( 1.000000000000000000, 0.9458776633876959661, 1.000000000000000000),
 ( 1.000000000000000000, 0.9359444767143307864, 1.000000000000000000) ) ) 
 REPRESENTATION_ITEM ( '' )  SURFACE ( )  );
#94173=CARTESIAN_POINT ( 'NONE',  ( 12.39255972526328087, -3.227357870849989041, 20.63924567340875527 ) ) ;
#94176=DIRECTION ( 'NONE',  ( 0.000000000000000000, 0.000000000000000000, -1.000000000000000000 ) ) ;
#94181=EDGE_CURVE ( 'NONE', #67261, #63106, #15910, .T. ) ;
#94188=CARTESIAN_POINT ( 'NONE',  ( 1.000000000000000000, -69.59657292934913642, 12.76848391599222765 ) ) ;
#94189=DIRECTION ( 'NONE',  ( 1.000000000000000000, -0.000000000000000000, 1.224646799147353207E-16 ) ) ;
#94240=CARTESIAN_POINT ( 'NONE',  ( 2.399714434301968069, -53.72915769422170484, 40.79469093396801327 ) ) ;
#94264=ORIENTED_EDGE ( 'NONE', *, *, #91986, .F. ) ;
#94273=EDGE_LOOP ( 'NONE', ( #24840, #51916, #59688, #51032 ) ) ;
#94275=DIRECTION ( 'NONE',  ( 0.000000000000000000, 0.000000000000000000, 1.000000000000000000 ) ) ;
#94293=CARTESIAN_POINT ( 'NONE',  ( 3.553996988732007534, -69.76421179181549803, 13.45721127476620005 ) ) ;
#94305=CARTESIAN_POINT ( 'NONE',  ( 3.365451957726352639, -49.06858650466293881, 104.1992105446093859 ) ) ;
#94315=EDGE_LOOP ( 'NONE', ( #69740, #26365, #33235, #65002, #88937 ) ) ;
#94331=CARTESIAN_POINT ( 'NONE',  ( 2.152702816551222309, -7.044814775684611341, -13.28738398835386292 ) ) ;
#94341=VECTOR ( 'NONE', #10893, 1000.000000000000000 ) ;
#94379=DIRECTION ( 'NONE',  ( 0.000000000000000000, 0.000000000000000000, -1.000000000000000000 ) ) ;
#94381=CARTESIAN_POINT ( 'NONE',  ( -11.08629307112589224, -1.234131506493649333, 20.41691545949602826 ) ) ;
#94409=CARTESIAN_POINT ( 'NONE',  ( -7.000000000000007105, -12.54465221550630716, 8.223849511754988129 ) ) ;
#94410=SURFACE_STYLE_FILL_AREA ( #4857 ) ;
#94414=PRESENTATION_STYLE_ASSIGNMENT (( #77151 ) ) ;
#94438=CARTESIAN_POINT ( 'NONE',  ( -3.504981525174552193, -68.37518638738055188, 13.08580713192159095 ) ) ;
#94454=( GEOMETRIC_REPRESENTATION_CONTEXT ( 3 ) GLOBAL_UNCERTAINTY_ASSIGNED_CONTEXT ( ( #85829 ) ) GLOBAL_UNIT_ASSIGNED_CONTEXT ( ( #18046, #42292, #34245 ) ) REPRESENTATION_CONTEXT ( 'NONE', 'WORKASPACE' ) );
#94476=TOROIDAL_SURFACE ( 'NONE', #68608, 18.00000000000000355, 4.000000000000000000 ) ;
#94482=( GEOMETRIC_REPRESENTATION_CONTEXT ( 3 ) GLOBAL_UNCERTAINTY_ASSIGNED_CONTEXT ( ( #14986 ) ) GLOBAL_UNIT_ASSIGNED_CONTEXT ( ( #40075, #82111, #16874 ) ) REPRESENTATION_CONTEXT ( 'NONE', 'WORKASPACE' ) );
#94485=ORIENTED_EDGE ( 'NONE', *, *, #106145, .T. ) ;
#94525=CARTESIAN_POINT ( 'NONE',  ( -0.9999999999999943379, -1.409462824231155764E-15, 101.0455488498966758 ) ) ;
#94531=FACE_OUTER_BOUND ( 'NONE', #80306, .T. ) ;
#94559=CARTESIAN_POINT ( 'NONE',  ( 13.87268571384243465, -57.59061059622465706, 28.89968788215285755 ) ) ;
#94563=PRESENTATION_STYLE_ASSIGNMENT (( #27732 ) ) ;
#94573=CARTESIAN_POINT ( 'NONE',  ( 3.778364440264287083, -48.87981973393538482, 103.2432911248130978 ) ) ;
#94581=CARTESIAN_POINT ( 'NONE',  ( 4.031080902170319114, -1.378107924927665318, 103.0284855429829207 ) ) ;
#94606=EDGE_LOOP ( 'NONE', ( #91401, #65839, #6693, #27797 ) ) ;
#94619=STYLED_ITEM ( 'NONE', ( #85419 ), #12484 ) ;
#94626=CARTESIAN_POINT ( 'NONE',  ( 2.423637387739231652, -49.74034360832548884, 44.58576659056175373 ) ) ;
#94638=VECTOR ( 'NONE', #74582, 1000.000000000000000 ) ;
#94643=CARTESIAN_POINT ( 'NONE',  ( -0.9999999999999943379, -50.00000000000000000, 101.0455488498966758 ) ) ;
#94648=CARTESIAN_POINT ( 'NONE',  ( -4.464818165989834498, -48.01567804769277359, 43.16242680068418736 ) ) ;
#94659=EDGE_CURVE ( 'NONE', #25863, #101939, #45265, .T. ) ;
#94679=DIRECTION ( 'NONE',  ( 0.000000000000000000, 1.000000000000000000, 0.000000000000000000 ) ) ;
#94706=DIRECTION ( 'NONE',  ( -1.000000000000000000, -0.000000000000000000, -0.000000000000000000 ) ) ;
#94718=CARTESIAN_POINT ( 'NONE',  ( -13.99656100229485389, -57.97463508733147819, 26.59581618167199579 ) ) ;
#94725=DIRECTION ( 'NONE',  ( 1.000000000000000000, 0.000000000000000000, 0.000000000000000000 ) ) ;
#94732=ADVANCED_FACE ( 'NONE', ( #38881 ), #102142, .T. ) ;
#94789=( NAMED_UNIT ( * ) PLANE_ANGLE_UNIT ( ) SI_UNIT ( $, .RADIAN. ) );
#94798=CARTESIAN_POINT ( 'NONE',  ( 6.999999999999996447, -4.000000000000003553, 39.12435565298213902 ) ) ;
#94799=ORIENTED_EDGE ( 'NONE', *, *, #33526, .T. ) ;
#94835=CARTESIAN_POINT ( 'NONE',  ( 5.484304246340809819, -66.41744476707179956, 14.11761977215489061 ) ) ;
#94840=ORIENTED_EDGE ( 'NONE', *, *, #52145, .T. ) ;
#94841=CARTESIAN_POINT ( 'NONE',  ( -6.223369765831527012, -7.361822309467675574, 13.83569840248939897 ) ) ;
#94844=CARTESIAN_POINT ( 'NONE',  ( 3.438773559904778843, -49.17061000814753413, 103.7823003339739074 ) ) ;
#94880=CARTESIAN_POINT ( 'NONE',  ( -5.285714285714275817, -50.19912527334259522, 103.1763305333244318 ) ) ;
#94890=FILL_AREA_STYLE_COLOUR ( '', #36660 ) ;
#94902=CARTESIAN_POINT ( 'NONE',  ( 3.498313567328457108, -0.8571732103886707810, 104.2430177423142936 ) ) ;
#94918=CARTESIAN_POINT ( 'NONE',  ( -11.47498123831195649, 2.263339934408738152, 14.82868161565088450 ) ) ;
#94943=VERTEX_POINT ( 'NONE', #60911 ) ;
#94946=CARTESIAN_POINT ( 'NONE',  ( -0.8750000000009734435, -70.58759490697451611, 13.02737050516266315 ) ) ;
#94972=CARTESIAN_POINT ( 'NONE',  ( -3.223917338551602008, -68.72997618365062067, 13.04841264822337443 ) ) ;
#94973=SURFACE_SIDE_STYLE ('',( #44826 ) ) ;
#95005=DIRECTION ( 'NONE',  ( 0.000000000000000000, 0.000000000000000000, 1.000000000000000000 ) ) ;
#95040=DIRECTION ( 'NONE',  ( 1.000000000000000000, -0.000000000000000000, 1.224646799147353207E-16 ) ) ;
#95056=( NAMED_UNIT ( * ) SI_UNIT ( $, .STERADIAN. ) SOLID_ANGLE_UNIT ( ) );
#95065=ORIENTED_EDGE ( 'NONE', *, *, #71814, .F. ) ;
#95070=CARTESIAN_POINT ( 'NONE',  ( -2.152702816552580778, -7.044814775684473673, -13.28738398835509216 ) ) ;
#95089=CARTESIAN_POINT ( 'NONE',  ( 3.415268766438305459, -49.17042234883166429, 103.8819051289220710 ) ) ;
#95128=VERTEX_POINT ( 'NONE', #32258 ) ;
#95132=CARTESIAN_POINT ( 'NONE',  ( 3.352941176470589646, -48.79941684889505638, 104.5794940929807524 ) ) ;
#95141=( NAMED_UNIT ( * ) PLANE_ANGLE_UNIT ( ) SI_UNIT ( $, .RADIAN. ) );
#95166=CARTESIAN_POINT ( 'NONE',  ( -1.729304526577840617, -50.00420662738919475, 40.95323976638580632 ) ) ;
#95197=CARTESIAN_POINT ( 'NONE',  ( 0.9999999999999961142, 0.000000000000000000, 27.00000000000000000 ) ) ;
#95220=( GEOMETRIC_REPRESENTATION_CONTEXT ( 3 ) GLOBAL_UNCERTAINTY_ASSIGNED_CONTEXT ( ( #67542 ) ) GLOBAL_UNIT_ASSIGNED_CONTEXT ( ( #6910, #32280, #82930 ) ) REPRESENTATION_CONTEXT ( 'NONE', 'WORKASPACE' ) );
#95239=CARTESIAN_POINT ( 'NONE',  ( 11.33125095928769355, 2.319207801596048224, 14.82048394585365791 ) ) ;
#95290=CARTESIAN_POINT ( 'NONE',  ( 13.69901872062297166, -51.35359963483656287, 24.10656755472290769 ) ) ;
#95315=ORIENTED_EDGE ( 'NONE', *, *, #58322, .T. ) ;
#95334=ORIENTED_EDGE ( 'NONE', *, *, #13164, .T. ) ;
#95354=CARTESIAN_POINT ( 'NONE',  ( -11.55112723807207331, -8.861487880012006713, 19.08437505212382845 ) ) ;
#95371=CARTESIAN_POINT ( 'NONE',  ( 0.000000000000000000, -48.79941684889505638, 120.1428571428571388 ) ) ;
#95385=FILL_AREA_STYLE_COLOUR ( '', #2416 ) ;
#95411=SURFACE_SIDE_STYLE ('',( #36161 ) ) ;
#95417=CARTESIAN_POINT ( 'NONE',  ( 0.000000000000000000, -78.00000000000000000, 27.00000000000000000 ) ) ;
#95424=CARTESIAN_POINT ( 'NONE',  ( -11.18613547696531185, 2.364262554124563653, 14.81278392879739947 ) ) ;
#95436=CARTESIAN_POINT ( 'NONE',  ( 5.000000000000000000, 0.000000000000000000, 35.66025403784438907 ) ) ;
#95458=CARTESIAN_POINT ( 'NONE',  ( 0.9999999999999940048, -50.00000000000000000, 101.0455488498966758 ) ) ;
#95461=CARTESIAN_POINT ( 'NONE',  ( -13.87407757772530736, -50.52807032218477445, 25.11348823608586400 ) ) ;
#95478=CARTESIAN_POINT ( 'NONE',  ( -2.119141824078783376, -69.49710365781473342, 12.89375316341194377 ) ) ;
#95479=PRESENTATION_STYLE_ASSIGNMENT (( #45354 ) ) ;
#95488=ORIENTED_EDGE ( 'NONE', *, *, #98244, .T. ) ;
#95507=EDGE_CURVE ( 'NONE', #42044, #53428, #52309, .T. ) ;
#95541=CARTESIAN_POINT ( 'NONE',  ( -4.551587301587297851, -48.79941684889506348, 104.4018401814738013 ) ) ;
#95554=MECHANICAL_DESIGN_GEOMETRIC_PRESENTATION_REPRESENTATION('',(#55860),#83459);
#95570=CARTESIAN_POINT ( 'NONE',  ( -2.228836330356652073, -0.1847672526321134656, 102.4817230975930897 ) ) ;
#95573=UNCERTAINTY_MEASURE_WITH_UNIT (LENGTH_MEASURE( 1.000000000000000082E-05 ), #60464, 'distance_accuracy_value', 'NONE');
#95582=COLOUR_RGB ( '', 0.09019608, 0.27058824, 0.51372549) ;
#95612=CARTESIAN_POINT ( 'NONE',  ( 1.000000000000000000, -63.35320086167136822, 9.447768535959317759 ) ) ;
#95629=ORIENTED_EDGE ( 'NONE', *, *, #78625, .T. ) ;
#95676=DIRECTION ( 'NONE',  ( 0.000000000000000000, 0.000000000000000000, 1.000000000000000000 ) ) ;
#95685=CARTESIAN_POINT ( 'NONE',  ( -1.432938875184908145, -50.02820789671614676, 40.96157042262397852 ) ) ;
#95692=ORIENTED_EDGE ( 'NONE', *, *, #83882, .T. ) ;
#95706=FACE_OUTER_BOUND ( 'NONE', #29711, .T. ) ;
#95762=PRESENTATION_STYLE_ASSIGNMENT (( #23489 ) ) ;
#95773=EDGE_CURVE ( 'NONE', #76782, #85296, #105665, .T. ) ;
#95784=CARTESIAN_POINT ( 'NONE',  ( -1.184166769438234956, -69.62625514036700736, 12.78541671988950945 ) ) ;
#95823=CARTESIAN_POINT ( 'NONE',  ( 5.000000000000000000, -13.86855732159281018, 11.25329773914766918 ) ) ;
#95833=FILL_AREA_STYLE ('',( #71016 ) ) ;
#95861=CARTESIAN_POINT ( 'NONE',  ( -5.833333333391548692, -3.737948356783034942, 103.8776713793676834 ) ) ;
#95891=CARTESIAN_POINT ( 'NONE',  ( -5.369327769978998965, -15.91632837477424367, 14.07056384452391029 ) ) ;
#95896=STYLED_ITEM ( 'NONE', ( #75441 ), #100986 ) ;
#95920=STYLED_ITEM ( 'NONE', ( #103223 ), #66649 ) ;
#95929=CARTESIAN_POINT ( 'NONE',  ( 27.99999999999999645, 0.000000000000000000, 0.000000000000000000 ) ) ;
#95952=ADVANCED_FACE ( 'NONE', ( #76019 ), #1181, .F. ) ;
#95963=COLOUR_RGB ( '', 0.72549020, 0.75294118, 0.79215686) ;
#95965=CARTESIAN_POINT ( 'NONE',  ( -9.717036974652998538, 2.772147514592163908, 14.74200096892023026 ) ) ;
#95967=DIRECTION ( 'NONE',  ( -1.000000000000000000, -0.000000000000000000, -0.000000000000000000 ) ) ;
#95986=STYLED_ITEM ( 'NONE', ( #49747 ), #66973 ) ;
#96079=CARTESIAN_POINT ( 'NONE',  ( -5.000000000000000888, -51.24344465340260513, 3.816021516648668843 ) ) ;
#96085=MECHANICAL_DESIGN_GEOMETRIC_PRESENTATION_REPRESENTATION('',(#32354),#90928);
#96092=ADVANCED_FACE ( 'NONE', ( #64119 ), #74469, .T. ) ;
#96100=CARTESIAN_POINT ( 'NONE',  ( -3.363582653045783299, -1.214734195355907431, 104.5994639297836386 ) ) ;
#96103=CYLINDRICAL_SURFACE ( 'NONE', #61696, 4.000000000000003553 ) ;
#96113=EDGE_CURVE ( 'NONE', #26304, #62818, #77962, .T. ) ;
#96253=FACE_BOUND ( 'NONE', #44796, .T. ) ;
#96289=CARTESIAN_POINT ( 'NONE',  ( -30.00000000000000000, -54.00000000000000711, 31.11721482942554928 ) ) ;
#96320=ORIENTED_EDGE ( 'NONE', *, *, #20879, .T. ) ;
#96331=VERTEX_POINT ( 'NONE', #94643 ) ;
#96408=CARTESIAN_POINT ( 'NONE',  ( 4.999999999999999112, -12.54465221550629472, 8.223849511754998787 ) ) ;
#96429=CARTESIAN_POINT ( 'NONE',  ( -14.61009150661556255, -7.492150338152962163, 13.00688103712339050 ) ) ;
#96475=CARTESIAN_POINT ( 'NONE',  ( 3.714954396655703928, -1.055462661311022288, 103.2971887958214836 ) ) ;
#96500=AXIS2_PLACEMENT_3D ( 'NONE', #18582, #2357, #67646 ) ;
#96525=FILL_AREA_STYLE_COLOUR ( '', #23272 ) ;
#96528=SURFACE_STYLE_USAGE ( .BOTH. , #62570 ) ;
#96553=CARTESIAN_POINT ( 'NONE',  ( -3.355892750373183020, -49.00480196350172690, 104.3125661743345916 ) ) ;
#96610=CARTESIAN_POINT ( 'NONE',  ( -4.861072549008415677, -47.07915654916947545, 102.3606070684416665 ) ) ;
#96630=SURFACE_SIDE_STYLE ('',( #88540 ) ) ;
#96632=UNCERTAINTY_MEASURE_WITH_UNIT (LENGTH_MEASURE( 1.000000000000000082E-05 ), #57067, 'distance_accuracy_value', 'NONE');
#96641=CIRCLE ( 'NONE', #72538, 2.000000000000000000 ) ;
#96666=ORIENTED_EDGE ( 'NONE', *, *, #54688, .T. ) ;
#96710=CARTESIAN_POINT ( 'NONE',  ( -3.386172510860506968, -49.13793332017446147, 104.0372841442787006 ) ) ;
#96727=AXIS2_PLACEMENT_3D ( 'NONE', #95929, #87840, #106112 ) ;
#96755=CARTESIAN_POINT ( 'NONE',  ( 0.9999999999999954481, -50.00000000000000000, 44.97220075561143204 ) ) ;
#96827=CARTESIAN_POINT ( 'NONE',  ( 14.78075358320714905, 0.1660929298666962151, 15.00000000000000178 ) ) ;
#96846=CARTESIAN_POINT ( 'NONE',  ( -3.558726380635282016, -68.96874620124219746, 13.45354069684906229 ) ) ;
#96863=SURFACE_STYLE_USAGE ( .BOTH. , #72569 ) ;
#96900=PRESENTATION_STYLE_ASSIGNMENT (( #80166 ) ) ;
#96916=CARTESIAN_POINT ( 'NONE',  ( -4.725902370230324223, -2.526352736915706387, 103.4500010546506275 ) ) ;
#96922=CARTESIAN_POINT ( 'NONE',  ( 6.846801517543655180, -12.21872792266575658, 8.794481130080901821 ) ) ;
#96939=FILL_AREA_STYLE ('',( #50891 ) ) ;
#96991=( BOUNDED_SURFACE ( )  B_SPLINE_SURFACE ( 3, 2, ( 
 ( #59989, #68046, #102004 ),
 ( #84768, #19014, #49325 ),
 ( #61038, #76661, #51856 ),
 ( #43771, #67532, #93925 ),
 ( #82232, #100412, #101484 ),
 ( #20084, #98421, #26575 ),
 ( #27637, #60515, #8345 ),
 ( #93401, #59444, #19550 ),
 ( #86907, #55030, #70710 ),
 ( #45382, #61576, #104121 ) ),
 .UNSPECIFIED., .F., .F., .T. ) 
 B_SPLINE_SURFACE_WITH_KNOTS ( ( 4, 2, 2, 2, 4 ),
 ( 3, 3 ),
 ( -1.185673698478311820E-05, 0.001059589481406181949, 0.002131035699797147187, 0.003202481918188112425, 0.004273928136579077663 ),
 ( 0.000000000000000000, 1.000000000000000000 ),
 .UNSPECIFIED. ) 
 GEOMETRIC_REPRESENTATION_ITEM ( )  RATIONAL_B_SPLINE_SURFACE ( (
 ( 1.000000000000000000, 1.000000000000000000, 1.000000000000000000),
 ( 1.000000000000000000, 0.9999922502423410631, 1.000000000000000000),
 ( 1.000000000000000000, 0.9961090584666346670, 1.000000000000000000),
 ( 1.000000000000000000, 0.9800114100223730196, 1.000000000000000000),
 ( 1.000000000000000000, 0.9677016975220472661, 1.000000000000000000),
 ( 1.000000000000000000, 0.9345728642045315615, 1.000000000000000000),
 ( 1.000000000000000000, 0.9137480076090285230, 1.000000000000000000),
 ( 1.000000000000000000, 0.8628371017890346106, 1.000000000000000000),
 ( 1.000000000000000000, 0.8327438998408613902, 1.000000000000000000),
 ( 1.000000000000000000, 0.7973879088788907721, 1.000000000000000000) ) ) 
 REPRESENTATION_ITEM ( '' )  SURFACE ( )  );
#96994=SURFACE_STYLE_FILL_AREA ( #22067 ) ;
#97011=PRESENTATION_STYLE_ASSIGNMENT (( #72211 ) ) ;
#97014=DIRECTION ( 'NONE',  ( 0.000000000000000000, 0.000000000000000000, -1.000000000000000000 ) ) ;
#97020=( LENGTH_UNIT ( ) NAMED_UNIT ( * ) SI_UNIT ( .MILLI., .METRE. ) );
#97032=TOROIDAL_SURFACE ( 'NONE', #12643, 5.999999999999996447, 4.000000000000000000 ) ;
#97037=CARTESIAN_POINT ( 'NONE',  ( -5.962730926206976534, -13.90752838006589442, 13.89020537729797766 ) ) ;
#97124=CARTESIAN_POINT ( 'NONE',  ( -4.448407490268950326, -48.03096409756967944, 102.6871849564181218 ) ) ;
#97137=CIRCLE ( 'NONE', #33426, 11.00000000000000000 ) ;
#97138=VERTEX_POINT ( 'NONE', #51458 ) ;
#97153=STYLED_ITEM ( 'NONE', ( #100088 ), #85105 ) ;
#97171=EDGE_LOOP ( 'NONE', ( #70745, #61226, #58044, #79516, #2420 ) ) ;
#97184=CARTESIAN_POINT ( 'NONE',  ( -4.195612334302273538, -1.058759987296271632, 104.4881327927214159 ) ) ;
#97189=CARTESIAN_POINT ( 'NONE',  ( 1.000000000000000000, -51.23885339960735053, 3.814018968273865440 ) ) ;
#97191=CARTESIAN_POINT ( 'NONE',  ( 12.37144696128342503, -4.000000000000004441, 20.44658103856077602 ) ) ;
#97217=EDGE_CURVE ( 'NONE', #56644, #43338, #103969, .T. ) ;
#97221=EDGE_LOOP ( 'NONE', ( #22610, #104488, #52515, #97473 ) ) ;
#97233=MECHANICAL_DESIGN_GEOMETRIC_PRESENTATION_REPRESENTATION('',(#18028),#35291);
#97234=( GEOMETRIC_REPRESENTATION_CONTEXT ( 3 ) GLOBAL_UNCERTAINTY_ASSIGNED_CONTEXT ( ( #44015 ) ) GLOBAL_UNIT_ASSIGNED_CONTEXT ( ( #104759, #8186, #49707 ) ) REPRESENTATION_CONTEXT ( 'NONE', 'WORKASPACE' ) );
#97264=CARTESIAN_POINT ( 'NONE',  ( -7.163135071507197971, -15.11851566007659464, 14.95876950282627327 ) ) ;
#97266=CARTESIAN_POINT ( 'NONE',  ( -4.770986019692863955, -47.38877792675871348, 40.36182486515247803 ) ) ;
#97294=CARTESIAN_POINT ( 'NONE',  ( -2.691566728956864996, -0.5366288636816407553, 103.4274024144617954 ) ) ;
#97321=CARTESIAN_POINT ( 'NONE',  ( 1.469576158976823750E-15, -80.00000000000000000, 15.00000000000000000 ) ) ;
#97333=FILL_AREA_STYLE_COLOUR ( '', #13922 ) ;
#97334=DIRECTION ( 'NONE',  ( 1.000000000000000000, 0.000000000000000000, 0.000000000000000000 ) ) ;
#97341=DIRECTION ( 'NONE',  ( -0.000000000000000000, 1.000000000000000000, 0.000000000000000000 ) ) ;
#97345=VERTEX_POINT ( 'NONE', #95132 ) ;
#97351=CARTESIAN_POINT ( 'NONE',  ( -2.751797500100344518, -70.28872839323150856, 13.27139841227441686 ) ) ;
#97379=CIRCLE ( 'NONE', #18204, 1.999999999999999778 ) ;
#97386=DIRECTION ( 'NONE',  ( 0.000000000000000000, 5.412337245047638135E-13, 1.000000000000000000 ) ) ;
#97403=( LENGTH_UNIT ( ) NAMED_UNIT ( * ) SI_UNIT ( .MILLI., .METRE. ) );
#97415=ORIENTED_EDGE ( 'NONE', *, *, #92939, .T. ) ;
#97422=CARTESIAN_POINT ( 'NONE',  ( -4.188755055078491552, -1.571875576994959278, 102.8981131900555113 ) ) ;
#97430=VERTEX_POINT ( 'NONE', #2899 ) ;
#97457=CARTESIAN_POINT ( 'NONE',  ( 4.211261491273226909, -48.41319459705742645, 103.7733746176744347 ) ) ;
#97473=ORIENTED_EDGE ( 'NONE', *, *, #102694, .F. ) ;
#97484=CARTESIAN_POINT ( 'NONE',  ( -5.238409285680669214, -48.00301508172829301, 104.1169421774613824 ) ) ;
#97486=EDGE_CURVE ( 'NONE', #10296, #90150, #39429, .T. ) ;
#97518=SURFACE_STYLE_USAGE ( .BOTH. , #6929 ) ;
#97531=EDGE_LOOP ( 'NONE', ( #88303, #78111, #46910 ) ) ;
#97546=ADVANCED_FACE ( 'NONE', ( #72167 ), #82493, .F. ) ;
#97552=CARTESIAN_POINT ( 'NONE',  ( -5.988549711970257761, -14.40160760345779600, 14.13124080977631714 ) ) ;
#97584=ORIENTED_EDGE ( 'NONE', *, *, #25919, .F. ) ;
#97590=( BOUNDED_SURFACE ( )  B_SPLINE_SURFACE ( 3, 2, ( 
 ( #60354, #45225, #95891 ),
 ( #45740, #38722, #70555 ),
 ( #103961, #5289, #29593 ),
 ( #72134, #20986, #80214 ),
 ( #78101, #61948, #38210 ),
 ( #103442, #54327, #30643 ),
 ( #79691, #62463, #14405 ),
 ( #71590, #37152, #46798 ),
 ( #87271, #94841, #104496 ),
 ( #102915, #78618, #105043 ),
 ( #63531, #4219, #88333 ),
 ( #6319, #47318, #54872 ),
 ( #64069, #30105, #5800 ),
 ( #96429, #62994, #22564 ),
 ( #29083, #53306, #95354 ),
 ( #13348, #53819, #55402 ),
 ( #21491, #39258, #87801 ),
 ( #13881, #22016, #4751 ),
 ( #46276, #31184, #86751 ),
 ( #20464, #12297, #70017 ) ),
 .UNSPECIFIED., .F., .F., .F. ) 
 B_SPLINE_SURFACE_WITH_KNOTS ( ( 4, 2, 2, 2, 2, 2, 2, 2, 2, 4 ),
 ( 3, 3 ),
 ( 0.04523211244313660867, 0.04749178741066553688, 0.04975146237819445816, 0.05088129986195892573, 0.05201113734572338637, 0.05427081231325231458, 0.05653048728078123586, 0.05879016224831016407, 0.06104983721583909229, 0.06330951218336801356 ),
 ( 0.000000000000000000, 1.000000000000000000 ),
 .UNSPECIFIED. ) 
 GEOMETRIC_REPRESENTATION_ITEM ( )  RATIONAL_B_SPLINE_SURFACE ( (
 ( 1.000000000000000000, 0.4978119256231663958, 1.000000000000000000),
 ( 1.000000000000000000, 0.4952435806854573741, 1.000000000000000000),
 ( 1.000000000000000000, 0.4926028278389767978, 1.000000000000000000),
 ( 1.000000000000000000, 0.4880840605303077839, 1.000000000000000000),
 ( 1.000000000000000000, 0.4861908647209867707, 1.000000000000000000),
 ( 1.000000000000000000, 0.4843174878990902377, 1.000000000000000000),
 ( 1.000000000000000000, 0.4838530966740423600, 1.000000000000000000),
 ( 1.000000000000000000, 0.4832976052536793188, 1.000000000000000000),
 ( 1.000000000000000000, 0.4832078365194457104, 1.000000000000000000),
 ( 1.000000000000000000, 0.4835465747219757637, 1.000000000000000000),
 ( 1.000000000000000000, 0.4845818995314541966, 1.000000000000000000),
 ( 1.000000000000000000, 0.4880562902870073105, 1.000000000000000000),
 ( 1.000000000000000000, 0.4905018916449791488, 1.000000000000000000),
 ( 1.000000000000000000, 0.4962841545783361896, 1.000000000000000000),
 ( 1.000000000000000000, 0.4995601523126184107, 1.000000000000000000),
 ( 1.000000000000000000, 0.5062178729972902635, 1.000000000000000000),
 ( 1.000000000000000000, 0.5096177700154203016, 1.000000000000000000),
 ( 1.000000000000000000, 0.5157644467808917277, 1.000000000000000000),
 ( 1.000000000000000000, 0.5185252516010817603, 1.000000000000000000),
 ( 1.000000000000000000, 0.5207636911093219689, 1.000000000000000000) ) ) 
 REPRESENTATION_ITEM ( '' )  SURFACE ( )  );
#97606=AXIS2_PLACEMENT_3D ( 'NONE', #2454, #11606, #99553 ) ;
#97613=CARTESIAN_POINT ( 'NONE',  ( 9.960763185286923616, -50.12841120676987572, 26.07764662560745705 ) ) ;
#97617=CARTESIAN_POINT ( 'NONE',  ( -9.728280252476675827, -50.82205733719180785, 24.67413300948206967 ) ) ;
#97628=CARTESIAN_POINT ( 'NONE',  ( 4.551587301587293410, -48.79941684889506348, 104.4018401814738013 ) ) ;
#97662=ORIENTED_EDGE ( 'NONE', *, *, #20474, .F. ) ;
#97666=UNCERTAINTY_MEASURE_WITH_UNIT (LENGTH_MEASURE( 1.000000000000000082E-05 ), #85512, 'distance_accuracy_value', 'NONE');
#97709=FILL_AREA_STYLE_COLOUR ( '', #91537 ) ;
#97719=PRESENTATION_STYLE_ASSIGNMENT (( #58889 ) ) ;
#97737=CARTESIAN_POINT ( 'NONE',  ( -6.474893736874855144, -49.25205468179242274, 39.41360864784692097 ) ) ;
#97745=CARTESIAN_POINT ( 'NONE',  ( -3.352941176470589646, -48.79941684889505638, 104.5794940929807524 ) ) ;
#97758=CARTESIAN_POINT ( 'NONE',  ( 4.022544416453471605, -1.369395410676485625, 103.0357414394655962 ) ) ;
#97764=SURFACE_STYLE_USAGE ( .BOTH. , #16322 ) ;
#97772=ORIENTED_EDGE ( 'NONE', *, *, #86409, .F. ) ;
#97775=( LENGTH_UNIT ( ) NAMED_UNIT ( * ) SI_UNIT ( .MILLI., .METRE. ) );
#97805=B_SPLINE_CURVE_WITH_KNOTS ( 'NONE', 3,
 ( #18644, #92493, #51503, #9431, #42352, #2421, #18101, #35364, #75239, #1335, #101126, #34300, #8386, #41288, #67176, #21837, #28336, #21307 ),
 .UNSPECIFIED., .F., .F.,
 ( 4, 2, 2, 2, 2, 2, 2, 2, 4 ),
 ( 0.000000000000000000, 0.0008424128194421235966, 0.001684825638884247193, 0.003369651277768483978, 0.004212064097210603889, 0.005054476916652722931, 0.005475683326373779851, 0.005896889736094835903, 0.006739302555536954079 ),
 .UNSPECIFIED. ) ;
#97854=COLOUR_RGB ( '', 0.72549020, 0.75294118, 0.79215686) ;
#97889=CARTESIAN_POINT ( 'NONE',  ( -5.051174013757951720, -64.37264992930795415, 13.91140790810193018 ) ) ;
#97891=CARTESIAN_POINT ( 'NONE',  ( -5.385673916453011856, 0.000000000000000000, 18.57417562100670949 ) ) ;
#97893=ORIENTED_EDGE ( 'NONE', *, *, #70224, .T. ) ;
#97902=( NAMED_UNIT ( * ) PLANE_ANGLE_UNIT ( ) SI_UNIT ( $, .RADIAN. ) );
#97945=ORIENTED_EDGE ( 'NONE', *, *, #30299, .F. ) ;
#97947=CARTESIAN_POINT ( 'NONE',  ( 7.398498408818926286, -14.96086698649159530, 15.11142416646496578 ) ) ;
#97952=CARTESIAN_POINT ( 'NONE',  ( 5.000000000000000000, -60.71953810597847223, 12.61250543006446989 ) ) ;
#97955=MECHANICAL_DESIGN_GEOMETRIC_PRESENTATION_REPRESENTATION('',(#37730),#18781);
#97980=CARTESIAN_POINT ( 'NONE',  ( 6.923875968564608741, -12.36264606019372714, 8.501481527785209380 ) ) ;
#97996=CARTESIAN_POINT ( 'NONE',  ( 5.983613182656019269, -12.98062839397017143, 13.15810238988798275 ) ) ;
#98001=CARTESIAN_POINT ( 'NONE',  ( 5.164787682159408533, -48.11244280217346869, 104.1470044518087121 ) ) ;
#98002=ORIENTED_EDGE ( 'NONE', *, *, #5398, .T. ) ;
#98010=ORIENTED_EDGE ( 'NONE', *, *, #92939, .F. ) ;
#98031=CARTESIAN_POINT ( 'NONE',  ( -4.869065774733876140, -47.04879514974081189, 102.3543991519893979 ) ) ;
#98034=ORIENTED_EDGE ( 'NONE', *, *, #1640, .T. ) ;
#98035=CARTESIAN_POINT ( 'NONE',  ( 0.9999999999999940048, -50.00000000000000000, 101.0455488498966758 ) ) ;
#98083=DIRECTION ( 'NONE',  ( 1.000000000000000000, 0.000000000000000000, 0.000000000000000000 ) ) ;
#98084=DIRECTION ( 'NONE',  ( -0.1108331996454381269, -0.9715652913456128692, -0.2092292678113389093 ) ) ;
#98091=CARTESIAN_POINT ( 'NONE',  ( 4.284822031654949015, -48.90716638558772900, 104.4267991316944943 ) ) ;
#98097=CARTESIAN_POINT ( 'NONE',  ( -6.073384266107519913, -15.26795065999669276, 14.38582946078376779 ) ) ;
#98151=ORIENTED_EDGE ( 'NONE', *, *, #24278, .T. ) ;
#98159=CARTESIAN_POINT ( 'NONE',  ( -9.269408785705698151, -52.95403500424551169, 23.24750950774772562 ) ) ;
#98179=FILL_AREA_STYLE ('',( #31877 ) ) ;
#98182=( GEOMETRIC_REPRESENTATION_CONTEXT ( 3 ) GLOBAL_UNCERTAINTY_ASSIGNED_CONTEXT ( ( #90485 ) ) GLOBAL_UNIT_ASSIGNED_CONTEXT ( ( #54746, #103326, #80616 ) ) REPRESENTATION_CONTEXT ( 'NONE', 'WORKASPACE' ) );
#98200=ORIENTED_EDGE ( 'NONE', *, *, #91986, .T. ) ;
#98244=EDGE_CURVE ( 'NONE', #87879, #92559, #98950, .T. ) ;
#98252=CARTESIAN_POINT ( 'NONE',  ( 9.204611235795193025, -55.29781778581994445, 30.90985867601607850 ) ) ;
#98258=CARTESIAN_POINT ( 'NONE',  ( 1.000000000000000000, -15.67194501421539599, -10.31047629133078480 ) ) ;
#98260=PRESENTATION_STYLE_ASSIGNMENT (( #24930 ) ) ;
#98264=B_SPLINE_CURVE_WITH_KNOTS ( 'NONE', 3,
 ( #70498, #87214, #38666, #71533, #20407, #21962 ),
 .UNSPECIFIED., .F., .F.,
 ( 4, 2, 4 ),
 ( 0.000000000000000000, 0.0003910247833730985559, 0.0007820495667461968949 ),
 .UNSPECIFIED. ) ;
#98337=DIRECTION ( 'NONE',  ( 0.000000000000000000, 0.000000000000000000, 1.000000000000000000 ) ) ;
#98360=CARTESIAN_POINT ( 'NONE',  ( 4.999999999999995559, -50.00000000000000000, 40.07669683062201926 ) ) ;
#98364=DIRECTION ( 'NONE',  ( 0.000000000000000000, 0.9371777605526924182, 0.3488521823429523994 ) ) ;
#98379=DIRECTION ( 'NONE',  ( 0.000000000000000000, 0.000000000000000000, 1.000000000000000000 ) ) ;
#98396=FACE_OUTER_BOUND ( 'NONE', #5576, .T. ) ;
#98420=CARTESIAN_POINT ( 'NONE',  ( -4.473249400556560396, -67.33440330485672121, 13.71903601027506348 ) ) ;
#98421=CARTESIAN_POINT ( 'NONE',  ( 2.678351059745897711, -49.64194654076311508, 103.0656783881315874 ) ) ;
#98433=CARTESIAN_POINT ( 'NONE',  ( 4.999999999999995559, -46.27021379719273142, 42.58845726913239105 ) ) ;
#98474=CARTESIAN_POINT ( 'NONE',  ( 1.843375668371956433, -70.60499474404922182, 13.11394492857258065 ) ) ;
#98481=CARTESIAN_POINT ( 'NONE',  ( 4.970849588242775674, -46.55209929711413253, 102.2755693391596168 ) ) ;
#98489=CARTESIAN_POINT ( 'NONE',  ( 5.802268690544502228, -3.456390741716395265, 103.8899761878886636 ) ) ;
#98503=CARTESIAN_POINT ( 'NONE',  ( 5.000000000000157208, -12.42851940633512520, 8.537252933897461205 ) ) ;
#98511=ADVANCED_FACE ( 'NONE', ( #55053 ), #23156, .T. ) ;
#98524=CARTESIAN_POINT ( 'NONE',  ( 10.17470798438142410, -0.7156995453649822592, 20.10980123007764675 ) ) ;
#98539=CARTESIAN_POINT ( 'NONE',  ( -3.653369855178271397, -8.635023481229975317, -12.30779604435681129 ) ) ;
#98550=STYLED_ITEM ( 'NONE', ( #8101 ), #82998 ) ;
#98573=CARTESIAN_POINT ( 'NONE',  ( 8.999999999999996447, -80.00000000000000000, 42.58845726811989607 ) ) ;
#98597=FACE_OUTER_BOUND ( 'NONE', #44037, .T. ) ;
#98604=CARTESIAN_POINT ( 'NONE',  ( -9.000000000000001776, -80.00000000000000000, 42.58845726811989607 ) ) ;
#98609=ORIENTED_EDGE ( 'NONE', *, *, #59334, .T. ) ;
#98621=CARTESIAN_POINT ( 'NONE',  ( -6.459500862575596969, -11.87485980093857485, 10.39038571060303262 ) ) ;
#98626=FACE_OUTER_BOUND ( 'NONE', #22634, .T. ) ;
#98640=CARTESIAN_POINT ( 'NONE',  ( 9.346890874034901486, -3.133782013405083777, 14.76170641224502589 ) ) ;
#98653=MECHANICAL_DESIGN_GEOMETRIC_PRESENTATION_REPRESENTATION('',(#79728),#5666);
#98668=SURFACE_STYLE_USAGE ( .BOTH. , #91148 ) ;
#98675=CARTESIAN_POINT ( 'NONE',  ( 9.934750400155193617, -50.13194482833283416, 28.16945530398552222 ) ) ;
#98698=EDGE_CURVE ( 'NONE', #25211, #3119, #76631, .T. ) ;
#98736=ORIENTED_EDGE ( 'NONE', *, *, #37988, .F. ) ;
#98757=ORIENTED_EDGE ( 'NONE', *, *, #3471, .T. ) ;
#98767=AXIS2_PLACEMENT_3D ( 'NONE', #53789, #12788, #45705 ) ;
#98769=CARTESIAN_POINT ( 'NONE',  ( 9.668268460383899310, -57.17502809900269511, 29.56382476086920974 ) ) ;
#98782=CARTESIAN_POINT ( 'NONE',  ( -3.677502082062658051, -48.98465343287618623, 104.5296620117538424 ) ) ;
#98798=CARTESIAN_POINT ( 'NONE',  ( -7.000000000000002665, -46.47749919162729526, 39.12435565298215323 ) ) ;
#98804=EDGE_CURVE ( 'NONE', #56644, #52640, #43926, .T. ) ;
#98816=ADVANCED_FACE ( 'NONE', ( #84662 ), #2661, .T. ) ;
#98841=( GEOMETRIC_REPRESENTATION_CONTEXT ( 3 ) GLOBAL_UNCERTAINTY_ASSIGNED_CONTEXT ( ( #26150 ) ) GLOBAL_UNIT_ASSIGNED_CONTEXT ( ( #82847, #40789, #1915 ) ) REPRESENTATION_CONTEXT ( 'NONE', 'WORKASPACE' ) );
#98857=DIRECTION ( 'NONE',  ( -1.000000000000000000, 0.000000000000000000, 0.000000000000000000 ) ) ;
#98870=CARTESIAN_POINT ( 'NONE',  ( -5.939725004866447833, -11.78992312938697218, -9.289959103330964751 ) ) ;
#98877=EDGE_CURVE ( 'NONE', #34973, #25863, #90423, .T. ) ;
#98921=CARTESIAN_POINT ( 'NONE',  ( -15.66596225472208914, -1.206787384264950580, 14.95386751741624920 ) ) ;
#98927=EDGE_LOOP ( 'NONE', ( #65177, #46792, #29506, #50692, #3019, #4094 ) ) ;
#98934=CARTESIAN_POINT ( 'NONE',  ( -3.195909155964999027, -68.75976616688309662, 13.04431807157711454 ) ) ;
#98942=CARTESIAN_POINT ( 'NONE',  ( 3.866514940527741029, -48.81811806873775339, 103.9726926151936652 ) ) ;
#98948=( NAMED_UNIT ( * ) SI_UNIT ( $, .STERADIAN. ) SOLID_ANGLE_UNIT ( ) );
#98950=CIRCLE ( 'NONE', #12799, 4.000000000000003553 ) ;
#98958=DIRECTION ( 'NONE',  ( 1.000000000000000000, 0.000000000000000000, 0.000000000000000000 ) ) ;
#98995=CARTESIAN_POINT ( 'NONE',  ( 4.856083419063446094, -65.85369684545175062, 13.84668161063944503 ) ) ;
#99000=CARTESIAN_POINT ( 'NONE',  ( 4.022544416453469829, -48.63060458932351793, 103.0357414394656104 ) ) ;
#99013=ORIENTED_EDGE ( 'NONE', *, *, #57481, .T. ) ;
#99025=CARTESIAN_POINT ( 'NONE',  ( 6.081241251370853362, -12.38970427209928005, 12.35256966254937971 ) ) ;
#99036=VERTEX_POINT ( 'NONE', #35891 ) ;
#99044=CARTESIAN_POINT ( 'NONE',  ( 5.803898591548438901, -46.53140123172246945, 103.8893302396402589 ) ) ;
#99063=FACE_BOUND ( 'NONE', #4305, .T. ) ;
#99084=( NAMED_UNIT ( * ) SI_UNIT ( $, .STERADIAN. ) SOLID_ANGLE_UNIT ( ) );
#99086=UNCERTAINTY_MEASURE_WITH_UNIT (LENGTH_MEASURE( 1.000000000000000082E-05 ), #9638, 'distance_accuracy_value', 'NONE');
#99133=( GEOMETRIC_REPRESENTATION_CONTEXT ( 3 ) GLOBAL_UNCERTAINTY_ASSIGNED_CONTEXT ( ( #89517 ) ) GLOBAL_UNIT_ASSIGNED_CONTEXT ( ( #714, #41216, #58474 ) ) REPRESENTATION_CONTEXT ( 'NONE', 'WORKASPACE' ) );
#99137=CIRCLE ( 'NONE', #71582, 17.00000000000000000 ) ;
#99170=CARTESIAN_POINT ( 'NONE',  ( 11.48053704661521479, -1.561145388285825275, 20.53821296167100030 ) ) ;
#99179=SURFACE_STYLE_FILL_AREA ( #9110 ) ;
#99198=CARTESIAN_POINT ( 'NONE',  ( 3.510631567122396657, -68.36704268726951739, 13.08651599561504497 ) ) ;
#99221=CARTESIAN_POINT ( 'NONE',  ( 4.401189997858475422, -13.27310044850791471, -9.172641694124337164 ) ) ;
#99229=CARTESIAN_POINT ( 'NONE',  ( -8.022151257807545122, -0.1402635695912273495, 19.37061829778098954 ) ) ;
#99262=ORIENTED_EDGE ( 'NONE', *, *, #16592, .F. ) ;
#99277=CARTESIAN_POINT ( 'NONE',  ( -5.000000000000000000, -13.80280838537006538, 10.52502860397554230 ) ) ;
#99297=CARTESIAN_POINT ( 'NONE',  ( 9.901632022247257581, -57.79079078909488487, 28.42038564161779135 ) ) ;
#99303=CARTESIAN_POINT ( 'NONE',  ( 5.000000000000000888, -4.607437535715905419, -14.28092741399824384 ) ) ;
#99310=CARTESIAN_POINT ( 'NONE',  ( -2.807206530941451561, -49.57822929777214682, 102.9378052260345839 ) ) ;
#99398=CARTESIAN_POINT ( 'NONE',  ( -5.000000000000000000, -15.93202192939577344, -5.930487099830192399 ) ) ;
#99418=EDGE_CURVE ( 'NONE', #550, #27751, #42296, .T. ) ;
#99420=ORIENTED_EDGE ( 'NONE', *, *, #93623, .T. ) ;
#99427=CARTESIAN_POINT ( 'NONE',  ( 2.691749510577694515, -0.5367988052720203962, 103.4277152940129412 ) ) ;
#99429=CARTESIAN_POINT ( 'NONE',  ( -9.000000000000001776, -46.00000000000000000, 42.58845726811989607 ) ) ;
#99437=SURFACE_STYLE_USAGE ( .BOTH. , #25614 ) ;
#99451=FACE_OUTER_BOUND ( 'NONE', #75412, .T. ) ;
#99500=DIRECTION ( 'NONE',  ( 1.000000000000000000, 0.000000000000000000, 0.000000000000000000 ) ) ;
#99502=STYLED_ITEM ( 'NONE', ( #92880 ), #67844 ) ;
#99507=SURFACE_STYLE_FILL_AREA ( #25682 ) ;
#99530=CARTESIAN_POINT ( 'NONE',  ( 9.283973715592685139, -13.34910468049023535, 16.51841009919174397 ) ) ;
#99535=CARTESIAN_POINT ( 'NONE',  ( 4.814131498176642765, -64.23532120076806962, 13.02162479025466624 ) ) ;
#99536=ORIENTED_EDGE ( 'NONE', *, *, #59589, .F. ) ;
#99553=DIRECTION ( 'NONE',  ( 0.000000000000000000, -6.071532165918824830E-15, 1.000000000000000000 ) ) ;
#99556=ORIENTED_EDGE ( 'NONE', *, *, #71019, .T. ) ;
#99579=CARTESIAN_POINT ( 'NONE',  ( 6.224163897435908588, -12.02839407259639337, 11.51386142893530362 ) ) ;
#99586=FILL_AREA_STYLE ('',( #2485 ) ) ;
#99623=EDGE_CURVE ( 'NONE', #10104, #42316, #3093, .T. ) ;
#99714=EDGE_CURVE ( 'NONE', #51662, #45005, #28631, .T. ) ;
#99718=CARTESIAN_POINT ( 'NONE',  ( 9.805789921995232916, -0.5587250708512973008, 19.98157798524368189 ) ) ;
#99731=VERTEX_POINT ( 'NONE', #106141 ) ;
#99747=FILL_AREA_STYLE ('',( #65791 ) ) ;
#99755=DIRECTION ( 'NONE',  ( 0.000000000000000000, 0.000000000000000000, -1.000000000000000000 ) ) ;
#99768=CARTESIAN_POINT ( 'NONE',  ( 3.912407852882054726, -11.95585042648033003, -10.32340492114883546 ) ) ;
#99800=PRESENTATION_STYLE_ASSIGNMENT (( #66368 ) ) ;
#99818=EDGE_CURVE ( 'NONE', #39260, #103713, #23682, .T. ) ;
#99826=CARTESIAN_POINT ( 'NONE',  ( -5.000000000000000000, -13.85485428919850648, 10.16324337853805204 ) ) ;
#99840=DIRECTION ( 'NONE',  ( 0.000000000000000000, 1.000000000000000000, 0.000000000000000000 ) ) ;
#99858=CARTESIAN_POINT ( 'NONE',  ( -1.257803174857021755, -49.99999999975079845, 101.3280723981089722 ) ) ;
#99884=CIRCLE ( 'NONE', #6872, 11.00000000000000000 ) ;
#99886=DIRECTION ( 'NONE',  ( 0.000000000000000000, 0.000000000000000000, 1.000000000000000000 ) ) ;
#99895=CIRCLE ( 'NONE', #22407, 1.999999999999999778 ) ;
#99902=SURFACE_STYLE_FILL_AREA ( #10875 ) ;
#99907=CARTESIAN_POINT ( 'NONE',  ( 0.000000000000000000, -4.000000000000003553, 37.00000000000000000 ) ) ;
#99946=CARTESIAN_POINT ( 'NONE',  ( 1.000000000000000000, -48.56827653475308182, 2.661071982229600064 ) ) ;
#99949=CARTESIAN_POINT ( 'NONE',  ( -5.175128423392746591, -10.69566144610010028, -10.53077195007410793 ) ) ;
#99951=CARTESIAN_POINT ( 'NONE',  ( -9.317330270139585480, -11.89270385133543506, 9.146501922081970548 ) ) ;
#99952=CARTESIAN_POINT ( 'NONE',  ( -6.677362058809294787, -11.98847278904867508, 9.465251842568026319 ) ) ;
#99977=ADVANCED_FACE ( 'NONE', ( #73021 ), #80065, .F. ) ;
#100074=CARTESIAN_POINT ( 'NONE',  ( 2.367671974756863751, -69.88010167377507287, 13.19913436203879620 ) ) ;
#100088=PRESENTATION_STYLE_ASSIGNMENT (( #291 ) ) ;
#100104=CARTESIAN_POINT ( 'NONE',  ( 5.000000000000000000, -14.65803281199247898, 12.34559804589062537 ) ) ;
#100185=COLOUR_RGB ( '', 0.40784314, 0.44705882, 0.49803922) ;
#100187=DIRECTION ( 'NONE',  ( 0.000000000000000000, 0.000000000000000000, 1.000000000000000000 ) ) ;
#100218=CARTESIAN_POINT ( 'NONE',  ( -3.508895115992890723, -1.149532983824396615, 104.5950737443410645 ) ) ;
#100244=CARTESIAN_POINT ( 'NONE',  ( 10.15437730543717976, -0.6969019443260592306, 20.10336840207808251 ) ) ;
#100251=EDGE_CURVE ( 'NONE', #18508, #21120, #32617, .T. ) ;
#100257=CARTESIAN_POINT ( 'NONE',  ( 27.99999999999999645, 0.000000000000000000, 0.000000000000000000 ) ) ;
#100259=ORIENTED_EDGE ( 'NONE', *, *, #89921, .F. ) ;
#100295=SURFACE_STYLE_FILL_AREA ( #100819 ) ;
#100314=LINE ( 'NONE', #59349, #58662 ) ;
#100340=SURFACE_STYLE_USAGE ( .BOTH. , #76060 ) ;
#100350=COLOUR_RGB ( '', 0.08235294, 0.09019608, 0.10196078) ;
#100375=CARTESIAN_POINT ( 'NONE',  ( -2.714483990415212045, -0.3795274241210661037, 102.8323277908853868 ) ) ;
#100384=CARTESIAN_POINT ( 'NONE',  ( 6.903355605563677777, -12.56553646782259293, 8.191904130043296206 ) ) ;
#100412=CARTESIAN_POINT ( 'NONE',  ( 2.230802491789472874, -49.81451076291526192, 102.4842558203777827 ) ) ;
#100416=( NAMED_UNIT ( * ) SI_UNIT ( $, .STERADIAN. ) SOLID_ANGLE_UNIT ( ) );
#100422=CARTESIAN_POINT ( 'NONE',  ( 0.000000000000000000, -1.550510257216834331, 112.0000000000000000 ) ) ;
#100455=LINE ( 'NONE', #2273, #94341 ) ;
#100476=CARTESIAN_POINT ( 'NONE',  ( 3.396360046676592859, -0.8468429378662341023, 103.9790200242207021 ) ) ;
#100494=CARTESIAN_POINT ( 'NONE',  ( 15.80778651423128700, -3.783390974281282571, 14.51852905608714828 ) ) ;
#100498=SURFACE_STYLE_FILL_AREA ( #1792 ) ;
#100511=ORIENTED_EDGE ( 'NONE', *, *, #6161, .F. ) ;
#100543=CARTESIAN_POINT ( 'NONE',  ( 0.000000000000000000, -50.00000000000000000, 119.0000000000000142 ) ) ;
#100558=CARTESIAN_POINT ( 'NONE',  ( 3.905812579222632586, -52.93498169485550164, 40.44872036466767895 ) ) ;
#100607=CARTESIAN_POINT ( 'NONE',  ( 5.413543642048970206, -66.62195522163649741, 14.08876852576774041 ) ) ;
#100636=CARTESIAN_POINT ( 'NONE',  ( 5.000000000000000000, -13.87446176118116448, 11.25142367426022538 ) ) ;
#100650=CARTESIAN_POINT ( 'NONE',  ( -13.87298779988979724, -57.59168965358072256, 28.89736879381397827 ) ) ;
#100690=DIRECTION ( 'NONE',  ( 0.000000000000000000, 0.000000000000000000, -1.000000000000000000 ) ) ;
#100706=MECHANICAL_DESIGN_GEOMETRIC_PRESENTATION_REPRESENTATION('',(#85236),#7694);
#100713=CARTESIAN_POINT ( 'NONE',  ( -9.000000000000001776, 0.000000000000000000, 42.58845726811989607 ) ) ;
#100718=CARTESIAN_POINT ( 'NONE',  ( 2.622924477838863844, -53.64565257674880172, 40.75381538023534489 ) ) ;
#100738=DIRECTION ( 'NONE',  ( 1.000000000000000000, 0.000000000000000000, 0.000000000000000000 ) ) ;
#100754=DIRECTION ( 'NONE',  ( 0.000000000000000000, 1.000000000000000000, 0.000000000000000000 ) ) ;
#100773=CARTESIAN_POINT ( 'NONE',  ( 14.45183933456885761, 0.5067537316480897891, 14.99274988531763775 ) ) ;
#100779=DIRECTION ( 'NONE',  ( 0.000000000000000000, -1.000000000000000000, 0.000000000000000000 ) ) ;
#100800=CARTESIAN_POINT ( 'NONE',  ( 3.216749358082111598, -8.903395928605879917, -12.12543985758794918 ) ) ;
#100819=FILL_AREA_STYLE ('',( #93810 ) ) ;
#100850=PRODUCT_DEFINITION_SHAPE ( 'NONE', 'NONE',  #15959 ) ;
#100860=CARTESIAN_POINT ( 'NONE',  ( -1.000000000001115108, -15.98025244997938721, -10.26003014047063822 ) ) ;
#100901=CARTESIAN_POINT ( 'NONE',  ( -3.352941176470593199, -1.200583151104949176, 104.5794940929807382 ) ) ;
#100907=DIRECTION ( 'NONE',  ( 0.000000000000000000, 0.000000000000000000, 1.000000000000000000 ) ) ;
#100909=CARTESIAN_POINT ( 'NONE',  ( 4.149711973588559033, -8.980130494280730957, 13.48951460889846921 ) ) ;
#100968=CARTESIAN_POINT ( 'NONE',  ( 6.457467314873006181, -2.602085213965210642E-15, 18.85860952240310340 ) ) ;
#100986=ADVANCED_FACE ( 'NONE', ( #51692 ), #97590, .F. ) ;
#100988=ADVANCED_FACE ( 'NONE', ( #86225 ), #15691, .F. ) ;
#100998=VECTOR ( 'NONE', #47736, 1000.000000000000000 ) ;
#101016=CARTESIAN_POINT ( 'NONE',  ( -15.37676141849992639, -5.579222135594369192, 13.92723728277131556 ) ) ;
#101017=CARTESIAN_POINT ( 'NONE',  ( -6.073849149975423245, -15.27114203292415873, 14.38605564242085499 ) ) ;
#101018=CARTESIAN_POINT ( 'NONE',  ( 3.351415132801500718, -0.9950411258689764171, 104.3291499688503450 ) ) ;
#101033=CIRCLE ( 'NONE', #16583, 15.00000000000000000 ) ;
#101049=CARTESIAN_POINT ( 'NONE',  ( 4.844458925423827722, -2.858988884354966675, 103.3760426044467380 ) ) ;
#101050=CARTESIAN_POINT ( 'NONE',  ( -3.718188220750955786, -48.95098499554293170, 104.2423402216923591 ) ) ;
#101059=DIRECTION ( 'NONE',  ( -1.000000000000000000, 0.000000000000000000, 0.000000000000000000 ) ) ;
#101061=FILL_AREA_STYLE_COLOUR ( '', #34858 ) ;
#101089=VERTEX_POINT ( 'NONE', #34903 ) ;
#101096=ADVANCED_FACE ( 'NONE', ( #27893 ), #35434, .T. ) ;
#101099=CARTESIAN_POINT ( 'NONE',  ( 4.328822244912061912, -48.31633875694424063, 40.50747960775626666 ) ) ;
#101126=CARTESIAN_POINT ( 'NONE',  ( 2.819467257040595420, -49.57152905888915484, 44.39875113217646430 ) ) ;
#101133=DIRECTION ( 'NONE',  ( 1.000000000000000000, 0.000000000000000000, 0.000000000000000000 ) ) ;
#101138=TOROIDAL_SURFACE ( 'NONE', #102916, 8.499999999999992895, 0.5000000000000000000 ) ;
#101195=CARTESIAN_POINT ( 'NONE',  ( -13.95266368664216294, -57.79432512081118034, 25.82453759514263680 ) ) ;
#101200=DIRECTION ( 'NONE',  ( 0.000000000000000000, 0.000000000000000000, 1.000000000000000000 ) ) ;
#101220=STYLED_ITEM ( 'NONE', ( #10820 ), #1568 ) ;
#101221=ORIENTED_EDGE ( 'NONE', *, *, #99418, .T. ) ;
#101256=ORIENTED_EDGE ( 'NONE', *, *, #39246, .F. ) ;
#101265=LINE ( 'NONE', #1470, #41680 ) ;
#101277=ORIENTED_EDGE ( 'NONE', *, *, #20474, .T. ) ;
#101322=STYLED_ITEM ( 'NONE', ( #65942 ), #39165 ) ;
#101329=CARTESIAN_POINT ( 'NONE',  ( -1.221766272017100308, -5.532494385104715917, -13.95387042840530256 ) ) ;
#101343=TOROIDAL_SURFACE ( 'NONE', #6630, 11.00000000000000000, 2.000000000000000000 ) ;
#101361=CIRCLE ( 'NONE', #68651, 9.999999999999998224 ) ;
#101397=FILL_AREA_STYLE ('',( #54818 ) ) ;
#101449=ORIENTED_EDGE ( 'NONE', *, *, #18511, .F. ) ;
#101452=CARTESIAN_POINT ( 'NONE',  ( -1.560777554885082852, -0.03795747330964680671, 101.5963436445145476 ) ) ;
#101484=CARTESIAN_POINT ( 'NONE',  ( 2.122576366385977575, -49.78385856110771357, 102.5552564100475763 ) ) ;
#101547=ORIENTED_EDGE ( 'NONE', *, *, #57222, .F. ) ;
#101550=CARTESIAN_POINT ( 'NONE',  ( 1.000000000000000222, -40.48763664057447187, -0.7135409870748585792 ) ) ;
#101556=CARTESIAN_POINT ( 'NONE',  ( -5.964242399901850789, -13.95070288504640743, 13.91433285878926007 ) ) ;
#101590=PRESENTATION_STYLE_ASSIGNMENT (( #85959 ) ) ;
#101599=( NAMED_UNIT ( * ) PLANE_ANGLE_UNIT ( ) SI_UNIT ( $, .RADIAN. ) );
#101604=CARTESIAN_POINT ( 'NONE',  ( 0.000000000000000000, -48.44948974278317877, 112.0000000000000000 ) ) ;
#101636=CARTESIAN_POINT ( 'NONE',  ( 1.192997108011318863, -53.99999999871816669, 40.95527494392581502 ) ) ;
#101656=CARTESIAN_POINT ( 'NONE',  ( -3.000704772616793026, -49.56994904094584342, 40.82253472268489958 ) ) ;
#101709=CARTESIAN_POINT ( 'NONE',  ( 6.697918543062176155, -13.04454418786335701, -7.429595805581659107 ) ) ;
#101717=UNCERTAINTY_MEASURE_WITH_UNIT (LENGTH_MEASURE( 1.000000000000000082E-05 ), #35068, 'distance_accuracy_value', 'NONE');
#101719=CARTESIAN_POINT ( 'NONE',  ( -4.551587301587297851, -48.79941684889506348, 104.4018401814738013 ) ) ;
#101720=CARTESIAN_POINT ( 'NONE',  ( -13.59360248487383771, -56.00807882655470138, 23.64795065864135637 ) ) ;
#101749=DIRECTION ( 'NONE',  ( -0.6505632072693953161, 0.6639782930160468277, 0.3686466326319209341 ) ) ;
#101764=FACE_OUTER_BOUND ( 'NONE', #82765, .T. ) ;
#101778=CARTESIAN_POINT ( 'NONE',  ( 5.000000000000000000, -14.29896967480689440, 12.05578540490725103 ) ) ;
#101787=CARTESIAN_POINT ( 'NONE',  ( 0.7777777777777741264, -54.00000000000000711, 40.97837836547555668 ) ) ;
#101805=CARTESIAN_POINT ( 'NONE',  ( 30.00000000000000000, 0.000000000000000000, 0.000000000000000000 ) ) ;
#101848=CARTESIAN_POINT ( 'NONE',  ( -3.912401218062240282, -11.95583337082086572, -10.32341866952809006 ) ) ;
#101871=CARTESIAN_POINT ( 'NONE',  ( 1.574031687329273232, -6.039084736203306214, -13.77476369213296259 ) ) ;
#101905=CARTESIAN_POINT ( 'NONE',  ( 2.230802491789480424, -0.1854892370859804462, 102.4842558203776974 ) ) ;
#101918=( NAMED_UNIT ( * ) PLANE_ANGLE_UNIT ( ) SI_UNIT ( $, .RADIAN. ) );
#101924=CARTESIAN_POINT ( 'NONE',  ( 1.000000000000000444, -5.000000000000000000, -14.14213562373095101 ) ) ;
#101935=CARTESIAN_POINT ( 'NONE',  ( -3.867083106916794133, -48.81750179905139220, 103.9715359882822270 ) ) ;
#101939=VERTEX_POINT ( 'NONE', #53338 ) ;
#101953=CARTESIAN_POINT ( 'NONE',  ( -13.72589306172073442, -50.98891492079946630, 29.76321791924474525 ) ) ;
#101969=CARTESIAN_POINT ( 'NONE',  ( -3.352941176470596307, -1.200583151104958279, 104.5794940929807524 ) ) ;
#101978=DIRECTION ( 'NONE',  ( 0.000000000000000000, 1.000000000000000000, 0.000000000000000000 ) ) ;
#101979=UNCERTAINTY_MEASURE_WITH_UNIT (LENGTH_MEASURE( 1.000000000000000082E-05 ), #13568, 'distance_accuracy_value', 'NONE');
#102004=CARTESIAN_POINT ( 'NONE',  ( 0.9999999999999940048, -50.00000000000000000, 101.0455488498966758 ) ) ;
#102028=CARTESIAN_POINT ( 'NONE',  ( 7.386188840451400672, -0.04421783097938639107, 19.15859931866217636 ) ) ;
#102045=COLOUR_RGB ( '', 0.40784314, 0.44705882, 0.49803922) ;
#102053=AXIS2_PLACEMENT_3D ( 'NONE', #26678, #36379, #3964 ) ;
#102074=CARTESIAN_POINT ( 'NONE',  ( -5.960000261375883568, -13.79916237020877112, 13.82526581198430016 ) ) ;
#102086=CARTESIAN_POINT ( 'NONE',  ( 13.90377727273328645, -57.59477087426256503, 25.34355585267129740 ) ) ;
#102108=CARTESIAN_POINT ( 'NONE',  ( 4.051286199644066777, -1.398729870307594547, 103.8758286790405094 ) ) ;
#102136=ORIENTED_EDGE ( 'NONE', *, *, #41694, .F. ) ;
#102137=CARTESIAN_POINT ( 'NONE',  ( -9.822490609848976817, -57.47042247602874454, 25.11095637839896000 ) ) ;
#102142=TOROIDAL_SURFACE ( 'NONE', #36670, 11.00000000000000000, 2.000000000000000000 ) ;
#102146=ORIENTED_EDGE ( 'NONE', *, *, #36786, .T. ) ;
#102158=CARTESIAN_POINT ( 'NONE',  ( 4.408087643829541769, -52.50239862025969018, 40.28907920670494036 ) ) ;
#102178=CARTESIAN_POINT ( 'NONE',  ( -3.478182438133638588, -49.25293460592492067, 40.73187655623500092 ) ) ;
#102247=UNCERTAINTY_MEASURE_WITH_UNIT (LENGTH_MEASURE( 1.000000000000000082E-05 ), #54432, 'distance_accuracy_value', 'NONE');
#102251=CARTESIAN_POINT ( 'NONE',  ( -13.38090213880806978, -54.00000000000000711, 31.11721482942554928 ) ) ;
#102255=CARTESIAN_POINT ( 'NONE',  ( 11.84572884306312979, -1.963608633182635232, 20.63449361704874718 ) ) ;
#102278=ORIENTED_EDGE ( 'NONE', *, *, #42584, .T. ) ;
#102296=CARTESIAN_POINT ( 'NONE',  ( -4.781335833249819700, -2.669875467129551261, 102.4226025779373401 ) ) ;
#102297=CARTESIAN_POINT ( 'NONE',  ( 0.000000000000000000, -46.00000000000000000, 112.0000000000000000 ) ) ;
#102311=FACE_OUTER_BOUND ( 'NONE', #48741, .T. ) ;
#102319=CARTESIAN_POINT ( 'NONE',  ( 5.163300830990278811, -51.69768845676519931, 40.01618609069083732 ) ) ;
#102323=FACE_OUTER_BOUND ( 'NONE', #25077, .T. ) ;
#102324=AXIS2_PLACEMENT_3D ( 'NONE', #58832, #51776, #76052 ) ;
#102345=SURFACE_STYLE_USAGE ( .BOTH. , #29048 ) ;
#102381=SURFACE_SIDE_STYLE ('',( #28533 ) ) ;
#102407=CARTESIAN_POINT ( 'NONE',  ( 4.837657582856586203, -12.04835165414415066, -8.962574246966335423 ) ) ;
#102409=( GEOMETRIC_REPRESENTATION_CONTEXT ( 3 ) GLOBAL_UNCERTAINTY_ASSIGNED_CONTEXT ( ( #40865 ) ) GLOBAL_UNIT_ASSIGNED_CONTEXT ( ( #88312, #72638, #30623 ) ) REPRESENTATION_CONTEXT ( 'NONE', 'WORKASPACE' ) );
#102422=DIRECTION ( 'NONE',  ( -0.6505632072693978696, 0.6639782930160472718, -0.3686466326319159381 ) ) ;
#102458=CARTESIAN_POINT ( 'NONE',  ( -9.922755624444706157, -3.234633340497464982, 15.16391852634635562 ) ) ;
#102479=CARTESIAN_POINT ( 'NONE',  ( -3.801077171203065319, -48.88909605940821734, 104.1059035333590828 ) ) ;
#102485=VECTOR ( 'NONE', #47321, 1000.000000000000000 ) ;
#102492=CARTESIAN_POINT ( 'NONE',  ( -5.000000000000000000, -12.54465221550630183, 8.223849511754982800 ) ) ;
#102499=CARTESIAN_POINT ( 'NONE',  ( -13.99657022045423282, -50.02530620882281198, 26.59685899168112400 ) ) ;
#102507=ORIENTED_EDGE ( 'NONE', *, *, #47375, .F. ) ;
#102574=CARTESIAN_POINT ( 'NONE',  ( 10.29956429353439873, 2.626117177127659463, 14.76850153968369916 ) ) ;
#102577=CARTESIAN_POINT ( 'NONE',  ( -5.000000000000000888, -4.607398061199006634, -14.28094137034753608 ) ) ;
#102579=CARTESIAN_POINT ( 'NONE',  ( 30.00000000000000000, 0.000000000000000000, 0.000000000000000000 ) ) ;
#102611=CARTESIAN_POINT ( 'NONE',  ( 7.000000000000000000, -14.05766640829038039, -5.232782735144291486 ) ) ;
#102676=CARTESIAN_POINT ( 'NONE',  ( -9.864331116128868260, -57.59319873990106231, 25.34043079474438898 ) ) ;
#102694=EDGE_CURVE ( 'NONE', #40108, #66555, #94042, .T. ) ;
#102695=CARTESIAN_POINT ( 'NONE',  ( 2.751717838649724079, -49.70119617224028730, 40.86150536811170753 ) ) ;
#102706=CIRCLE ( 'NONE', #25205, 2.000000000000001776 ) ;
#102715=CARTESIAN_POINT ( 'NONE',  ( -4.140888306088402970, -48.57836392318088059, 40.56393780175194763 ) ) ;
#102747=FILL_AREA_STYLE ('',( #20287 ) ) ;
#102774=CARTESIAN_POINT ( 'NONE',  ( 6.138844529812615747, -12.09084599930882931, -8.896264339907997254 ) ) ;
#102776=VERTEX_POINT ( 'NONE', #15626 ) ;
#102779=VECTOR ( 'NONE', #38681, 1000.000000000000000 ) ;
#102790=CARTESIAN_POINT ( 'NONE',  ( -13.77150638301485941, -57.01344421731529621, 24.47399976921181519 ) ) ;
#102792=CIRCLE ( 'NONE', #94169, 18.00000000000000000 ) ;
#102795=CARTESIAN_POINT ( 'NONE',  ( 11.46095665410260267, -1.517388566600422539, 20.53707809498644821 ) ) ;
#102830=COLOUR_RGB ( '', 0.08235294, 0.09019608, 0.10196078) ;
#102843=( GEOMETRIC_REPRESENTATION_CONTEXT ( 3 ) GLOBAL_UNCERTAINTY_ASSIGNED_CONTEXT ( ( #40794 ) ) GLOBAL_UNIT_ASSIGNED_CONTEXT ( ( #29367, #95141, #13123 ) ) REPRESENTATION_CONTEXT ( 'NONE', 'WORKASPACE' ) );
#102849=FILL_AREA_STYLE_COLOUR ( '', #757 ) ;
#102875=CARTESIAN_POINT ( 'NONE',  ( 30.00000000000000000, 1.836970198721029589E-15, -15.00000000000000000 ) ) ;
#102877=DIRECTION ( 'NONE',  ( -0.000000000000000000, -1.000000000000000000, -0.000000000000000000 ) ) ;
#102909=CARTESIAN_POINT ( 'NONE',  ( 4.942316422488831407, -67.89573842932429670, 13.89850810157859229 ) ) ;
#102915=CARTESIAN_POINT ( 'NONE',  ( -12.56633547050704003, -10.06780447540685408, 11.12955203454668585 ) ) ;
#102916=AXIS2_PLACEMENT_3D ( 'NONE', #100422, #26588, #66464 ) ;
#102978=CARTESIAN_POINT ( 'NONE',  ( 3.301573598373376939, -0.7118794392489854461, 103.9445864789742728 ) ) ;
#102992=CARTESIAN_POINT ( 'NONE',  ( -11.91718080433585314, -2.063830786854366384, 20.64942540265304416 ) ) ;
#103006=LINE ( 'NONE', #29164, #27129 ) ;
#103016=DIRECTION ( 'NONE',  ( 0.000000000000000000, 0.000000000000000000, 1.000000000000000000 ) ) ;
#103025=CARTESIAN_POINT ( 'NONE',  ( -3.544943868593964709, -69.77176130519234221, 13.45484724895946904 ) ) ;
#103026=SURFACE_STYLE_USAGE ( .BOTH. , #93341 ) ;
#103029=CARTESIAN_POINT ( 'NONE',  ( 8.999999999999996447, -4.000000000000003553, 42.58845726811989607 ) ) ;
#103034=CARTESIAN_POINT ( 'NONE',  ( -13.95403936970824965, -50.13007754844869623, 28.16216733762122004 ) ) ;
#103081=ORIENTED_EDGE ( 'NONE', *, *, #14366, .T. ) ;
#103084=SURFACE_STYLE_USAGE ( .BOTH. , #39937 ) ;
#103108=COLOUR_RGB ( '', 0.08235294, 0.09019608, 0.10196078) ;
#103109=CARTESIAN_POINT ( 'NONE',  ( -4.392764327028860549, -48.86087519462214601, 104.3925874334283179 ) ) ;
#103113=EDGE_CURVE ( 'NONE', #104941, #11338, #46816, .T. ) ;
#103116=UNCERTAINTY_MEASURE_WITH_UNIT (LENGTH_MEASURE( 1.000000000000000082E-05 ), #36334, 'distance_accuracy_value', 'NONE');
#103136=UNCERTAINTY_MEASURE_WITH_UNIT (LENGTH_MEASURE( 1.000000000000000082E-05 ), #25715, 'distance_accuracy_value', 'NONE');
#103165=AXIS2_PLACEMENT_3D ( 'NONE', #95417, #71136, #20533 ) ;
#103179=CARTESIAN_POINT ( 'NONE',  ( 1.000000000000000000, -48.52751354259076777, 2.643394033303763546 ) ) ;
#103184=AXIS2_PLACEMENT_3D ( 'NONE', #943, #25854, #59779 ) ;
#103187=CARTESIAN_POINT ( 'NONE',  ( 4.551587301587300516, -1.200583151104944069, 104.4018401814738013 ) ) ;
#103223=PRESENTATION_STYLE_ASSIGNMENT (( #103744 ) ) ;
#103228=ORIENTED_EDGE ( 'NONE', *, *, #75635, .T. ) ;
#103247=CARTESIAN_POINT ( 'NONE',  ( -11.20109389684249734, -9.957101141484953288, 18.59593266893761765 ) ) ;
#103249=CARTESIAN_POINT ( 'NONE',  ( -1.533598151288847911, -49.97300464335175718, 44.88852685968546297 ) ) ;
#103265=FILL_AREA_STYLE ('',( #54686 ) ) ;
#103279=TOROIDAL_SURFACE ( 'NONE', #41213, 11.00000000000000000, 2.000000000000000000 ) ;
#103307=ORIENTED_EDGE ( 'NONE', *, *, #1969, .T. ) ;
#103312=CARTESIAN_POINT ( 'NONE',  ( 7.000000000000000000, -14.05766640829038039, -5.232782735144291486 ) ) ;
#103326=( NAMED_UNIT ( * ) PLANE_ANGLE_UNIT ( ) SI_UNIT ( $, .RADIAN. ) );
#103379=CARTESIAN_POINT ( 'NONE',  ( 13.99656100229485389, -50.02536491266853602, 26.59581618167199579 ) ) ;
#103380=CARTESIAN_POINT ( 'NONE',  ( 0.000000000000000000, -80.00000000000000000, 27.00000000000000000 ) ) ;
#103442=CARTESIAN_POINT ( 'NONE',  ( -10.86574196480413335, -11.19705879606434529, 9.983399294863108508 ) ) ;
#103493=CARTESIAN_POINT ( 'NONE',  ( 4.051286199644070329, -1.398729870307595879, 103.8758286790405236 ) ) ;
#103502=CARTESIAN_POINT ( 'NONE',  ( 0.9999999999999941158, -1.734723475976807094E-15, 101.0455488498966758 ) ) ;
#103514=CARTESIAN_POINT ( 'NONE',  ( -9.960308305544327112, -2.965541965107718614, 15.28860432758946075 ) ) ;
#103520=COLOUR_RGB ( '', 0.31764706, 0.68627451, 0.89019608) ;
#103535=DIRECTION ( 'NONE',  ( -1.000000000000000000, 0.000000000000000000, 0.000000000000000000 ) ) ;
#103546=CARTESIAN_POINT ( 'NONE',  ( -6.124999999999272582, -61.24691634665675366, 14.41094225130375683 ) ) ;
#103551=CARTESIAN_POINT ( 'NONE',  ( 3.454253436624921569, -49.15858197120396511, 103.7259032015043090 ) ) ;
#103567=( GEOMETRIC_REPRESENTATION_CONTEXT ( 3 ) GLOBAL_UNCERTAINTY_ASSIGNED_CONTEXT ( ( #101979 ) ) GLOBAL_UNIT_ASSIGNED_CONTEXT ( ( #13568, #29803, #95056 ) ) REPRESENTATION_CONTEXT ( 'NONE', 'WORKASPACE' ) );
#103654=CARTESIAN_POINT ( 'NONE',  ( -1.545654944154558175, -0.02845455282771877301, 101.5781950003720624 ) ) ;
#103688=DIRECTION ( 'NONE',  ( 0.000000000000000000, 0.000000000000000000, -1.000000000000000000 ) ) ;
#103700=CARTESIAN_POINT ( 'NONE',  ( 5.000000000000000000, -62.87212009006479008, 13.68440685388289602 ) ) ;
#103710=EDGE_LOOP ( 'NONE', ( #6372, #77385, #71044, #10394 ) ) ;
#103713=VERTEX_POINT ( 'NONE', #14846 ) ;
#103724=AXIS2_PLACEMENT_3D ( 'NONE', #74426, #18901, #58802 ) ;
#103744=SURFACE_STYLE_USAGE ( .BOTH. , #3466 ) ;
#103751=EDGE_CURVE ( 'NONE', #63106, #5701, #8753, .T. ) ;
#103771=CARTESIAN_POINT ( 'NONE',  ( -0.7777777777777783452, -50.00000000000000711, 40.97837836547554957 ) ) ;
#103789=AXIS2_PLACEMENT_3D ( 'NONE', #376, #26346, #59207 ) ;
#103803=EDGE_CURVE ( 'NONE', #102776, #10296, #36378, .T. ) ;
#103818=DIRECTION ( 'NONE',  ( 0.000000000000000000, 1.000000000000000000, 0.000000000000000000 ) ) ;
#103823=MECHANICAL_DESIGN_GEOMETRIC_PRESENTATION_REPRESENTATION('',(#15971),#95220);
#103828=CARTESIAN_POINT ( 'NONE',  ( 6.931097425531398848, -13.59559899332509225, -6.365431243532045258 ) ) ;
#103830=ORIENTED_EDGE ( 'NONE', *, *, #56773, .F. ) ;
#103837=VERTEX_POINT ( 'NONE', #57420 ) ;
#103841=SURFACE_SIDE_STYLE ('',( #88730 ) ) ;
#103876=EDGE_LOOP ( 'NONE', ( #31591, #102136, #36481 ) ) ;
#103895=CARTESIAN_POINT ( 'NONE',  ( 13.95266368664216294, -50.20567487918883387, 25.82453759514263680 ) ) ;
#103919=B_SPLINE_CURVE_WITH_KNOTS ( 'NONE', 3,
 ( #88719, #72523, #73569, #14810 ),
 .UNSPECIFIED., .F., .F.,
 ( 4, 4 ),
 ( 0.000000000000000000, 0.0008765341530664233537 ),
 .UNSPECIFIED. ) ;
#103933=( LENGTH_UNIT ( ) NAMED_UNIT ( * ) SI_UNIT ( .MILLI., .METRE. ) );
#103944=B_SPLINE_CURVE_WITH_KNOTS ( 'NONE', 3,
 ( #44788, #3787, #39868, #82443, #65733, #81891, #32323, #80836 ),
 .UNSPECIFIED., .F., .F.,
 ( 4, 2, 2, 4 ),
 ( 0.000000000000000000, 0.0002399520006080664222, 0.0004799040012161328445, 0.0009598080024322654721 ),
 .UNSPECIFIED. ) ;
#103961=CARTESIAN_POINT ( 'NONE',  ( -8.239527348356862291, -12.24602314337617059, 8.669075505165368511 ) ) ;
#103969=CIRCLE ( 'NONE', #76406, 4.000000000000002665 ) ;
#103987=CARTESIAN_POINT ( 'NONE',  ( -4.999999999999999112, 0.000000000000000000, 35.66025403784438197 ) ) ;
#103991=FILL_AREA_STYLE ('',( #95385 ) ) ;
#104022=CARTESIAN_POINT ( 'NONE',  ( 3.677584134044427078, -1.015418994119225760, 104.5297932675492234 ) ) ;
#104034=CARTESIAN_POINT ( 'NONE',  ( -9.620303054984660207, -0.5026337155641874554, 19.91726907925657386 ) ) ;
#104045=ORIENTED_EDGE ( 'NONE', *, *, #18891, .F. ) ;
#104051=ORIENTED_EDGE ( 'NONE', *, *, #91945, .T. ) ;
#104063=CARTESIAN_POINT ( 'NONE',  ( -5.000000000000000000, -14.11573700085287442, 9.475244962101804447 ) ) ;
#104095=CARTESIAN_POINT ( 'NONE',  ( 4.324717655747504885, -48.88831368632219210, 104.4045892612655990 ) ) ;
#104097=UNCERTAINTY_MEASURE_WITH_UNIT (LENGTH_MEASURE( 1.000000000000000082E-05 ), #60796, 'distance_accuracy_value', 'NONE');
#104121=CARTESIAN_POINT ( 'NONE',  ( 3.363648053944603422, -48.78517836376548189, 104.5995868353016505 ) ) ;
#104137=EDGE_LOOP ( 'NONE', ( #27187, #70441, #72210, #41796, #64824 ) ) ;
#104152=CARTESIAN_POINT ( 'NONE',  ( -5.000000000000000000, -14.29242795212260297, -6.555798487938274910 ) ) ;
#104166=COLOUR_RGB ( '', 0.72549020, 0.75294118, 0.79215686) ;
#104172=EDGE_LOOP ( 'NONE', ( #34677, #69052, #8849 ) ) ;
#104175=CARTESIAN_POINT ( 'NONE',  ( -1.238932115551811597, -1.825546356131314218E-15, 101.3452916561003434 ) ) ;
#104179=( NAMED_UNIT ( * ) SI_UNIT ( $, .STERADIAN. ) SOLID_ANGLE_UNIT ( ) );
#104180=SURFACE_SIDE_STYLE ('',( #71285 ) ) ;
#104185=AXIS2_PLACEMENT_3D ( 'NONE', #12349, #3213, #52275 ) ;
#104204=CARTESIAN_POINT ( 'NONE',  ( 13.72589306172073442, -57.01108507920052659, 29.76321791924474525 ) ) ;
#104219=CARTESIAN_POINT ( 'NONE',  ( 5.000000000000000000, -38.85173860975186955, 2.939083565186168201 ) ) ;
#104360=UNCERTAINTY_MEASURE_WITH_UNIT (LENGTH_MEASURE( 1.000000000000000082E-05 ), #103933, 'distance_accuracy_value', 'NONE');
#104366=CARTESIAN_POINT ( 'NONE',  ( 7.114815031913489740, 3.125246181595257688, 14.67111259585466954 ) ) ;
#104368=VERTEX_POINT ( 'NONE', #74319 ) ;
#104405=FILL_AREA_STYLE ('',( #57429 ) ) ;
#104422=CARTESIAN_POINT ( 'NONE',  ( 13.49952125780149714, -52.22498368979241690, 30.71129996282902397 ) ) ;
#104423=CARTESIAN_POINT ( 'NONE',  ( 0.000000000000000000, 0.000000000000000000, 27.00000000000000000 ) ) ;
#104466=CARTESIAN_POINT ( 'NONE',  ( -4.526657684027568074, -2.093347780961939186, 103.5746540667394555 ) ) ;
#104477=SURFACE_STYLE_USAGE ( .BOTH. , #47818 ) ;
#104485=ADVANCED_FACE ( 'NONE', ( #4169 ), #94160, .F. ) ;
#104488=ORIENTED_EDGE ( 'NONE', *, *, #33854, .F. ) ;
#104496=CARTESIAN_POINT ( 'NONE',  ( -9.235252277563404277, -13.40511626313917048, 16.47531707632386500 ) ) ;
#104522=TOROIDAL_SURFACE ( 'NONE', #11508, 12.00000000000000000, 2.000000000000000000 ) ;
#104524=CARTESIAN_POINT ( 'NONE',  ( 1.450845733305902385, -0.02389980327605355920, 101.4859859777359077 ) ) ;
#104537=MECHANICAL_DESIGN_GEOMETRIC_PRESENTATION_REPRESENTATION('',(#68368),#30503);
#104548=EDGE_LOOP ( 'NONE', ( #94485, #53513, #73337, #39578 ) ) ;
#104595=CARTESIAN_POINT ( 'NONE',  ( -6.018857979291350802, -63.35165937125906765, 14.35967520096848027 ) ) ;
#104598=CYLINDRICAL_SURFACE ( 'NONE', #58257, 9.999999999999994671 ) ;
#104605=CARTESIAN_POINT ( 'NONE',  ( -15.90614609307868399, -4.000000000000002665, 18.57417562100670949 ) ) ;
#104662=CARTESIAN_POINT ( 'NONE',  ( -9.933618426942553370, -50.20576216351469867, 25.82409549033520690 ) ) ;
#104684=( BOUNDED_SURFACE ( )  B_SPLINE_SURFACE ( 3, 2, ( 
 ( #92381, #42775, #75667 ),
 ( #92915, #34725, #93990 ),
 ( #58976, #51919, #51387 ),
 ( #52451, #67598, #100476 ),
 ( #36330, #50849, #20150 ),
 ( #27706, #26636, #59507 ),
 ( #43836, #35245, #2298 ),
 ( #18527, #27167, #84302 ),
 ( #28230, #11455, #44381 ),
 ( #11993, #2840, #10397 ),
 ( #43313, #10918, #85922 ),
 ( #76196, #91863, #60580 ) ),
 .UNSPECIFIED., .F., .F., .F. ) 
 B_SPLINE_SURFACE_WITH_KNOTS ( ( 4, 2, 2, 2, 2, 4 ),
 ( 3, 3 ),
 ( 7.589415207398531038E-19, 0.0007735885786023073089, 0.001547177157204613750, 0.001933971446505767080, 0.002320765735806920409, 0.003094354314409226633 ),
 ( 0.000000000000000000, 1.000000000000000000 ),
 .UNSPECIFIED. ) 
 GEOMETRIC_REPRESENTATION_ITEM ( )  RATIONAL_B_SPLINE_SURFACE ( (
 ( 1.000000000000000000, 0.9603284238771496728, 1.000000000000000000),
 ( 1.000000000000000000, 0.9628724889917197327, 1.000000000000000000),
 ( 1.000000000000000000, 0.9663306537743611146, 1.000000000000000000),
 ( 1.000000000000000000, 0.9744563874115511615, 1.000000000000000000),
 ( 1.000000000000000000, 0.9789903143386995410, 1.000000000000000000),
 ( 1.000000000000000000, 0.9855527733005633451, 1.000000000000000000),
 ( 1.000000000000000000, 0.9877025284829050733, 1.000000000000000000),
 ( 1.000000000000000000, 0.9916277982505179445, 1.000000000000000000),
 ( 1.000000000000000000, 0.9934221110298004920, 1.000000000000000000),
 ( 1.000000000000000000, 0.9980179737616273750, 1.000000000000000000),
 ( 1.000000000000000000, 1.000016370385754527, 1.000000000000000000),
 ( 1.000000000000000000, 1.000000000000000000, 1.000000000000000000) ) ) 
 REPRESENTATION_ITEM ( '' )  SURFACE ( )  );
#104688=CARTESIAN_POINT ( 'NONE',  ( -4.628159615119684211, -47.68919827030617142, 102.5435725457686118 ) ) ;
#104710=CARTESIAN_POINT ( 'NONE',  ( -2.321165800182275252, -0.2152620590929751054, 102.3911379722518262 ) ) ;
#104757=CARTESIAN_POINT ( 'NONE',  ( 5.000000000000000888, -59.33342285675411176, 7.478329308075513104 ) ) ;
#104759=( LENGTH_UNIT ( ) NAMED_UNIT ( * ) SI_UNIT ( .MILLI., .METRE. ) );
#104783=CARTESIAN_POINT ( 'NONE',  ( -3.995243879123565378, -48.66248409693900356, 43.59136604025376016 ) ) ;
#104790=STYLED_ITEM ( 'NONE', ( #77118 ), #44186 ) ;
#104818=EDGE_CURVE ( 'NONE', #76724, #50280, #12116, .T. ) ;
#104821=CARTESIAN_POINT ( 'NONE',  ( 0.000000000000000000, -80.00000000000000000, 27.00000000000000000 ) ) ;
#104825=ADVANCED_FACE ( 'NONE', ( #95706, #96253 ), #86575, .T. ) ;
#104941=VERTEX_POINT ( 'NONE', #76717 ) ;
#104989=CARTESIAN_POINT ( 'NONE',  ( -3.040531029381596806, -49.16841272187355116, 104.0108099329909095 ) ) ;
#105009=CARTESIAN_POINT ( 'NONE',  ( -4.642888266381866913, -2.342832151813632802, 102.5319024079573751 ) ) ;
#105015=( BOUNDED_SURFACE ( )  B_SPLINE_SURFACE ( 3, 2, ( 
 ( #94525, #79897, #61633 ),
 ( #80424, #88012, #104175 ),
 ( #103654, #71801, #79373 ),
 ( #72347, #53516, #46998 ),
 ( #104710, #95570, #30863 ),
 ( #14619, #47529, #6533 ),
 ( #39466, #105249, #20677 ),
 ( #54544, #62680, #78311 ),
 ( #38416, #86964, #86443 ),
 ( #63209, #37368, #96100 ) ),
 .UNSPECIFIED., .F., .F., .F. ) 
 B_SPLINE_SURFACE_WITH_KNOTS ( ( 4, 2, 2, 2, 4 ),
 ( 3, 3 ),
 ( -1.185673698477775140E-05, 0.001057471059733317183, 0.002126798856451412017, 0.003196126653169506851, 0.004265454449887602119 ),
 ( 0.000000000000000000, 1.000000000000000000 ),
 .UNSPECIFIED. ) 
 GEOMETRIC_REPRESENTATION_ITEM ( )  RATIONAL_B_SPLINE_SURFACE ( (
 ( 1.000000000000000000, 1.000000000000000000, 1.000000000000000000),
 ( 1.000000000000000000, 0.9999925199709330803, 1.000000000000000000),
 ( 1.000000000000000000, 0.9961033022472992604, 1.000000000000000000),
 ( 1.000000000000000000, 0.9800616282250097511, 1.000000000000000000),
 ( 1.000000000000000000, 0.9678427155945901195, 1.000000000000000000),
 ( 1.000000000000000000, 0.9345111840693876015, 1.000000000000000000),
 ( 1.000000000000000000, 0.9135791977929141883, 1.000000000000000000),
 ( 1.000000000000000000, 0.8625981283153052459, 1.000000000000000000),
 ( 1.000000000000000000, 0.8325406200923007871, 1.000000000000000000),
 ( 1.000000000000000000, 0.7974033994356889421, 1.000000000000000000) ) ) 
 REPRESENTATION_ITEM ( '' )  SURFACE ( )  );
#105021=CARTESIAN_POINT ( 'NONE',  ( 6.249254171376327882, -12.00724809823987549, 11.39149369528576017 ) ) ;
#105038=( NAMED_UNIT ( * ) SI_UNIT ( $, .STERADIAN. ) SOLID_ANGLE_UNIT ( ) );
#105043=CARTESIAN_POINT ( 'NONE',  ( -9.773816476656509877, -12.75255233517122022, 16.96466978235007161 ) ) ;
#105139=CARTESIAN_POINT ( 'NONE',  ( -4.999999999999959144, -13.68989806552422728, 13.02619096221388517 ) ) ;
#105146=AXIS2_PLACEMENT_3D ( 'NONE', #39453, #38400, #48036 ) ;
#105147=ADVANCED_FACE ( 'NONE', ( #94531 ), #36321, .F. ) ;
#105198=CARTESIAN_POINT ( 'NONE',  ( 9.933368185767806224, -50.20648247506351680, 25.82212275612567964 ) ) ;
#105249=CARTESIAN_POINT ( 'NONE',  ( -2.894864961505325240, -0.4655938164488910291, 103.3614437639293584 ) ) ;
#105251=UNCERTAINTY_MEASURE_WITH_UNIT (LENGTH_MEASURE( 1.000000000000000082E-05 ), #679, 'distance_accuracy_value', 'NONE');
#105292=CARTESIAN_POINT ( 'NONE',  ( 5.000000000000000000, -68.02076148470871431, 16.47608826392310277 ) ) ;
#105294=CARTESIAN_POINT ( 'NONE',  ( 10.66896053074161088, -11.24066709036755007, 17.92507180936227940 ) ) ;
#105308=B_SPLINE_CURVE_WITH_KNOTS ( 'NONE', 3,
 ( #71200, #78756, #104095, #22690, #62599, #21628, #14014, #30235 ),
 .UNSPECIFIED., .F., .F.,
 ( 4, 2, 2, 4 ),
 ( 0.000000000000000000, 7.350793746623692176E-05, 0.0001470158749324738435, 0.0002940317498649437297 ),
 .UNSPECIFIED. ) ;
#105317=CARTESIAN_POINT ( 'NONE',  ( -4.438869422347556437, -48.05855701245207001, 43.18766101621736908 ) ) ;
#105327=CARTESIAN_POINT ( 'NONE',  ( -9.667921046838758414, -57.17403655832323039, 29.56517872135010094 ) ) ;
#105353=SURFACE_STYLE_USAGE ( .BOTH. , #22870 ) ;
#105358=CIRCLE ( 'NONE', #15808, 4.000000000000003553 ) ;
#105363=CARTESIAN_POINT ( 'NONE',  ( -1.000000000000000222, -59.21823443912413865, 7.425173686806289197 ) ) ;
#105386=CARTESIAN_POINT ( 'NONE',  ( -1.000000000000000888, -46.00000000000000000, 40.07669683062201926 ) ) ;
#105393=EDGE_CURVE ( 'NONE', #103837, #12868, #90661, .T. ) ;
#105442=CARTESIAN_POINT ( 'NONE',  ( 9.684147237222786586, 2.793897972684820985, 14.73931554192828663 ) ) ;
#105457=CARTESIAN_POINT ( 'NONE',  ( -3.088900377613861270, -69.43752249126038123, 13.34077525874367076 ) ) ;
#105472=PRESENTATION_STYLE_ASSIGNMENT (( #96863 ) ) ;
#105498=CARTESIAN_POINT ( 'NONE',  ( 15.26476282643411864, -0.4519630325742635679, 14.99528456596575232 ) ) ;
#105513=SURFACE_SIDE_STYLE ('',( #47270 ) ) ;
#105530=CARTESIAN_POINT ( 'NONE',  ( -5.603804764709576780, -2.702239074867451407, 103.9691152301460590 ) ) ;
#105533=ORIENTED_EDGE ( 'NONE', *, *, #43815, .F. ) ;
#105542=B_SPLINE_CURVE_WITH_KNOTS ( 'NONE', 3,
 ( #49741, #105849, #83697, #82650, #24967, #73473 ),
 .UNSPECIFIED., .F., .F.,
 ( 4, 2, 4 ),
 ( 2.611104600503255956E-18, 0.0003916983043530442889, 0.0007833966087060859756 ),
 .UNSPECIFIED. ) ;
#105555=CARTESIAN_POINT ( 'NONE',  ( -1.226412146326429475, -69.63306384108153679, 12.78930087777542646 ) ) ;
#105588=CARTESIAN_POINT ( 'NONE',  ( -4.464768147783013674, -48.00301508167383702, 102.6740199126133888 ) ) ;
#105591=ORIENTED_EDGE ( 'NONE', *, *, #14502, .F. ) ;
#105606=CARTESIAN_POINT ( 'NONE',  ( 4.335182740490085784, -1.119534022499610426, 104.3855524028841160 ) ) ;
#105627=ORIENTED_EDGE ( 'NONE', *, *, #103751, .F. ) ;
#105637=EDGE_CURVE ( 'NONE', #97430, #40622, #69286, .T. ) ;
#105651=ORIENTED_EDGE ( 'NONE', *, *, #36786, .F. ) ;
#105655=CARTESIAN_POINT ( 'NONE',  ( -4.999999999999920952, -12.45789892056845716, 11.15956302481699502 ) ) ;
#105665=CIRCLE ( 'NONE', #59198, 9.000000000000000000 ) ;
#105694=ORIENTED_EDGE ( 'NONE', *, *, #62702, .F. ) ;
#105718=CARTESIAN_POINT ( 'NONE',  ( -9.287587386881233087, -52.21912220077189914, 30.70844757271691350 ) ) ;
#105728=B_SPLINE_CURVE_WITH_KNOTS ( 'NONE', 3,
 ( #69625, #105555, #31695, #86356, #53940, #95478, #21109, #72657, #23608, #48374, #94972, #94438, #62081, #13479, #4346, #86876, #3823, #11898, #87404, #7378, #21623, #80741, #15484, #20598 ),
 .UNSPECIFIED., .F., .F.,
 ( 4, 2, 2, 2, 2, 2, 2, 2, 2, 2, 2, 4 ),
 ( 2.105069348217797382E-15, 0.0006796014968221845759, 0.001019402245232224483, 0.001359202993642264065, 0.002038804490462343879, 0.002718405987282424344, 0.003398007484102504375, 0.004077608980922584406, 0.005436811974562746202, 0.006796014968202907132, 0.008155217961843066327, 0.01087362394912343155 ),
 .UNSPECIFIED. ) ;
#105738=STYLED_ITEM ( 'NONE', ( #29623 ), #97546 ) ;
#105740=ORIENTED_EDGE ( 'NONE', *, *, #55334, .F. ) ;
#105809=CARTESIAN_POINT ( 'NONE',  ( 9.981808881366681874, -57.97224676535203969, 27.65604031336897251 ) ) ;
#105830=EDGE_CURVE ( 'NONE', #104368, #35586, #8813, .T. ) ;
#105849=CARTESIAN_POINT ( 'NONE',  ( -3.778364440264291524, -1.120180266064636276, 103.2432911248131120 ) ) ;
#105887=CARTESIAN_POINT ( 'NONE',  ( -3.857142857142847880, -48.79941684889506348, 103.1763305333244318 ) ) ;
#105970=CARTESIAN_POINT ( 'NONE',  ( -5.076380833017271499, -61.76466786245471496, 13.90212445768889360 ) ) ;
#106003=( NAMED_UNIT ( * ) SI_UNIT ( $, .STERADIAN. ) SOLID_ANGLE_UNIT ( ) );
#106027=( NAMED_UNIT ( * ) PLANE_ANGLE_UNIT ( ) SI_UNIT ( $, .RADIAN. ) );
#106043=CARTESIAN_POINT ( 'NONE',  ( -5.000000000093224095, -3.772466818847465042, 103.2791840072271015 ) ) ;
#106076=CARTESIAN_POINT ( 'NONE',  ( 5.833333333333327708, -46.00000000000000000, 103.8776713793258608 ) ) ;
#106086=EDGE_LOOP ( 'NONE', ( #64329, #12665, #63886, #75187, #105651, #68941 ) ) ;
#106089=CIRCLE ( 'NONE', #18285, 2.000000000000000444 ) ;
#106091=CARTESIAN_POINT ( 'NONE',  ( -6.697922209380616110, -13.04455172910126137, -7.429582257095876052 ) ) ;
#106099=B_SPLINE_CURVE_WITH_KNOTS ( 'NONE', 3,
 ( #36336, #2305, #44386, #99952, #84310, #19625, #10405, #59513, #2845, #52458, #69205, #35797, #68121, #75673, #34732, #102074, #101556, #28235, #27712, #85375, #101017, #67603 ),
 .UNSPECIFIED., .F., .F.,
 ( 4, 2, 2, 2, 2, 2, 2, 2, 2, 2, 4 ),
 ( 5.553824967135426632E-18, 0.001048074399358199906, 0.002096148798716394174, 0.003144223198074588659, 0.004192297597432782276, 0.005240371996790976761, 0.005764409196470074437, 0.006288446396149171246, 0.006812483595828268054, 0.007336520795507365730, 0.008384595194865552409 ),
 .UNSPECIFIED. ) ;
#106106=CARTESIAN_POINT ( 'NONE',  ( -4.750186375024242125, -48.62189236691707350, 104.3180500829685258 ) ) ;
#106112=DIRECTION ( 'NONE',  ( 0.000000000000000000, 0.000000000000000000, -1.000000000000000000 ) ) ;
#106141=CARTESIAN_POINT ( 'NONE',  ( -1.000000000000000666, 0.000000000000000000, 42.58845726811989607 ) ) ;
#106145=EDGE_CURVE ( 'NONE', #30348, #95128, #79578, .T. ) ;
#106172=CARTESIAN_POINT ( 'NONE',  ( -5.000000000000039968, -14.19087030044497943, 13.37859801193910769 ) ) ;
#106237=CARTESIAN_POINT ( 'NONE',  ( -9.171168021175072127, -52.95225154708963800, 30.98659277684255997 ) ) ;
#106248=CARTESIAN_POINT ( 'NONE',  ( 5.596957125887387363, -47.31575451833740686, 103.9718581041641698 ) ) ;
#106262=CARTESIAN_POINT ( 'NONE',  ( -4.382959417677086300, -48.13794921561773776, 102.7400018439556533 ) ) ;
#106291=CARTESIAN_POINT ( 'NONE',  ( -13.27939269558071622, 1.397586449971225164, 14.93522390679500234 ) ) ;
#106323=CARTESIAN_POINT ( 'NONE',  ( 9.499205784528923502, -56.64306915247485819, 30.13083833152229829 ) ) ;
#106333=CARTESIAN_POINT ( 'NONE',  ( 8.238879630815576505, -5.127845683665249510, 14.25497928744678333 ) ) ;
#106359=CARTESIAN_POINT ( 'NONE',  ( -6.736021983150922487, -48.35471770697892424, 39.27387210330255840 ) ) ;
#106363=CARTESIAN_POINT ( 'NONE',  ( -9.498520115305538525, -56.64062589231861011, 30.13282173121349317 ) ) ;
#106375=( GEOMETRIC_REPRESENTATION_CONTEXT ( 3 ) GLOBAL_UNCERTAINTY_ASSIGNED_CONTEXT ( ( #89069 ) ) GLOBAL_UNIT_ASSIGNED_CONTEXT ( ( #17184, #47532, #64274 ) ) REPRESENTATION_CONTEXT ( 'NONE', 'WORKASPACE' ) );
#106376=CARTESIAN_POINT ( 'NONE',  ( 4.628159615119684211, -2.310801729693849005, 102.5435725457685976 ) ) ;
#106389=EDGE_CURVE ( 'NONE', #76782, #40039, #26201, .T. ) ;
#106397=ORIENTED_EDGE ( 'NONE', *, *, #76707, .T. ) ;
#106415=CIRCLE ( 'NONE', #23783, 8.142857142857131691 ) ;
#106433=B_SPLINE_CURVE_WITH_KNOTS ( 'NONE', 3,
 ( #3160, #4756, #3705, #11230, #60879, #44698, #36104, #101848, #36631, #62468, #20990, #53310, #27481, #70559, #101329, #44155 ),
 .UNSPECIFIED., .F., .F.,
 ( 4, 2, 2, 2, 2, 2, 2, 4 ),
 ( 0.000000000000000000, 0.001820320936770163881, 0.003640641873540327762, 0.005460962810310492077, 0.007281283747080655525, 0.01092192562062098415, 0.01274224655739114760, 0.01456256749416131105 ),
 .UNSPECIFIED. ) ;
#106461=CARTESIAN_POINT ( 'NONE',  ( -6.999999999999994671, -46.00000000000000000, 102.2532056551910387 ) ) ;
#106483=CARTESIAN_POINT ( 'NONE',  ( -5.000000000000000000, -15.93202192939577344, -5.930487099830192399 ) ) ;
#106505=CARTESIAN_POINT ( 'NONE',  ( -4.990218406113974936, -61.74584101121605784, 12.75302187936684994 ) ) ;
#106506=CARTESIAN_POINT ( 'NONE',  ( -30.00000000000000000, -54.00000000000000711, 23.11721482942554928 ) ) ;
#106514=( LENGTH_UNIT ( ) NAMED_UNIT ( * ) SI_UNIT ( .MILLI., .METRE. ) );
#106530=LINE ( 'NONE', #91438, #11953 ) ;
#106545=AXIS2_PLACEMENT_3D ( 'NONE', #77133, #84167, #25976 ) ;
#106584=COLOUR_RGB ( '', 0.09019608, 0.27058824, 0.51372549) ;
#106586=CARTESIAN_POINT ( 'NONE',  ( 3.991147588110782074, -1.050389752018302314, 104.5610969444638556 ) ) ;
#106588=DIRECTION ( 'NONE',  ( 0.000000000000000000, 0.000000000000000000, -1.000000000000000000 ) ) ;
#106613=DIRECTION ( 'NONE',  ( -0.1091179629862816802, 0.9940288075069678708, 0.000000000000000000 ) ) ;
#106614=CARTESIAN_POINT ( 'NONE',  ( 6.594225035609136754, -11.92007582869072735, 9.808253832663687888 ) ) ;
#106619=CARTESIAN_POINT ( 'NONE',  ( 4.999999999999993783, -45.99999999999999289, 103.2791840072761858 ) ) ;
#106646=CARTESIAN_POINT ( 'NONE',  ( -4.399054598113077752, -48.11244280224737935, 102.7269706464928021 ) ) ;
#106650=CARTESIAN_POINT ( 'NONE',  ( 3.040134639727833044, -49.16875784325965526, 104.0101424759970428 ) ) ;
#106651=CYLINDRICAL_SURFACE ( 'NONE', #14109, 2.000000000000000000 ) ;
#106654=UNCERTAINTY_MEASURE_WITH_UNIT (LENGTH_MEASURE( 1.000000000000000082E-05 ), #61638, 'distance_accuracy_value', 'NONE');
#106663=DIRECTION ( 'NONE',  ( 0.000000000000000000, 1.000000000000000000, 0.000000000000000000 ) ) ;
#106665=DIRECTION ( 'NONE',  ( 0.000000000000000000, 0.000000000000000000, -1.000000000000000000 ) ) ;
#106698=VECTOR ( 'NONE', #58980, 1000.000000000000000 ) ;
#106699=SURFACE_SIDE_STYLE ('',( #64659 ) ) ;
#106700=CARTESIAN_POINT ( 'NONE',  ( 15.90614609307868577, -4.000000000000003553, 18.57417562100670949 ) ) ;
#106713=TOROIDAL_SURFACE ( 'NONE', #46525, 11.00000000000000000, 2.000000000000000000 ) ;
#106714=CARTESIAN_POINT ( 'NONE',  ( -5.000000000000000000, -13.96166769374574024, 11.51022196660654195 ) ) ;
#106732=ORIENTED_EDGE ( 'NONE', *, *, #43628, .T. ) ;
#106736=CARTESIAN_POINT ( 'NONE',  ( 15.00756260254757990, -0.09903668703488825720, 15.00122431754954810 ) ) ;
#106773=CARTESIAN_POINT ( 'NONE',  ( 9.822490609848976817, -50.52957752397126967, 25.11095637839896000 ) ) ;
ENDSEC;
END-ISO-10303-21;
